ISO-10303-21;
HEADER;
FILE_DESCRIPTION (('STEP AP214'),
    '1' );
FILE_NAME ('Terminal Screw 1.step',
    '2026-10-05T22:38:29',
    ( '' ),
    ( '' ),
    'SwSTEP 2.0',
    'SolidWorks 2020',
    '' );
FILE_SCHEMA (( 'AUTOMOTIVE_DESIGN' ));
ENDSEC;

DATA;
#13=CARTESIAN_POINT ( 'NONE',  ( 11.38795122972049967, -3.601717549869600354, -6.578956058177199751 ) ) ;
#30=CARTESIAN_POINT ( 'NONE',  ( 10.08762143724499794, -3.241588663654300095, -6.646450532840099790 ) ) ;
#60=CARTESIAN_POINT ( 'NONE',  ( 9.554646554150998838, -3.380689388027600106, -8.619302797893999113 ) ) ;
#84=CARTESIAN_POINT ( 'NONE',  ( 11.18687482311539938, -2.942322404451000128, -7.927326830586499007 ) ) ;
#91=CARTESIAN_POINT ( 'NONE',  ( 11.59999999999999964, -4.640264089079230381, -6.808168915892154338 ) ) ;
#130=CARTESIAN_POINT ( 'NONE',  ( 11.04749144726329924, -4.500836215462999945, -6.793273974143599681 ) ) ;
#142=CARTESIAN_POINT ( 'NONE',  ( 8.851468108405999402, -3.165798890946399879, -7.736255015838599647 ) ) ;
#155=CARTESIAN_POINT ( 'NONE',  ( 10.85679632507500081, -3.509334349252600127, -8.409605917786398877 ) ) ;
#173=CARTESIAN_POINT ( 'NONE',  ( 9.593930206849998754, -2.750000000000000000, -7.500000000000000000 ) ) ;
#261=CARTESIAN_POINT ( 'NONE',  ( 9.352250488097009651, -5.092274670905195144, -6.870455438679058169 ) ) ;
#273=CARTESIAN_POINT ( 'NONE',  ( 10.96949144726329806, -4.580206776679999869, -6.681274802424499448 ) ) ;
#277=CARTESIAN_POINT ( 'NONE',  ( 11.63611496860034933, -2.828587461987000395, -6.899705789500199415 ) ) ;
#307=CARTESIAN_POINT ( 'NONE',  ( 10.94072200990529886, -5.077092948368999714, -7.124286150322599376 ) ) ;
#324=EDGE_CURVE ( 'NONE', #49260, #51205, #2147, .T. ) ;
#335=ORIENTED_EDGE ( 'NONE', *, *, #34880, .T. ) ;
#344=ORIENTED_EDGE ( 'NONE', *, *, #13743, .T. ) ;
#355=CARTESIAN_POINT ( 'NONE',  ( 10.55103166480599874, -5.000984463463999496, -7.570575893572789816 ) ) ;
#369=CARTESIAN_POINT ( 'NONE',  ( 10.08351354018237345, -2.750000000000000000, -7.663624617374468428 ) ) ;
#372=CARTESIAN_POINT ( 'NONE',  ( 9.099784697134998268, -3.380386586585000241, -6.540930833646799947 ) ) ;
#403=CARTESIAN_POINT ( 'NONE',  ( 11.16486084871730000, -2.792989229543000107, -7.174999999999999822 ) ) ;
#425=CARTESIAN_POINT ( 'NONE',  ( 10.47303166480599934, -5.137916160623999140, -7.580230465881790280 ) ) ;
#432=CARTESIAN_POINT ( 'NONE',  ( 11.27745123989519982, -3.589787500396900199, -8.292221125039500151 ) ) ;
#435=ADVANCED_FACE ( 'NONE', ( #64566 ), #48853, .T. ) ;
#472=STYLED_ITEM ( 'NONE', ( #6780 ), #31992 ) ;
#486=CARTESIAN_POINT ( 'NONE',  ( 10.16455864497999961, -3.101067942814400347, -8.204026508301600629 ) ) ;
#500=CARTESIAN_POINT ( 'NONE',  ( 11.10612378248509913, -4.482960757953799558, -6.586279795136899651 ) ) ;
#516=CARTESIAN_POINT ( 'NONE',  ( 10.30226354018233437, -5.092232985442821658, -6.870476274536374994 ) ) ;
#581=ORIENTED_EDGE ( 'NONE', *, *, #21347, .T. ) ;
#622=CARTESIAN_POINT ( 'NONE',  ( 11.58071932425156980, -4.167269912168199753, -8.628410767520000135 ) ) ;
#626=CARTESIAN_POINT ( 'NONE',  ( 11.39189666366029918, -4.052152326617509459, -8.673729056199000809 ) ) ;
#654=CARTESIAN_POINT ( 'NONE',  ( 10.34995525820099971, -4.107710726525199973, -6.364355462479999836 ) ) ;
#662=CARTESIAN_POINT ( 'NONE',  ( 10.98937577273789046, -4.461177266722074819, -8.699885912910444219 ) ) ;
#677=CARTESIAN_POINT ( 'NONE',  ( 11.46989666366029859, -4.058428102321880004, -8.814970315645998866 ) ) ;
#704=CARTESIAN_POINT ( 'NONE',  ( 11.33456651104149948, -3.887457492043800311, -6.364824110469998963 ) ) ;
#717=CARTESIAN_POINT ( 'NONE',  ( 10.05226354018249779, -2.907767014557177898, -8.129523725463625894 ) ) ;
#720=CARTESIAN_POINT ( 'NONE',  ( 10.28824205624999877, -4.360201998293100623, -8.437601616732200327 ) ) ;
#750=CARTESIAN_POINT ( 'NONE',  ( 11.37299956498129916, -5.207010770456999893, -7.174999999999999822 ) ) ;
#753=CARTESIAN_POINT ( 'NONE',  ( 10.14393020684899938, -2.750000000000000000, -7.500000000000000000 ) ) ;
#756=( GEOMETRIC_REPRESENTATION_CONTEXT ( 3 ) GLOBAL_UNCERTAINTY_ASSIGNED_CONTEXT ( ( #28801 ) ) GLOBAL_UNIT_ASSIGNED_CONTEXT ( ( #13097, #2935, #24264 ) ) REPRESENTATION_CONTEXT ( 'NONE', 'WORKASPACE' ) );
#772=CARTESIAN_POINT ( 'NONE',  ( 10.71918447801630059, -2.859536135895000442, -7.474854604063350116 ) ) ;
#779=CARTESIAN_POINT ( 'NONE',  ( 9.841846873515665450, -4.999583552997724389, -6.731816600031354625 ) ) ;
#780=CARTESIAN_POINT ( 'NONE',  ( 11.59999999999999964, -4.817420948848700313, -7.174999999999999822 ) ) ;
#833=CARTESIAN_POINT ( 'NONE',  ( 9.128076168957999670, -4.509700402263200125, -8.365475476407400635 ) ) ;
#846=CARTESIAN_POINT ( 'NONE',  ( 10.98656920625009903, -3.967932847735990531, -6.608450613814399688 ) ) ;
#861=CARTESIAN_POINT ( 'NONE',  ( 11.67766954483535891, -3.284117569315500251, -6.395429936871999566 ) ) ;
#939=CARTESIAN_POINT ( 'NONE',  ( 10.99375810342578141, -3.998140074039970848, -6.625879789168364731 ) ) ;
#959=CARTESIAN_POINT ( 'NONE',  ( 9.196006702408608291, -3.000394487162607149, -6.731788826750699783 ) ) ;
#961=CARTESIAN_POINT ( 'NONE',  ( 11.59999999999999964, -4.000000000000000000, -7.500000000000000000 ) ) ;
#970=CARTESIAN_POINT ( 'NONE',  ( 10.28026357027499849, -3.014700852776899698, -7.690095141806899903 ) ) ;
#974=FACE_OUTER_BOUND ( 'NONE', #62452, .T. ) ;
#995=CARTESIAN_POINT ( 'NONE',  ( 11.48052502238429895, -2.954316262216015065, -7.824990984965952912 ) ) ;
#1002=CARTESIAN_POINT ( 'NONE',  ( 11.33041235500449950, -4.942357465271699724, -6.636704692336500067 ) ) ;
#1007=CARTESIAN_POINT ( 'NONE',  ( 11.10391045180384140, -2.870950512581996961, -8.114538794791119614 ) ) ;
#1055=CARTESIAN_POINT ( 'NONE',  ( 10.44841638348500013, -5.108333310975999630, -7.230023356477299323 ) ) ;
#1070=CARTESIAN_POINT ( 'NONE',  ( 8.897151519676997466, -3.975306837623020062, -8.641543873690000765 ) ) ;
#1119=CARTESIAN_POINT ( 'NONE',  ( 10.09964828895399869, -2.878385131502000149, -8.112615456209400833 ) ) ;
#1129=CARTESIAN_POINT ( 'NONE',  ( 11.73671932425159881, -4.127012898954600217, -8.356835045446798560 ) ) ;
#1180=CARTESIAN_POINT ( 'NONE',  ( 8.874784697134998623, -3.454948069423500190, -6.656340890368899643 ) ) ;
#1184=B_SPLINE_SURFACE_WITH_KNOTS ( 'NONE', 3, 3, ( 
 ( #28833, #59584, #60627, #54337, #43518, #861, #38966, #1903, #55385, #22178, #33374, #50144, #59930, #39304, #64816, #1549, #33722, #44570, #11685, #65862, #7480, #2249, #23562, #12388, #16926, #44903, #27788, #18328, #33025, #6439, #12041, #49438, #22870, #44220, #65514 ),
 ( #17642, #60283, #24603, #7837, #56767, #8178, #40673, #34758, #55734, #29868, #24941, #29172, #56417, #29527, #14800, #9195, #41022, #19702, #8864, #50829, #35781, #67578, #51176, #45591, #25286, #50480, #2582, #13437, #30202, #62005, #62344, #3272, #51507, #23910, #66897 ),
 ( #2925, #24253, #66553, #56068, #18671, #30538, #14461, #45247, #57096, #67235, #3606, #40003, #8520, #45925, #19010, #61318, #51849, #40335, #3947, #46620, #61658, #67925, #13772, #35105, #19351, #14117, #46274, #20041, #41370, #62679, #35441, #52888, #15488, #31232, #4636 ),
 ( #25975, #58472, #42741, #36815, #27009, #21747, #68262, #58133, #37153, #432, #47304, #43080, #20383, #21073, #5668, #64386, #36119, #42057, #48327, #57434, #46960, #10576, #64045, #16165, #31916, #47987, #68608, #63011, #9892, #37490, #57780, #26674, #53230, #20728, #52539 ) ),
 .UNSPECIFIED., .F., .F., .F.,
 ( 4, 4 ),
 ( 4, 1, 1, 1, 1, 1, 1, 1, 1, 1, 1, 1, 1, 1, 1, 1, 1, 1, 1, 1, 1, 1, 1, 1, 1, 1, 1, 1, 1, 1, 1, 1, 4 ),
 ( -0.02000000000000000042, 1.020000000000000018 ),
 ( 0.1633025096610999927, 0.1899619885200000136, 0.2166214673788000034, 0.2432809462376999965, 0.2699404250964999585, 0.2965999039553000038, 0.3232593828141999692, 0.3499188616730000145, 0.3765783405318000043, 0.4032378193906999697, 0.4298972982494999595, 0.4565567771083000048, 0.4832162559671999702, 0.5098757348260000155, 0.5365352136848999809, 0.5631946925437000262, 0.5898541714025000715, 0.6165136502614000369, 0.6431731291201999712, 0.6698326079790000165, 0.6964920868378999819, 0.7231515656967000272, 0.7498110445554999615, 0.7764705234143999268, 0.8031300022731999722, 0.8297894811320000175, 0.8564489599908999828, 0.8831084388497000282, 0.9097679177085999935, 0.9364273965674000388, 0.9630868754261999731, 0.9897463542851000495, 1.016405833144000015 ),
 .UNSPECIFIED. ) ;
#1195=CARTESIAN_POINT ( 'NONE',  ( 10.29399293566599916, -3.453258297007899991, -8.170700474995699736 ) ) ;
#1299=CARTESIAN_POINT ( 'NONE',  ( 9.258504216683469679, -3.836370129433861020, -6.250027056024106464 ) ) ;
#1307=CARTESIAN_POINT ( 'NONE',  ( 10.37872469555899890, -3.497841151814999883, -6.631215019384099740 ) ) ;
#1311=CARTESIAN_POINT ( 'NONE',  ( 10.59725056272499977, -2.683866746800999792, -7.519505747156228992 ) ) ;
#1340=CARTESIAN_POINT ( 'NONE',  ( 10.96118313518939935, -4.792748567750200195, -8.502430091786999711 ) ) ;
#1362=CARTESIAN_POINT ( 'NONE',  ( 11.55300581613033906, -2.892415530317000272, -8.211208432468300344 ) ) ;
#1393=CARTESIAN_POINT ( 'NONE',  ( 11.57656516821460890, -3.100463633631699967, -8.407828142327998577 ) ) ;
#1409=CARTESIAN_POINT ( 'NONE',  ( 9.226430433046999724, -4.971677342931100085, -6.900352112302299723 ) ) ;
#1423=ADVANCED_FACE ( 'NONE', ( #974 ), #63655, .F. ) ;
#1427=CARTESIAN_POINT ( 'NONE',  ( 11.46595122972049907, -3.656201404350900130, -6.704952129760900270 ) ) ;
#1444=CARTESIAN_POINT ( 'NONE',  ( 11.59999999999999964, -4.883784007588900522, -7.825000000000000178 ) ) ;
#1463=CARTESIAN_POINT ( 'NONE',  ( 10.19810941423799910, -3.053977294209000437, -6.640722727400100389 ) ) ;
#1473=CARTESIAN_POINT ( 'NONE',  ( 11.49056651104150006, -3.914543207408039738, -6.638028001068500217 ) ) ;
#1477=VECTOR ( 'NONE', #32084, 1000.000000000000000 ) ;
#1516=CARTESIAN_POINT ( 'NONE',  ( 10.74809687351632448, -3.672815144550895194, -6.282534154164607365 ) ) ;
#1521=CARTESIAN_POINT ( 'NONE',  ( 9.305380199233999505, -3.003429752324399793, -7.374740103075099640 ) ) ;
#1522=CARTESIAN_POINT ( 'NONE',  ( 9.614763540183329127, -2.782534154164604256, -7.172815144550903632 ) ) ;
#1538=CARTESIAN_POINT ( 'NONE',  ( 10.39393020684999946, -5.250000000000000000, -7.500000000000000000 ) ) ;
#1549=CARTESIAN_POINT ( 'NONE',  ( 11.26212378248529866, -4.615095948180499619, -6.336291382830999908 ) ) ;
#1577=CARTESIAN_POINT ( 'NONE',  ( 10.31759632033899976, -5.184381781355999586, -7.016653143730500197 ) ) ;
#1616=CARTESIAN_POINT ( 'NONE',  ( 11.00000000000000000, -2.920245322398999921, -7.825000000000000178 ) ) ;
#1625=( GEOMETRIC_REPRESENTATION_CONTEXT ( 3 ) GLOBAL_UNCERTAINTY_ASSIGNED_CONTEXT ( ( #23190 ) ) GLOBAL_UNIT_ASSIGNED_CONTEXT ( ( #12731, #28118, #7829 ) ) REPRESENTATION_CONTEXT ( 'NONE', 'WORKASPACE' ) );
#1626=CARTESIAN_POINT ( 'NONE',  ( 10.35376078907947495, -3.141705924399422312, -7.665591875800525479 ) ) ;
#1658=CARTESIAN_POINT ( 'NONE',  ( 11.17901463001529905, -3.302889347096799710, -6.383488688482000128 ) ) ;
#1688=CARTESIAN_POINT ( 'NONE',  ( 10.73964560330029983, -3.608363763633400279, -6.283473206644000442 ) ) ;
#1737=CARTESIAN_POINT ( 'NONE',  ( 10.30072469555899950, -3.429147315060100176, -6.512367818249299667 ) ) ;
#1752=ORIENTED_EDGE ( 'NONE', *, *, #5266, .T. ) ;
#1754=CARTESIAN_POINT ( 'NONE',  ( 9.353076168957999315, -4.579425901182000658, -8.483869947211399420 ) ) ;
#1775=CARTESIAN_POINT ( 'NONE',  ( 11.21979841651039855, -4.304975143798100312, -8.310733465454200442 ) ) ;
#1780=VECTOR ( 'NONE', #63109, 1000.000000000000000 ) ;
#1791=CARTESIAN_POINT ( 'NONE',  ( 11.25158531382729876, -3.727547057523674212, -6.249999999999998224 ) ) ;
#1821=CARTESIAN_POINT ( 'NONE',  ( 11.66287348028854964, -4.761955701524100526, -7.911973420841600380 ) ) ;
#1845=EDGE_CURVE ( 'NONE', #23021, #64952, #17865, .T. ) ;
#1873=CARTESIAN_POINT ( 'NONE',  ( 8.672151519676999598, -3.978278301382419890, -8.504175633905001419 ) ) ;
#1903=CARTESIAN_POINT ( 'NONE',  ( 11.59456039236534330, -2.685288321999000249, -7.563984187103470092 ) ) ;
#1913=SURFACE_SIDE_STYLE ('',( #29879 ) ) ;
#1960=FACE_OUTER_BOUND ( 'NONE', #9425, .T. ) ;
#1978=CARTESIAN_POINT ( 'NONE',  ( 10.59991360228957191, -4.849288934224095904, -7.293123446196289272 ) ) ;
#2006=CARTESIAN_POINT ( 'NONE',  ( 11.44366954483529852, -3.514796851401900124, -6.751356298874699569 ) ) ;
#2040=CARTESIAN_POINT ( 'NONE',  ( 10.83810672858429847, -5.021298157087000114, -6.731711997412900494 ) ) ;
#2044=CARTESIAN_POINT ( 'NONE',  ( 10.33744474310099903, -3.228742141949900279, -7.874284411628199365 ) ) ;
#2077=ORIENTED_EDGE ( 'NONE', *, *, #61893, .T. ) ;
#2078=DIRECTION ( 'NONE',  ( 1.000000000000000000, 0.000000000000000000, 0.000000000000000000 ) ) ;
#2094=CARTESIAN_POINT ( 'NONE',  ( 10.32533997688000049, -3.756890902898200046, -6.385465081946999355 ) ) ;
#2109=VERTEX_POINT ( 'NONE', #10683 ) ;
#2111=CARTESIAN_POINT ( 'NONE',  ( 9.097772138681998300, -4.373757805842100055, -6.567719246739500250 ) ) ;
#2126=CARTESIAN_POINT ( 'NONE',  ( 11.53979707368350027, -4.430269712815499972, -6.748224392138099326 ) ) ;
#2139=EDGE_CURVE ( 'NONE', #67987, #8310, #21178, .T. ) ;
#2147=B_SPLINE_CURVE_WITH_KNOTS ( 'NONE', 3,
 ( #68432, #35946, #15315, #41878, #21242, #36639, #57260, #42570, #63185, #9360 ),
 .UNSPECIFIED., .F., .F.,
 ( 4, 2, 2, 2, 4 ),
 ( 0.000000000000000000, 0.2500000000000004441, 0.5000000000000008882, 0.7500000000000004441, 1.000000000000000000 ),
 .UNSPECIFIED. ) ;
#2162=CARTESIAN_POINT ( 'NONE',  ( 11.23195122972050086, -3.492749840905900349, -6.326963915009999440 ) ) ;
#2222=CARTESIAN_POINT ( 'NONE',  ( 8.746126402770999064, -2.931626221533000010, -7.097120470443400109 ) ) ;
#2249=CARTESIAN_POINT ( 'NONE',  ( 11.01279632507519857, -3.375091146194399983, -8.658468685623999406 ) ) ;
#2251=PLANE ( 'NONE',  #36256 ) ;
#2340=CARTESIAN_POINT ( 'NONE',  ( 8.896714042595458949, -4.136150106425177775, -6.453285899984953389 ) ) ;
#2347=CARTESIAN_POINT ( 'NONE',  ( 10.68546886766499959, -4.566506264294200257, -6.470713638631999665 ) ) ;
#2378=CARTESIAN_POINT ( 'NONE',  ( 10.20226357027499908, -2.879914860223000250, -7.716099591766099053 ) ) ;
#2395=CARTESIAN_POINT ( 'NONE',  ( 11.64122412107036908, -3.937930136014310190, -6.326756392227999015 ) ) ;
#2440=ADVANCED_FACE ( 'NONE', ( #49466 ), #64224, .F. ) ;
#2445=CARTESIAN_POINT ( 'NONE',  ( 9.956950584426998319, -3.655872208659600275, -6.704208565179699875 ) ) ;
#2448=B_SPLINE_CURVE_WITH_KNOTS ( 'NONE', 3,
 ( #68583, #16486, #37467, #47282 ),
 .UNSPECIFIED., .F., .F.,
 ( 4, 4 ),
 ( 0.000000000000000000, 0.1494581667962512628 ),
 .UNSPECIFIED. ) ;
#2462=CARTESIAN_POINT ( 'NONE',  ( 11.41672066707849886, -3.258843737379200078, -7.051685395375099752 ) ) ;
#2477=LINE ( 'NONE', #56654, #64243 ) ;
#2496=CARTESIAN_POINT ( 'NONE',  ( 11.13349010443639919, -2.725546193138000284, -7.595309363461700158 ) ) ;
#2552=CARTESIAN_POINT ( 'NONE',  ( 10.11188779216199940, -2.816792857868000155, -7.926693309523199282 ) ) ;
#2559=DIRECTION ( 'NONE',  ( 0.000000000000000000, -1.000000000000000000, 0.000000000000000000 ) ) ;
#2582=CARTESIAN_POINT ( 'NONE',  ( 10.72702344389999851, -5.004394439171999664, -6.890449684422599752 ) ) ;
#2609=CARTESIAN_POINT ( 'NONE',  ( 10.49490035061499782, -3.659038130401700339, -8.732935057095000175 ) ) ;
#2691=CARTESIAN_POINT ( 'NONE',  ( 11.39700581613019992, -3.130347327833300053, -8.058426314824099990 ) ) ;
#2710=ADVANCED_FACE ( 'NONE', ( #39773 ), #24848, .T. ) ;
#2721=CARTESIAN_POINT ( 'NONE',  ( 10.24733997687999931, -3.727636250918499705, -6.251346978035999591 ) ) ;
#2739=CARTESIAN_POINT ( 'NONE',  ( 10.63880513895979973, -2.849548954067000039, -6.860457220153399760 ) ) ;
#2772=CARTESIAN_POINT ( 'NONE',  ( 11.53979707368350027, -4.430269712815499972, -6.748224392138099326 ) ) ;
#2773=CARTESIAN_POINT ( 'NONE',  ( 10.24733997687999931, -3.727636250918499705, -6.251346978035999591 ) ) ;
#2774=DIRECTION ( 'NONE',  ( -1.000000000000000000, 0.000000000000000000, 0.000000000000000000 ) ) ;
#2787=CARTESIAN_POINT ( 'NONE',  ( 10.33688779216199904, -3.198058499272899979, -7.789199634454999632 ) ) ;
#2804=CARTESIAN_POINT ( 'NONE',  ( 11.14179841651039915, -4.353306409735099969, -8.439215328713499886 ) ) ;
#2834=CARTESIAN_POINT ( 'NONE',  ( 8.737760194560388882, -4.066145789045418013, -8.370465981241705933 ) ) ;
#2851=CARTESIAN_POINT ( 'NONE',  ( 10.28441772631199846, -3.627481539113199815, -8.266796319406900295 ) ) ;
#2896=ORIENTED_EDGE ( 'NONE', *, *, #27471, .T. ) ;
#2897=CARTESIAN_POINT ( 'NONE',  ( 9.506000818238998562, -5.010295986746999830, -8.032011717116800398 ) ) ;
#2906=VERTEX_POINT ( 'NONE', #36582 ) ;
#2910=EDGE_CURVE ( 'NONE', #10029, #50859, #62792, .T. ) ;
#2925=CARTESIAN_POINT ( 'NONE',  ( 11.68788784977535933, -4.985985832792199979, -7.443657794094239222 ) ) ;
#2935=( NAMED_UNIT ( * ) PLANE_ANGLE_UNIT ( ) SI_UNIT ( $, .RADIAN. ) );
#2949=CARTESIAN_POINT ( 'NONE',  ( 10.49288779216199785, -2.943881405003000218, -7.880862084500499520 ) ) ;
#3030=CARTESIAN_POINT ( 'NONE',  ( 10.69057802013490033, -5.033226574983999946, -7.475947032624040034 ) ) ;
#3031=ORIENTED_EDGE ( 'NONE', *, *, #23349, .F. ) ;
#3079=CARTESIAN_POINT ( 'NONE',  ( 11.72433327354039889, -4.983220429128399687, -6.856888818507299810 ) ) ;
#3093=VECTOR ( 'NONE', #51941, 1000.000000000000227 ) ;
#3113=CARTESIAN_POINT ( 'NONE',  ( 11.63825819896753977, -4.851203879749700576, -7.660469764776300039 ) ) ;
#3114=CARTESIAN_POINT ( 'NONE',  ( 11.10887482311539998, -2.815046254222000055, -7.978749413531599721 ) ) ;
#3130=CARTESIAN_POINT ( 'NONE',  ( 8.920468108405998464, -3.033597967472499768, -7.773695785133000413 ) ) ;
#3149=CARTESIAN_POINT ( 'NONE',  ( 11.01872200990539952, -4.947480442174099657, -7.169497859994799605 ) ) ;
#3196=CARTESIAN_POINT ( 'NONE',  ( 10.24006601915162484, -4.042412777185713679, -8.373918476712228554 ) ) ;
#3200=CARTESIAN_POINT ( 'NONE',  ( 10.80133863405319872, -3.465595476214000215, -8.181696703306599261 ) ) ;
#3217=CARTESIAN_POINT ( 'NONE',  ( 11.28192504596561996, -3.091022006579346115, -7.825000185715046186 ) ) ;
#3219=CARTESIAN_POINT ( 'NONE',  ( 10.61476354018240187, -2.782534154164604256, -7.172815144550903632 ) ) ;
#3246=CARTESIAN_POINT ( 'NONE',  ( 9.126063610504999701, -3.531653260805799999, -8.541338455964998744 ) ) ;
#3272=CARTESIAN_POINT ( 'NONE',  ( 10.51925056272499859, -2.825232917634000085, -7.517410630436119234 ) ) ;
#3282=( NAMED_UNIT ( * ) PLANE_ANGLE_UNIT ( ) SI_UNIT ( $, .RADIAN. ) );
#3292=CARTESIAN_POINT ( 'NONE',  ( 9.099999931440999390, -4.000000000000000000, -7.500000000000000000 ) ) ;
#3294=CARTESIAN_POINT ( 'NONE',  ( 9.405747021775999528, -4.961496216383199709, -8.343747244947598674 ) ) ;
#3298=ORIENTED_EDGE ( 'NONE', *, *, #16906, .F. ) ;
#3368=CARTESIAN_POINT ( 'NONE',  ( 10.60235971519489873, -3.394698737128500010, -6.493038401303000029 ) ) ;
#3404=CARTESIAN_POINT ( 'NONE',  ( 8.775480666858998191, -3.710922827228400056, -8.317400147935998689 ) ) ;
#3418=CARTESIAN_POINT ( 'NONE',  ( 10.51925056272499859, -2.825232917634000085, -7.517410630436119234 ) ) ;
#3420=VERTEX_POINT ( 'NONE', #58850 ) ;
#3423=ORIENTED_EDGE ( 'NONE', *, *, #38032, .T. ) ;
#3446=CARTESIAN_POINT ( 'NONE',  ( 10.34580110216399973, -5.090698144635000588, -6.833896451085399448 ) ) ;
#3483=CARTESIAN_POINT ( 'NONE',  ( 9.593930206849998754, -2.750000000000000000, -7.500000000000000000 ) ) ;
#3485=CARTESIAN_POINT ( 'NONE',  ( 10.99410672858429905, -4.801902424331299990, -6.896755974168000236 ) ) ;
#3516=ORIENTED_EDGE ( 'NONE', *, *, #30043, .T. ) ;
#3529=CARTESIAN_POINT ( 'NONE',  ( 9.530849898046625412, -4.391573077584247642, -6.717566108970133953 ) ) ;
#3533=CARTESIAN_POINT ( 'NONE',  ( 10.92441504065829960, -3.305585767322499979, -6.982228367137699898 ) ) ;
#3538=CARTESIAN_POINT ( 'NONE',  ( 11.27769289846838241, -5.045673698156681652, -7.824982657629016458 ) ) ;
#3578=CARTESIAN_POINT ( 'NONE',  ( 9.202051052051999136, -2.879444846832000415, -7.719295683256799379 ) ) ;
#3606=CARTESIAN_POINT ( 'NONE',  ( 11.31389666366019853, -4.045876550911099656, -8.532487796751999198 ) ) ;
#3607=CARTESIAN_POINT ( 'NONE',  ( 11.59999999999999787, -3.165084187357963597, -6.701316188976606192 ) ) ;
#3609=CARTESIAN_POINT ( 'NONE',  ( 8.905196823546312146, -3.391797362091467427, -8.372486832488423403 ) ) ;
#3652=DIRECTION ( 'NONE',  ( -1.000000000000000000, 0.000000000000000000, 1.554312234491000161E-14 ) ) ;
#3709=CARTESIAN_POINT ( 'NONE',  ( 11.33810207955129812, -3.203462856645999945, -7.825000000000000178 ) ) ;
#3738=CARTESIAN_POINT ( 'NONE',  ( 10.19810941423799910, -3.053977294209000437, -6.640722727400100389 ) ) ;
#3739=ORIENTED_EDGE ( 'NONE', *, *, #36867, .F. ) ;
#3785=CARTESIAN_POINT ( 'NONE',  ( 11.58902763632552002, -4.786505910413500153, -7.137085349939700230 ) ) ;
#3786=CARTESIAN_POINT ( 'NONE',  ( 11.20733594839949809, -3.159733897807000425, -6.537051788466999191 ) ) ;
#3803=CARTESIAN_POINT ( 'NONE',  ( 8.943784697134999462, -3.529509552262100058, -6.771750947090999340 ) ) ;
#3821=CARTESIAN_POINT ( 'NONE',  ( 10.96949144726329806, -4.580206776679999869, -6.681274802424499448 ) ) ;
#3869=CARTESIAN_POINT ( 'NONE',  ( 10.13874943042162613, -4.847937002157847175, -7.715719979441764131 ) ) ;
#3873=CARTESIAN_POINT ( 'NONE',  ( 10.53057053952199951, -4.340412141385700195, -6.703496287302799672 ) ) ;
#3891=CARTESIAN_POINT ( 'NONE',  ( 10.83351354018309998, -5.249999999999999112, -7.336375382625531572 ) ) ;
#3919=CARTESIAN_POINT ( 'NONE',  ( 9.909254614703000286, -5.239722547583999912, -7.815392442832299835 ) ) ;
#3947=CARTESIAN_POINT ( 'NONE',  ( 10.98146005378009882, -3.088328798999600000, -7.013182449205100255 ) ) ;
#3973=ORIENTED_EDGE ( 'NONE', *, *, #10138, .T. ) ;
#4047=CARTESIAN_POINT ( 'NONE',  ( 10.90346005378009941, -3.213042707518099839, -7.079777642108599167 ) ) ;
#4051=CARTESIAN_POINT ( 'NONE',  ( 11.16544712921906957, -4.732401051283384952, -7.982093405445620959 ) ) ;
#4128=CARTESIAN_POINT ( 'NONE',  ( 10.38287885159599888, -3.139900861731399928, -7.397393329751199786 ) ) ;
#4148=CARTESIAN_POINT ( 'NONE',  ( 9.425038493598998812, -3.372531419565699906, -6.901676404381399621 ) ) ;
#4168=CARTESIAN_POINT ( 'NONE',  ( 10.74795391537419853, -3.169881940022800215, -8.063786182297898009 ) ) ;
#4214=CARTESIAN_POINT ( 'NONE',  ( 10.16407857760462718, -4.737836169116369511, -7.970244675898661590 ) ) ;
#4220=CARTESIAN_POINT ( 'NONE',  ( 11.75718044953559804, -3.110233631466100324, -7.963966784336999005 ) ) ;
#4226=CARTESIAN_POINT ( 'NONE',  ( 10.25851354018279160, -3.836375382625526687, -6.250000000000000888 ) ) ;
#4254=ORIENTED_EDGE ( 'NONE', *, *, #58869, .F. ) ;
#4269=CARTESIAN_POINT ( 'NONE',  ( 9.073392757686999488, -3.136549968260000210, -8.443842375698499936 ) ) ;
#4280=B_SPLINE_CURVE_WITH_KNOTS ( 'NONE', 3,
 ( #51771, #57698, #9808, #25203, #3196, #14721, #68527, #4214, #3869, #56340, #46538, #67503, #67844, #62597, #52459, #62263, #19620, #25895, #19966, #9121, #40942, #24523, #61580, #14384, #51432, #36036, #20303, #31157, #52111, #57352, #41629, #62935, #3529, #47224, #20649, #45848, #8785, #30129, #13696, #9456, #68185, #30459, #30798, #15059, #14038, #51093, #25552, #19269, #46877, #24864, #36382, #40598, #4554, #61923, #56686, #35704, #57021, #26244, #58055, #5253, #37077, #21666, #26591, #10158, #58388 ),
 .UNSPECIFIED., .F., .F.,
 ( 4, 1, 1, 1, 1, 1, 1, 1, 1, 1, 1, 1, 1, 1, 1, 1, 1, 1, 1, 1, 1, 1, 1, 1, 1, 1, 1, 1, 1, 1, 1, 1, 1, 1, 1, 1, 1, 1, 1, 1, 1, 1, 1, 1, 1, 1, 1, 1, 1, 1, 1, 1, 1, 1, 1, 1, 1, 1, 1, 1, 1, 1, 4 ),
 ( 0.000000000000000000, 0.01249986222369742044, 0.02874986775682986107, 0.04499987328996229996, 0.06124987882309473886, 0.07749988435622719163, 0.09374988988935963052, 0.1099998954224920694, 0.1262499009556244944, 0.1424999064887569333, 0.1587499120218893722, 0.1749999175550218111, 0.1912499230881542500, 0.2074999286212866889, 0.2237499341544191278, 0.2399999396875515667, 0.2562499452206840056, 0.2724999507538165000, 0.2887499562869489389, 0.3049999618200813778, 0.3212499673532137612, 0.3374999728863462556, 0.3537499784194786945, 0.3699999839526111334, 0.3862499894857435723, 0.4024999950188760112, 0.4187500005520084501, 0.4350000060851408890, 0.4512500116182733279, 0.4675000171514058223, 0.4837500226845382056, 0.5000000282176706445, 0.5162500337508030279, 0.5325000392839354113, 0.5487500448170679057, 0.5650000503502002891, 0.5812500558833328945, 0.5975000614164652779, 0.6137500669495976613, 0.6300000724827301557, 0.6462500780158625391, 0.6625000835489949225, 0.6787500890821274169, 0.6950000946152598003, 0.7112501001483924057, 0.7275001056815247891, 0.7437501112146571725, 0.7600001167477896669, 0.7762501222809220502, 0.7925001278140545447, 0.8087501333471869280, 0.8250001388803193114, 0.8412501444134519168, 0.8575001499465843002, 0.8737501554797167946, 0.8900001610128491780, 0.9062501665459815614, 0.9225001720791140558, 0.9387501776122464392, 0.9550001831453789336, 0.9712501886785113170, 0.9875001942116438114, 1.000000000000000000 ),
 .UNSPECIFIED. ) ;
#4296=DIRECTION ( 'NONE',  ( 0.000000000000000000, 0.000000000000000000, -1.000000000000000000 ) ) ;
#4390=LINE ( 'NONE', #25724, #1780 ) ;
#4405=ORIENTED_EDGE ( 'NONE', *, *, #23795, .T. ) ;
#4469=EDGE_CURVE ( 'NONE', #24854, #47095, #59314, .T. ) ;
#4470=CARTESIAN_POINT ( 'NONE',  ( 11.14179841651039915, -4.353306409735099969, -8.439215328713499886 ) ) ;
#4477=CARTESIAN_POINT ( 'NONE',  ( 11.58810207955109917, -4.796537143354000499, -7.174999999999999822 ) ) ;
#4489=CARTESIAN_POINT ( 'NONE',  ( 9.627671671056999614, -4.855035690642299784, -7.643603315539799326 ) ) ;
#4507=CARTESIAN_POINT ( 'NONE',  ( 10.74379975933729980, -2.921317947059999920, -7.128873141726999485 ) ) ;
#4513=UNCERTAINTY_MEASURE_WITH_UNIT (LENGTH_MEASURE( 1.000000000000000082E-05 ), #12748, 'distance_accuracy_value', 'NONE');
#4547=CARTESIAN_POINT ( 'NONE',  ( 9.110163692916374956, -2.765799910565780895, -7.245561603203542589 ) ) ;
#4554=CARTESIAN_POINT ( 'NONE',  ( 9.024266954400625096, -4.325581995510845879, -6.687886317613946474 ) ) ;
#4561=CARTESIAN_POINT ( 'NONE',  ( 11.50687348028854906, -5.003459210197000573, -8.042549288197099244 ) ) ;
#4576=CARTESIAN_POINT ( 'NONE',  ( 10.23959632033899858, -5.057167065956000407, -7.068569539041399175 ) ) ;
#4611=CARTESIAN_POINT ( 'NONE',  ( 9.326684229509998758, -4.901739481456999670, -6.592668585875199661 ) ) ;
#4636=CARTESIAN_POINT ( 'NONE',  ( 10.35814141025499957, -3.516507310755200066, -8.361148840840000318 ) ) ;
#4684=CARTESIAN_POINT ( 'NONE',  ( 9.054101285863998427, -4.558267473659599389, -6.836640842107200022 ) ) ;
#4698=CARTESIAN_POINT ( 'NONE',  ( 11.47500581613029880, -3.011381429075500105, -8.134817373646898275 ) ) ;
#4734=CARTESIAN_POINT ( 'NONE',  ( 10.36325056272499978, -3.107965259299500183, -7.513220396995270001 ) ) ;
#4782=ORIENTED_EDGE ( 'NONE', *, *, #4863, .T. ) ;
#4786=CARTESIAN_POINT ( 'NONE',  ( 11.04298866606778162, -4.505418116367177817, -6.786808489985508785 ) ) ;
#4818=CARTESIAN_POINT ( 'NONE',  ( 11.06795257254739973, -4.963546614172099858, -7.780229861306499295 ) ) ;
#4836=CARTESIAN_POINT ( 'NONE',  ( 9.121088727410999297, -4.863977618062000019, -7.572461161969050281 ) ) ;
#4854=CARTESIAN_POINT ( 'NONE',  ( 10.64533863405319991, -3.296214805808900028, -8.397761948794601139 ) ) ;
#4863=EDGE_CURVE ( 'NONE', #10153, #32857, #22845, .T. ) ;
#4907=CARTESIAN_POINT ( 'NONE',  ( 11.41256651104150066, -3.901000349726440053, -6.501426055769400136 ) ) ;
#4924=ORIENTED_EDGE ( 'NONE', *, *, #44537, .F. ) ;
#4926=CARTESIAN_POINT ( 'NONE',  ( 9.735025935145998233, -4.185743043590700374, -6.234344474498000110 ) ) ;
#4939=B_SPLINE_CURVE_WITH_KNOTS ( 'NONE', 3,
 ( #1444, #48649, #58788, #26983 ),
 .UNSPECIFIED., .F., .F.,
 ( 4, 4 ),
 ( 0.000000000000000000, 1.000000000000000000 ),
 .UNSPECIFIED. ) ;
#4942=CARTESIAN_POINT ( 'NONE',  ( 9.099999931440999390, -2.935682118448999844, -8.155535999783198875 ) ) ;
#4962=CARTESIAN_POINT ( 'NONE',  ( 8.668126402770999661, -2.803062940908000122, -7.048639765412399782 ) ) ;
#4964=DIRECTION ( 'NONE',  ( -1.000000000000000000, 0.000000000000000000, -2.609704304917999919E-14 ) ) ;
#4982=CARTESIAN_POINT ( 'NONE',  ( 10.59610807141099897, -3.947296672195129918, -8.639522915742999132 ) ) ;
#4987=DIRECTION ( 'NONE',  ( 0.000000000000000000, 1.000000000000000000, 0.000000000000000000 ) ) ;
#4994=VECTOR ( 'NONE', #35659, 1000.000000000000000 ) ;
#5017=DIRECTION ( 'NONE',  ( -1.000000000000000000, 0.000000000000000000, 0.000000000000000000 ) ) ;
#5037=CARTESIAN_POINT ( 'NONE',  ( 9.510025935145998588, -4.125890936441000356, -6.642177514500700042 ) ) ;
#5052=CARTESIAN_POINT ( 'NONE',  ( 10.44635971519499940, -3.540377183549800133, -6.735384833238199143 ) ) ;
#5089=CARTESIAN_POINT ( 'NONE',  ( 10.48791429142999831, -3.983006558652820051, -6.608036045330599961 ) ) ;
#5092=CARTESIAN_POINT ( 'NONE',  ( 8.731616107288068918, -3.999997736744774546, -8.381579007094499545 ) ) ;
#5143=ADVANCED_FACE ( 'NONE', ( #61295 ), #9176, .T. ) ;
#5150=CARTESIAN_POINT ( 'NONE',  ( 9.893930206848997599, -5.250000000000000000, -7.500000000000000000 ) ) ;
#5170=CARTESIAN_POINT ( 'NONE',  ( 11.63410404293056999, -4.442327784369100030, -8.400720262063998689 ) ) ;
#5205=CARTESIAN_POINT ( 'NONE',  ( 11.67918044953561996, -2.988516238873000219, -8.027436060358800418 ) ) ;
#5207=CONICAL_SURFACE ( 'NONE', #27525, 0.9999998338055000602, 0.7853981908209605178 ) ;
#5253=CARTESIAN_POINT ( 'NONE',  ( 8.846962924124625260, -3.158163127838481188, -7.738417548727159812 ) ) ;
#5257=CARTESIAN_POINT ( 'NONE',  ( 11.43718179236249988, -4.209680326224799707, -6.518682001772900136 ) ) ;
#5262=CARTESIAN_POINT ( 'NONE',  ( 10.24809687351608289, -3.672815144550895194, -6.282534154164607365 ) ) ;
#5266=EDGE_CURVE ( 'NONE', #47524, #41410, #51516, .T. ) ;
#5269=CARTESIAN_POINT ( 'NONE',  ( 9.948096873516250938, -4.327184855449103473, -8.717465845835395299 ) ) ;
#5272=CARTESIAN_POINT ( 'NONE',  ( 9.177784697135001224, -3.305825103746500293, -6.425520776924999566 ) ) ;
#5303=CARTESIAN_POINT ( 'NONE',  ( 9.149380199233998923, -2.730774061183999901, -7.340469740450900282 ) ) ;
#5324=CARTESIAN_POINT ( 'NONE',  ( 10.13662282008599824, -3.405288783432600219, -8.459250300176799797 ) ) ;
#5376=CARTESIAN_POINT ( 'NONE',  ( 11.71210404293059959, -4.381818659177399766, -8.277504409418298792 ) ) ;
#5385=CARTESIAN_POINT ( 'NONE',  ( 9.079430433046999482, -4.737822807309499673, -7.044669955395099770 ) ) ;
#5401=CARTESIAN_POINT ( 'NONE',  ( 11.48522412107029922, -3.952868550833580130, -6.609122077774299164 ) ) ;
#5461=CARTESIAN_POINT ( 'NONE',  ( 11.39975833414730033, -3.203462856645999945, -7.174999999999999822 ) ) ;
#5514=CARTESIAN_POINT ( 'NONE',  ( 10.70287750876920008, -4.469200303112399908, -8.228113772635300194 ) ) ;
#5530=CARTESIAN_POINT ( 'NONE',  ( 11.47822875044625945, -3.830319670899316353, -6.639682804525812720 ) ) ;
#5547=CARTESIAN_POINT ( 'NONE',  ( 11.65456516821461008, -3.197083038490000195, -8.310318115935698913 ) ) ;
#5553=CARTESIAN_POINT ( 'NONE',  ( 11.04664311227086593, -3.555960431980462300, -8.706333095531745059 ) ) ;
#5591=CARTESIAN_POINT ( 'NONE',  ( 10.57564694612699974, -4.931992688388300294, -7.871941502982999772 ) ) ;
#5606=CARTESIAN_POINT ( 'NONE',  ( 10.13626717315599990, -4.764472860199700399, -6.848522029265999400 ) ) ;
#5637=CARTESIAN_POINT ( 'NONE',  ( 9.048601287889788125, -3.999999532294070459, -8.698595322193611423 ) ) ;
#5640=CARTESIAN_POINT ( 'NONE',  ( 11.23424042080529794, -3.455907502640803042, -6.342116603374310380 ) ) ;
#5662=CARTESIAN_POINT ( 'NONE',  ( 11.52733460557258915, -3.793662715184400014, -8.761245990815998752 ) ) ;
#5668=CARTESIAN_POINT ( 'NONE',  ( 11.06967835872019812, -4.754733798270200928, -7.024326263066900111 ) ) ;
#5721=CARTESIAN_POINT ( 'NONE',  ( 9.862621437244998290, -3.332852462363599777, -6.749162825004299648 ) ) ;
#5736=CARTESIAN_POINT ( 'NONE',  ( 10.57102344389999971, -4.762665848028800220, -7.037150754511299233 ) ) ;
#5741=ORIENTED_EDGE ( 'NONE', *, *, #13743, .F. ) ;
#5753=CARTESIAN_POINT ( 'NONE',  ( 10.10434687351566474, -2.749999999999998224, -7.336375382625535124 ) ) ;
#5835=ORIENTED_EDGE ( 'NONE', *, *, #10138, .F. ) ;
#5853=CARTESIAN_POINT ( 'NONE',  ( 11.60533460557258323, -3.815825449682300086, -8.625775273268001087 ) ) ;
#5857=CARTESIAN_POINT ( 'NONE',  ( 11.55811496860034815, -2.954409148022000053, -6.964183526617899744 ) ) ;
#5886=CARTESIAN_POINT ( 'NONE',  ( 10.37457053952199892, -4.448306506338299826, -6.451042711717000167 ) ) ;
#5922=CARTESIAN_POINT ( 'NONE',  ( 9.143927823787141307, -2.750011555256801188, -7.499999844943244121 ) ) ;
#5936=CARTESIAN_POINT ( 'NONE',  ( 11.36333594839950045, -3.340240242524600056, -6.743912759487099784 ) ) ;
#5954=CARTESIAN_POINT ( 'NONE',  ( 9.125113844317997547, -3.711648483798899889, -6.395197822644999697 ) ) ;
#5988=LINE ( 'NONE', #753, #45560 ) ;
#6005=CARTESIAN_POINT ( 'NONE',  ( 10.49764694612699856, -5.059486515935999407, -7.922821994243300914 ) ) ;
#6018=VERTEX_POINT ( 'NONE', #17101 ) ;
#6027=CARTESIAN_POINT ( 'NONE',  ( 9.602263540182329749, -2.907767014557176566, -8.129523725463620565 ) ) ;
#6066=EDGE_CURVE ( 'NONE', #14453, #17504, #41857, .T. ) ;
#6067=CARTESIAN_POINT ( 'NONE',  ( 10.13922949779699856, -3.366547096154099972, -8.449985803660998940 ) ) ;
#6080=SHAPE_DEFINITION_REPRESENTATION ( #40536, #53976 ) ;
#6081=CARTESIAN_POINT ( 'NONE',  ( 11.40211496860029783, -3.206052520092899982, -7.093139000852099585 ) ) ;
#6088=CARTESIAN_POINT ( 'NONE',  ( 8.727215710425999973, -4.373963964882100264, -8.308760775591800041 ) ) ;
#6128=ORIENTED_EDGE ( 'NONE', *, *, #12355, .T. ) ;
#6179=ORIENTED_EDGE ( 'NONE', *, *, #60720, .T. ) ;
#6183=CARTESIAN_POINT ( 'NONE',  ( 9.227255459545913752, -3.370461114521380530, -6.407745725917161295 ) ) ;
#6193=CARTESIAN_POINT ( 'NONE',  ( 10.50180110216399854, -4.856393875115199599, -6.976989117212499814 ) ) ;
#6197=CARTESIAN_POINT ( 'NONE',  ( 11.10101463001529964, -3.377766160221900016, -6.503413421344399481 ) ) ;
#6229=CARTESIAN_POINT ( 'NONE',  ( 11.61759063708296047, -2.782734359457999851, -7.842242470354300110 ) ) ;
#6253=B_SPLINE_CURVE_WITH_KNOTS ( 'NONE', 3,
 ( #37212, #48388, #32660, #58529 ),
 .UNSPECIFIED., .F., .F.,
 ( 4, 4 ),
 ( 0.000000000000000000, 1.000000000000000000 ),
 .UNSPECIFIED. ) ;
#6278=CARTESIAN_POINT ( 'NONE',  ( 10.71918447801630059, -2.859536135895000442, -7.474854604063350116 ) ) ;
#6292=CARTESIAN_POINT ( 'NONE',  ( 9.854346873516623972, -5.250000000000000000, -7.663624617374463099 ) ) ;
#6296=CARTESIAN_POINT ( 'NONE',  ( 9.806988259785999418, -4.131418345883800747, -8.495776841814999258 ) ) ;
#6314=VERTEX_POINT ( 'NONE', #25452 ) ;
#6348=CARTESIAN_POINT ( 'NONE',  ( 10.94072200990529886, -5.077092948368999714, -7.124286150322599376 ) ) ;
#6357=CARTESIAN_POINT ( 'NONE',  ( 11.59999999999999964, -4.672781865721786332, -6.851153339015914057 ) ) ;
#6360=CARTESIAN_POINT ( 'NONE',  ( 11.78594988689359901, -3.606563555963900214, -8.271690446953899212 ) ) ;
#6375=EDGE_CURVE ( 'NONE', #7391, #62696, #33070, .T. ) ;
#6410=CARTESIAN_POINT ( 'NONE',  ( 9.938608878791999501, -4.227457260387500249, -6.521682313853199631 ) ) ;
#6422=CARTESIAN_POINT ( 'NONE',  ( 10.32169598648999909, -3.233475335853099875, -7.956401575444799867 ) ) ;
#6439=CARTESIAN_POINT ( 'NONE',  ( 10.68035971519489813, -3.321859513918399731, -6.371865185335000348 ) ) ;
#6442=CARTESIAN_POINT ( 'NONE',  ( 10.16684687351567185, -3.231816600031351516, -6.500416447002278275 ) ) ;
#6484=FACE_OUTER_BOUND ( 'NONE', #53085, .T. ) ;
#6491=CARTESIAN_POINT ( 'NONE',  ( 8.969356963619999235, -5.119357025014000584, -7.499999999914821025 ) ) ;
#6507=CARTESIAN_POINT ( 'NONE',  ( 11.05391045180431675, -2.870950512581995628, -8.114538794791121390 ) ) ;
#6546=CARTESIAN_POINT ( 'NONE',  ( 10.92026088462129962, -3.997864853650589634, -6.496532863517000322 ) ) ;
#6550=CARTESIAN_POINT ( 'NONE',  ( 10.97635090131019986, -3.000792947412299849, -8.118017011233499503 ) ) ;
#6581=CARTESIAN_POINT ( 'NONE',  ( 11.42887348028849992, -5.124210964533999935, -8.107837221875000111 ) ) ;
#6634=CARTESIAN_POINT ( 'NONE',  ( 11.60118044953561878, -2.866798846279000390, -8.090905336380599167 ) ) ;
#6647=CARTESIAN_POINT ( 'NONE',  ( 8.922480666858998433, -3.619299191678599925, -8.576476893896000320 ) ) ;
#6665=CARTESIAN_POINT ( 'NONE',  ( 11.12133729122639991, -4.865898216891100247, -7.477221318588949117 ) ) ;
#6684=CARTESIAN_POINT ( 'NONE',  ( 9.099999931440999390, -2.753634353389999845, -7.404749409716440134 ) ) ;
#6699=CARTESIAN_POINT ( 'NONE',  ( 10.24733997687999931, -3.727636250918499705, -6.251346978035999591 ) ) ;
#6705=B_SPLINE_CURVE_WITH_KNOTS ( 'NONE', 3,
 ( #43927, #16308, #28189, #10715, #64534, #48821, #32062, #16651, #6507, #63851 ),
 .UNSPECIFIED., .F., .F.,
 ( 4, 2, 2, 2, 4 ),
 ( 0.000000000000000000, 0.2500000000000000000, 0.5000000000000000000, 0.7500000000000000000, 1.000000000000000000 ),
 .UNSPECIFIED. ) ;
#6710=CARTESIAN_POINT ( 'NONE',  ( 11.81056516821459823, -3.390321848206700128, -8.115298063151199059 ) ) ;
#6757=B_SPLINE_CURVE_WITH_KNOTS ( 'NONE', 3,
 ( #34314, #7384, #55637, #29077, #24157, #50388 ),
 .UNSPECIFIED., .F., .F.,
 ( 4, 1, 1, 4 ),
 ( 0.000000000000000000, 0.3333333333333000081, 0.6666666666667000474, 1.000000000000000000 ),
 .UNSPECIFIED. ) ;
#6758=CARTESIAN_POINT ( 'NONE',  ( 10.06525461470299909, -4.973404788313100511, -7.747639695388999215 ) ) ;
#6780=PRESENTATION_STYLE_ASSIGNMENT (( #33367 ) ) ;
#6878=DIRECTION ( 'NONE',  ( -1.000000000000000000, 0.000000000000000000, 0.000000000000000000 ) ) ;
#6881=CARTESIAN_POINT ( 'NONE',  ( 9.310585478579783469, -4.629544268302964838, -6.407725666907082562 ) ) ;
#6890=CARTESIAN_POINT ( 'NONE',  ( 11.45764291764649911, -5.132124077409000229, -7.360052904210999891 ) ) ;
#6926=CARTESIAN_POINT ( 'NONE',  ( 10.88733729122639993, -5.277570687708000641, -7.466391690027689876 ) ) ;
#6939=ORIENTED_EDGE ( 'NONE', *, *, #5266, .F. ) ;
#6982=CARTESIAN_POINT ( 'NONE',  ( 11.28533594839949750, -3.249987070165300196, -6.640482273977399430 ) ) ;
#6996=CARTESIAN_POINT ( 'NONE',  ( 10.38955864497999926, -3.209241371122599773, -8.119307134446700047 ) ) ;
#7015=CARTESIAN_POINT ( 'NONE',  ( 10.72749279009019929, -4.225282629687599822, -8.336388861178200216 ) ) ;
#7073=ORIENTED_EDGE ( 'NONE', *, *, #13683, .T. ) ;
#7091=ADVANCED_FACE ( 'NONE', ( #24782 ), #36869, .F. ) ;
#7104=CARTESIAN_POINT ( 'NONE',  ( 10.77934687351631382, -4.163624617374463988, -6.249999999999999112 ) ) ;
#7112=CARTESIAN_POINT ( 'NONE',  ( 8.976101285863999024, -4.646739515667500875, -6.731514281717299930 ) ) ;
#7128=CARTESIAN_POINT ( 'NONE',  ( 10.62309687351639020, -2.782534154164605145, -7.827184855449101697 ) ) ;
#7135=CARTESIAN_POINT ( 'NONE',  ( 11.37299956498129916, -5.207010770456999893, -7.174999999999999822 ) ) ;
#7161=DIRECTION ( 'NONE',  ( 0.000000000000000000, -1.000000000000000000, 0.000000000000000000 ) ) ;
#7166=CARTESIAN_POINT ( 'NONE',  ( 10.57088779216199903, -2.816792857868000155, -7.926693309523199282 ) ) ;
#7180=CARTESIAN_POINT ( 'NONE',  ( 11.00009108335970609, -2.881106418324590468, -7.597657431955929574 ) ) ;
#7216=CARTESIAN_POINT ( 'NONE',  ( 10.52606775832647656, -4.343526402396090447, -6.696209471835564919 ) ) ;
#7245=CARTESIAN_POINT ( 'NONE',  ( 11.67766954483535891, -3.284117569315500251, -6.395429936871999566 ) ) ;
#7257=EDGE_CURVE ( 'NONE', #51205, #54348, #51762, .T. ) ;
#7261=DIRECTION ( 'NONE',  ( 0.000000000000000000, 0.000000000000000000, -1.000000000000000000 ) ) ;
#7276=CARTESIAN_POINT ( 'NONE',  ( 11.57656516821460890, -3.100463633631699967, -8.407828142327998577 ) ) ;
#7284=ORIENTED_EDGE ( 'NONE', *, *, #11991, .F. ) ;
#7325=CARTESIAN_POINT ( 'NONE',  ( 10.91610672858429965, -4.911600290708499905, -6.814233985789400094 ) ) ;
#7329=CARTESIAN_POINT ( 'NONE',  ( 11.59999999999999787, -4.292035002842709446, -8.536357045506706598 ) ) ;
#7341=CARTESIAN_POINT ( 'NONE',  ( 9.756329965421999262, -4.697624103824200148, -8.222608407156599242 ) ) ;
#7357=CARTESIAN_POINT ( 'NONE',  ( 11.24441369783139777, -4.043700988887960257, -8.365094684940499903 ) ) ;
#7374=CARTESIAN_POINT ( 'NONE',  ( 10.38528584683667688, -3.267379250638399846, -8.166081851074052267 ) ) ;
#7384=CARTESIAN_POINT ( 'NONE',  ( 11.13459739833729856, -4.823158118387800286, -7.825000000000000178 ) ) ;
#7391=VERTEX_POINT ( 'NONE', #5922 ) ;
#7393=CARTESIAN_POINT ( 'NONE',  ( 10.98579841651039857, -4.449968941611500028, -8.696179055230999211 ) ) ;
#7397=CARTESIAN_POINT ( 'NONE',  ( 8.734200250017998712, -3.906155787512310074, -8.386722339907899837 ) ) ;
#7419=B_SPLINE_CURVE_WITH_KNOTS ( 'NONE', 3,
 ( #27561, #48888, #995, #24727 ),
 .UNSPECIFIED., .F., .F.,
 ( 4, 4 ),
 ( 0.000000000000000000, 1.000000000000000000 ),
 .UNSPECIFIED. ) ;
#7453=CARTESIAN_POINT ( 'NONE',  ( 9.961925467520998723, -5.139081147506999514, -7.421078600323300023 ) ) ;
#7473=ORIENTED_EDGE ( 'NONE', *, *, #4469, .F. ) ;
#7480=CARTESIAN_POINT ( 'NONE',  ( 11.05435090131019926, -2.880552878538999995, -8.192386390235398608 ) ) ;
#7556=CARTESIAN_POINT ( 'NONE',  ( 10.67375944625267614, -4.674697381537265883, -8.055763479958521600 ) ) ;
#7582=CARTESIAN_POINT ( 'NONE',  ( 8.923129650240841926, -4.658877085170329835, -6.641242496392400163 ) ) ;
#7590=CARTESIAN_POINT ( 'NONE',  ( 11.68788784977535933, -4.985985832792199979, -7.443657794094239222 ) ) ;
#7623=CARTESIAN_POINT ( 'NONE',  ( 10.34580110216399973, -5.090698144635000588, -6.833896451085399448 ) ) ;
#7641=CARTESIAN_POINT ( 'NONE',  ( 11.68277869730536977, -4.531392946702499813, -6.452143920160000157 ) ) ;
#7676=CARTESIAN_POINT ( 'NONE',  ( 10.05862282008599884, -3.333723918618700210, -8.574682153725998290 ) ) ;
#7690=CARTESIAN_POINT ( 'NONE',  ( 11.56493925477931306, -2.826469659297513370, -7.948835763880663485 ) ) ;
#7692=ORIENTED_EDGE ( 'NONE', *, *, #66861, .T. ) ;
#7694=CARTESIAN_POINT ( 'NONE',  ( 10.05826717315599872, -4.659895246859299789, -6.937642277832399174 ) ) ;
#7712=CARTESIAN_POINT ( 'NONE',  ( 10.77672335273219950, -3.698477709264200275, -8.312023951944400579 ) ) ;
#7734=CARTESIAN_POINT ( 'NONE',  ( 11.59999999999999964, -4.817420948848700313, -7.174999999999999822 ) ) ;
#7746=CARTESIAN_POINT ( 'NONE',  ( 10.46887750876899936, -4.692271380433699512, -8.574279626736998949 ) ) ;
#7754=CARTESIAN_POINT ( 'NONE',  ( 9.716846873515667227, -3.231816600031351516, -6.500416447002277387 ) ) ;
#7799=CARTESIAN_POINT ( 'NONE',  ( 10.71684687351633869, -3.231816600031351516, -6.500416447002277387 ) ) ;
#7804=CARTESIAN_POINT ( 'NONE',  ( 9.784621437244998887, -3.241588663654300095, -6.646450532840099790 ) ) ;
#7805=CARTESIAN_POINT ( 'NONE',  ( 9.791846873516668381, -4.999583552997724389, -6.731816600031356401 ) ) ;
#7823=CARTESIAN_POINT ( 'NONE',  ( 10.64393020684969926, -2.750000000000000000, -7.500000000000000000 ) ) ;
#7829=( NAMED_UNIT ( * ) SI_UNIT ( $, .STERADIAN. ) SOLID_ANGLE_UNIT ( ) );
#7837=CARTESIAN_POINT ( 'NONE',  ( 11.68277869730536977, -4.531392946702499813, -6.452143920160000157 ) ) ;
#7862=CARTESIAN_POINT ( 'NONE',  ( 10.03897570133299944, -3.061513547538400104, -8.369268408503399925 ) ) ;
#7909=CARTESIAN_POINT ( 'NONE',  ( 10.31652245563454073, -3.317579219585636174, -8.028218637173727856 ) ) ;
#7940=CARTESIAN_POINT ( 'NONE',  ( 10.77368717260499942, -4.539928529895099985, -8.381256426168800289 ) ) ;
#7993=CARTESIAN_POINT ( 'NONE',  ( 11.64633327354034797, -4.864904118400500188, -6.934277916748599502 ) ) ;
#8023=CARTESIAN_POINT ( 'NONE',  ( 11.71210404293059959, -4.381818659177399766, -8.277504409418298792 ) ) ;
#8024=CARTESIAN_POINT ( 'NONE',  ( 10.88733729122639993, -5.277570687708000641, -7.466391690027689876 ) ) ;
#8038=CARTESIAN_POINT ( 'NONE',  ( 9.982279731608999285, -3.922199073804859992, -6.636486849903699969 ) ) ;
#8056=CARTESIAN_POINT ( 'NONE',  ( 11.56025819896753859, -4.986099335708799707, -7.685900384398899554 ) ) ;
#8100=CARTESIAN_POINT ( 'NONE',  ( 10.20851354018233614, -3.836375382625528019, -6.250000000000001776 ) ) ;
#8105=CARTESIAN_POINT ( 'NONE',  ( 10.33364828895399867, -3.239803852721999888, -7.915211961479200475 ) ) ;
#8119=EDGE_LOOP ( 'NONE', ( #53420, #25848, #39685, #49955 ) ) ;
#8129=CARTESIAN_POINT ( 'NONE',  ( 10.42363156114900136, -4.684311564990209398, -8.575598637068461372 ) ) ;
#8149=CARTESIAN_POINT ( 'NONE',  ( 8.822113844317998499, -3.711648483798899889, -6.395197822644999697 ) ) ;
#8171=PLANE ( 'NONE',  #68578 ) ;
#8178=CARTESIAN_POINT ( 'NONE',  ( 11.59966954483535773, -3.361010663344000005, -6.514072057539499916 ) ) ;
#8204=CARTESIAN_POINT ( 'NONE',  ( 9.608380199233998553, -2.730774061183999901, -7.340469740450900282 ) ) ;
#8234=CARTESIAN_POINT ( 'NONE',  ( 8.784678295047998020, -4.000000000000000000, -7.500000000000000000 ) ) ;
#8261=CARTESIAN_POINT ( 'NONE',  ( 9.385596873516666605, -5.092232985442824322, -8.129523725463620565 ) ) ;
#8274=CARTESIAN_POINT ( 'NONE',  ( 8.916525748329496182, -4.536323992761255752, -6.567753456898076436 ) ) ;
#8284=CARTESIAN_POINT ( 'NONE',  ( 10.48280513895999988, -3.096689368913399854, -6.997844089834400094 ) ) ;
#8307=LINE ( 'NONE', #35229, #56209 ) ;
#8310=VERTEX_POINT ( 'NONE', #35631 ) ;
#8335=CARTESIAN_POINT ( 'NONE',  ( 11.43856039236529831, -2.967715280237000375, -7.550239075043479353 ) ) ;
#8367=CARTESIAN_POINT ( 'NONE',  ( 11.36749010443639918, -3.136214309321499805, -7.564597762509089662 ) ) ;
#8368=CARTESIAN_POINT ( 'NONE',  ( 10.66579975933730040, -2.791514215189000225, -7.084213409908699965 ) ) ;
#8385=CARTESIAN_POINT ( 'NONE',  ( 10.23557120343299864, -4.042028078047379402, -8.365991721916298474 ) ) ;
#8400=CARTESIAN_POINT ( 'NONE',  ( 11.70794988689359961, -3.544213289744700290, -8.393984925606600811 ) ) ;
#8405=ADVANCED_FACE ( 'NONE', ( #67080 ), #25466, .T. ) ;
#8437=VERTEX_POINT ( 'NONE', #46800 ) ;
#8448=CARTESIAN_POINT ( 'NONE',  ( 11.44133594839949986, -3.430493414882899827, -6.847343244997600387 ) ) ;
#8494=CARTESIAN_POINT ( 'NONE',  ( 9.531329965421999617, -4.793057006135000186, -8.321459087847200564 ) ) ;
#8520=CARTESIAN_POINT ( 'NONE',  ( 11.23078751119019891, -4.915752892793999962, -7.979095341142500075 ) ) ;
#8531=FILL_AREA_STYLE ('',( #24612 ) ) ;
#8546=CARTESIAN_POINT ( 'NONE',  ( 9.910317406968998100, -3.787635830142400462, -8.621889436328999068 ) ) ;
#8591=ORIENTED_EDGE ( 'NONE', *, *, #36867, .T. ) ;
#8606=CARTESIAN_POINT ( 'NONE',  ( 9.099999931440999390, -2.935682118448999844, -8.155535999783198875 ) ) ;
#8623=CARTESIAN_POINT ( 'NONE',  ( 10.93990547754509812, -2.967013601007999934, -7.532784233952049213 ) ) ;
#8658=CARTESIAN_POINT ( 'NONE',  ( 8.826138961223998436, -3.281636118526699786, -7.985449642667900250 ) ) ;
#8674=CARTESIAN_POINT ( 'NONE',  ( 11.05435090131019926, -2.880552878538999995, -8.192386390235398608 ) ) ;
#8679=ORIENTED_EDGE ( 'NONE', *, *, #324, .T. ) ;
#8708=CARTESIAN_POINT ( 'NONE',  ( 11.13349010443639919, -2.725546193138000284, -7.595309363461700158 ) ) ;
#8724=CARTESIAN_POINT ( 'NONE',  ( 9.224417874593999755, -4.924352284713100047, -7.892956936667999912 ) ) ;
#8741=CARTESIAN_POINT ( 'NONE',  ( 11.60948876160955479, -4.695527826393099957, -8.223320049540498999 ) ) ;
#8785=CARTESIAN_POINT ( 'NONE',  ( 9.429533309317625012, -3.366787958683358006, -6.896199718737570095 ) ) ;
#8790=CARTESIAN_POINT ( 'NONE',  ( 11.70794988689359961, -3.544213289744700290, -8.393984925606600811 ) ) ;
#8807=CARTESIAN_POINT ( 'NONE',  ( 11.21022026213526601, -2.954246606487285209, -7.824998325091605977 ) ) ;
#8837=CARTESIAN_POINT ( 'NONE',  ( 9.911267173156000254, -4.869050473540199597, -6.759401780699699103 ) ) ;
#8864=CARTESIAN_POINT ( 'NONE',  ( 11.05946005378019947, -2.963614890480000152, -6.946587256304699309 ) ) ;
#8870=DIRECTION ( 'NONE',  ( 0.000000000000000000, 1.000000000000000000, 0.000000000000000000 ) ) ;
#8873=AXIS2_PLACEMENT_3D ( 'NONE', #50208, #13502, #56134 ) ;
#8962=CARTESIAN_POINT ( 'NONE',  ( 10.47769598648999967, -2.990523684589000197, -8.101059042556599366 ) ) ;
#9004=ORIENTED_EDGE ( 'NONE', *, *, #26760, .F. ) ;
#9010=CARTESIAN_POINT ( 'NONE',  ( 10.92968717260509948, -4.687649763627899979, -8.622362941748999532 ) ) ;
#9038=CARTESIAN_POINT ( 'NONE',  ( 11.51518179236248862, -4.180996681294200101, -6.652923384986699773 ) ) ;
#9039=CARTESIAN_POINT ( 'NONE',  ( 10.05041772631199848, -3.450375740502100275, -8.631352948887998977 ) ) ;
#9054=ADVANCED_FACE ( 'NONE', ( #22171 ), #10629, .F. ) ;
#9060=CARTESIAN_POINT ( 'NONE',  ( 9.678329965421998082, -4.602191201513400109, -8.123757726465999696 ) ) ;
#9078=CARTESIAN_POINT ( 'NONE',  ( 10.89564560330029863, -3.692495237344800341, -6.544808043482999160 ) ) ;
#9121=CARTESIAN_POINT ( 'NONE',  ( 9.860128811416625894, -3.130392736003965393, -7.596516710088708990 ) ) ;
#9125=CARTESIAN_POINT ( 'NONE',  ( 11.41672066707849886, -3.258843737379200078, -7.051685395375099752 ) ) ;
#9135=ADVANCED_FACE ( 'NONE', ( #49097 ), #1184, .F. ) ;
#9170=CARTESIAN_POINT ( 'NONE',  ( 10.03590035061499997, -3.659038130401700339, -8.732935057095000175 ) ) ;
#9173=ADVANCED_FACE ( 'NONE', ( #9538 ), #31569, .F. ) ;
#9176=PLANE ( 'NONE',  #38412 ) ;
#9190=ORIENTED_EDGE ( 'NONE', *, *, #30043, .F. ) ;
#9195=CARTESIAN_POINT ( 'NONE',  ( 11.18412378248529926, -4.549028353065900809, -6.461285588983000316 ) ) ;
#9196=CARTESIAN_POINT ( 'NONE',  ( 11.60000000000000142, -3.636382150325345730, -6.469788275435904623 ) ) ;
#9288=LINE ( 'NONE', #47057, #3093 ) ;
#9360=CARTESIAN_POINT ( 'NONE',  ( 11.41486084871699802, -5.207010770456999893, -7.825000000000000178 ) ) ;
#9371=CARTESIAN_POINT ( 'NONE',  ( 11.68333460557258796, -3.837988184179999873, -8.490304555719900392 ) ) ;
#9411=CARTESIAN_POINT ( 'NONE',  ( 11.46179707368349909, -4.498457171163099844, -6.629085939160999530 ) ) ;
#9425=EDGE_LOOP ( 'NONE', ( #43323, #44695, #65662, #54629 ) ) ;
#9441=CARTESIAN_POINT ( 'NONE',  ( 8.710288521113000115, -4.352953559891299840, -8.284550957747498501 ) ) ;
#9456=CARTESIAN_POINT ( 'NONE',  ( 9.353545867770625577, -3.141341610201948686, -7.668041776205901883 ) ) ;
#9460=CARTESIAN_POINT ( 'NONE',  ( 10.82595391537419971, -3.283439621430300104, -7.986661909549199301 ) ) ;
#9469=CARTESIAN_POINT ( 'NONE',  ( 10.14393020684899938, -2.750000000000000000, -7.500000000000000000 ) ) ;
#9480=CARTESIAN_POINT ( 'NONE',  ( 10.66684687351589744, -3.231816600031351516, -6.500416447002278275 ) ) ;
#9511=CARTESIAN_POINT ( 'NONE',  ( 8.921417874593998931, -5.177249570814000279, -8.000467616829000761 ) ) ;
#9538=FACE_OUTER_BOUND ( 'NONE', #21085, .T. ) ;
#9571=CYLINDRICAL_SURFACE ( 'NONE', #67875, 1.250000000000000222 ) ;
#9676=AXIS2_PLACEMENT_3D ( 'NONE', #40345, #19020, #18341 ) ;
#9720=CARTESIAN_POINT ( 'NONE',  ( 10.29262282008599882, -3.548418513060800361, -8.228386593078399258 ) ) ;
#9741=CARTESIAN_POINT ( 'NONE',  ( 9.551684229509998403, -4.611171355610000688, -6.885038603985500494 ) ) ;
#9759=CARTESIAN_POINT ( 'NONE',  ( 11.35918179236250047, -4.238363971154499588, -6.384440618559000136 ) ) ;
#9802=CARTESIAN_POINT ( 'NONE',  ( 9.232128830620874638, -4.207195853723359136, -6.256996123608767668 ) ) ;
#9808=CARTESIAN_POINT ( 'NONE',  ( 10.28877584378239796, -3.533998264153197510, -8.236827240972795394 ) ) ;
#9813=CARTESIAN_POINT ( 'NONE',  ( 10.45257053952200010, -4.394359323863099576, -6.577269499510100204 ) ) ;
#9828=CARTESIAN_POINT ( 'NONE',  ( 10.31558376188599802, -4.962881317320600338, -8.113672563022399586 ) ) ;
#9863=CARTESIAN_POINT ( 'NONE',  ( 9.250696787962999323, -3.780328739572700325, -6.239790126677999815 ) ) ;
#9890=AXIS2_PLACEMENT_3D ( 'NONE', #21407, #4296, #4987 ) ;
#9892=CARTESIAN_POINT ( 'NONE',  ( 10.48791429142999831, -3.983006558652820051, -6.608036045330599961 ) ) ;
#9897=ORIENTED_EDGE ( 'NONE', *, *, #22389, .F. ) ;
#9923=DIRECTION ( 'NONE',  ( 0.000000000000000000, 1.000000000000000000, 0.000000000000000000 ) ) ;
#9944=CARTESIAN_POINT ( 'NONE',  ( 9.788646554150998824, -3.580250267348600079, -8.258629096756299859 ) ) ;
#10000=EDGE_CURVE ( 'NONE', #35196, #65063, #62059, .T. ) ;
#10029=VERTEX_POINT ( 'NONE', #18080 ) ;
#10035=ORIENTED_EDGE ( 'NONE', *, *, #56935, .F. ) ;
#10070=CARTESIAN_POINT ( 'NONE',  ( 11.21564426047340035, -3.460037133261700149, -8.345807871442598724 ) ) ;
#10091=CARTESIAN_POINT ( 'NONE',  ( 9.450367640780999778, -3.591293244209800228, -6.735364967924099666 ) ) ;
#10112=CARTESIAN_POINT ( 'NONE',  ( 11.30995122972050027, -3.547233695387300045, -6.452959986593999275 ) ) ;
#10138=EDGE_CURVE ( 'NONE', #41410, #13264, #9288, .T. ) ;
#10142=EDGE_CURVE ( 'NONE', #7391, #17504, #25377, .T. ) ;
#10153=VERTEX_POINT ( 'NONE', #30632 ) ;
#10158=CARTESIAN_POINT ( 'NONE',  ( 8.757986382567201744, -3.848432872973398755, -8.349715092260979077 ) ) ;
#10163=CARTESIAN_POINT ( 'NONE',  ( 11.69559063708295987, -2.913481137622000006, -7.805482129094999166 ) ) ;
#10180=CARTESIAN_POINT ( 'NONE',  ( 9.152455549953000258, -3.004437130344999929, -6.696732323226999739 ) ) ;
#10208=CARTESIAN_POINT ( 'NONE',  ( 8.946747021775999897, -4.961496216383199709, -8.343747244947598674 ) ) ;
#10229=CARTESIAN_POINT ( 'NONE',  ( 11.01456785386839954, -4.946394603182100447, -8.136888821800198457 ) ) ;
#10235=CARTESIAN_POINT ( 'NONE',  ( 9.893930206848997599, -5.250000000000000000, -7.500000000000000000 ) ) ;
#10285=CARTESIAN_POINT ( 'NONE',  ( 10.09058376188599837, -4.847012523549299345, -8.039825975318500184 ) ) ;
#10299=CARTESIAN_POINT ( 'NONE',  ( 10.52946886766499901, -4.430164648092599577, -6.718432993015899690 ) ) ;
#10308=ORIENTED_EDGE ( 'NONE', *, *, #20177, .F. ) ;
#10333=ORIENTED_EDGE ( 'NONE', *, *, #61779, .F. ) ;
#10399=ORIENTED_EDGE ( 'NONE', *, *, #10000, .F. ) ;
#10411=CARTESIAN_POINT ( 'NONE',  ( 10.62903166480609940, -4.864052766304100217, -7.560921321260908989 ) ) ;
#10447=CARTESIAN_POINT ( 'NONE',  ( 11.23610538575739959, -2.890527834009000152, -7.234742334405199315 ) ) ;
#10450=CARTESIAN_POINT ( 'NONE',  ( 10.08521345716899908, -3.075109701058799772, -8.340879262988799780 ) ) ;
#10499=CARTESIAN_POINT ( 'NONE',  ( 10.79718447801629999, -2.996774412198000448, -7.477880487566260115 ) ) ;
#10512=CARTESIAN_POINT ( 'NONE',  ( 9.896013540183126622, -4.999583552997726166, -8.268183399968641822 ) ) ;
#10515=CARTESIAN_POINT ( 'NONE',  ( 9.557721904870000174, -2.884547197234000215, -8.126218358304999612 ) ) ;
#10548=CARTESIAN_POINT ( 'NONE',  ( 9.807938025973999885, -4.665064168510499876, -6.407263051216999017 ) ) ;
#10563=CARTESIAN_POINT ( 'NONE',  ( 11.03111947020579819, -4.908799224006100026, -7.174999999999999822 ) ) ;
#10571=CARTESIAN_POINT ( 'NONE',  ( 11.37964291764649971, -5.268358781405000357, -7.343212302062899433 ) ) ;
#10576=CARTESIAN_POINT ( 'NONE',  ( 10.77879632507499785, -3.576455950783300253, -8.285174533868300273 ) ) ;
#10577=CARTESIAN_POINT ( 'NONE',  ( 9.748096873515667227, -3.672815144550895194, -6.282534154164607365 ) ) ;
#10579=CARTESIAN_POINT ( 'NONE',  ( 11.60000000000000142, -4.531190383827668811, -6.694115079111574218 ) ) ;
#10627=CARTESIAN_POINT ( 'NONE',  ( 9.282063610504998508, -3.644370728184199937, -8.290718512198798962 ) ) ;
#10629=B_SPLINE_SURFACE_WITH_KNOTS ( 'NONE', 3, 3, ( 
 ( #58204, #37225, #27781, #59577 ),
 ( #31994, #65155, #48749, #11678 ),
 ( #58542, #31641, #36888, #6088 ),
 ( #37561, #47724, #58894, #27087 ) ),
 .UNSPECIFIED., .F., .F., .F.,
 ( 4, 4 ),
 ( 4, 4 ),
 ( 0.7363163806532000422, 1.013499456067999960 ),
 ( -0.0005287450254680999126, 0.02696599629895000266 ),
 .UNSPECIFIED. ) ;
#10640=EDGE_CURVE ( 'NONE', #67987, #49260, #38656, .T. ) ;
#10641=CARTESIAN_POINT ( 'NONE',  ( 10.81524174883999834, -4.028418853626810403, -8.533115712456000423 ) ) ;
#10683=CARTESIAN_POINT ( 'NONE',  ( 10.34393020684899867, -5.250000000000000000, -7.500000000000000000 ) ) ;
#10706=B_SPLINE_CURVE_WITH_KNOTS ( 'NONE', 3,
 ( #45831, #2834, #62922, #9441 ),
 .UNSPECIFIED., .F., .F.,
 ( 4, 4 ),
 ( 0.000000000000000000, 1.000000000000000000 ),
 .UNSPECIFIED. ) ;
#10715=CARTESIAN_POINT ( 'NONE',  ( 10.92028665956053324, -4.742415037725373317, -8.549395343567624650 ) ) ;
#10756=CARTESIAN_POINT ( 'NONE',  ( 11.78179573085659904, -3.026866171144600326, -7.668383662421899061 ) ) ;
#10793=CARTESIAN_POINT ( 'NONE',  ( 10.52226222744799955, -4.880489021643899861, -8.225278704382400718 ) ) ;
#10845=CARTESIAN_POINT ( 'NONE',  ( 11.01872200990539952, -4.947480442174099657, -7.169497859994799605 ) ) ;
#10859=CARTESIAN_POINT ( 'NONE',  ( 9.783671671056998420, -5.126041103316000047, -7.689118697196099639 ) ) ;
#10893=CARTESIAN_POINT ( 'NONE',  ( 11.35565467195930367, -5.136173005413449566, -6.911917091190551865 ) ) ;
#10914=CARTESIAN_POINT ( 'NONE',  ( 10.54687750876899877, -4.617914354660699772, -8.458891008702400072 ) ) ;
#10928=VECTOR ( 'NONE', #19448, 1000.000000000000000 ) ;
#10976=CARTESIAN_POINT ( 'NONE',  ( 9.130088727410999638, -4.863977618062000019, -7.572461161969050281 ) ) ;
#10987=ORIENTED_EDGE ( 'NONE', *, *, #45316, .T. ) ;
#10989=CARTESIAN_POINT ( 'NONE',  ( 11.11123293495519881, -4.891405920092699589, -7.464165716332529676 ) ) ;
#11056=CARTESIAN_POINT ( 'NONE',  ( 8.599999952505998024, -4.000000000000000000, -7.500000000000000000 ) ) ;
#11095=VERTEX_POINT ( 'NONE', #4477 ) ;
#11105=CARTESIAN_POINT ( 'NONE',  ( 10.40333997687999990, -3.786145554879500441, -6.519583185858300212 ) ) ;
#11111=CARTESIAN_POINT ( 'NONE',  ( 10.51414141025500015, -3.384226587288500010, -8.596754040696000132 ) ) ;
#11141=CARTESIAN_POINT ( 'NONE',  ( 11.06379841651039797, -4.401637675674300532, -8.567697191971999970 ) ) ;
#11187=CARTESIAN_POINT ( 'NONE',  ( 10.50180110216399854, -4.856393875115199599, -6.976989117212499814 ) ) ;
#11199=CARTESIAN_POINT ( 'NONE',  ( 10.09393020684899867, -2.750000000000000000, -7.500000000000000000 ) ) ;
#11204=CARTESIAN_POINT ( 'NONE',  ( 10.00962143724499853, -3.332852462363599777, -6.749162825004299648 ) ) ;
#11253=CARTESIAN_POINT ( 'NONE',  ( 10.96533729122639933, -5.140346530769000388, -7.470001566214039990 ) ) ;
#11257=CARTESIAN_POINT ( 'NONE',  ( 8.734020077949999461, -4.063547279775290733, -8.378811912355599745 ) ) ;
#11312=CARTESIAN_POINT ( 'NONE',  ( 9.811963142879999822, -3.017187828228399926, -7.292822454528599785 ) ) ;
#11324=PRODUCT_CONTEXT ( 'NONE', #24408, 'mechanical' ) ;
#11325=CARTESIAN_POINT ( 'NONE',  ( 10.77879632507499785, -3.576455950783300253, -8.285174533868300273 ) ) ;
#11403=CARTESIAN_POINT ( 'NONE',  ( 11.59999999999999964, -4.000000000000000000, -7.500000000000000000 ) ) ;
#11409=B_SPLINE_CURVE_WITH_KNOTS ( 'NONE', 3,
 ( #7823, #29160, #7128, #66540, #44891, #60272, #28466, #65150, #12027, #49780, #23210, #66195, #60616, #18659, #65502, #39640, #44558, #1538 ),
 .UNSPECIFIED., .F., .F.,
 ( 4, 2, 2, 2, 2, 2, 2, 2, 4 ),
 ( 0.000000000000000000, 0.1250000000000000000, 0.2500000000000000000, 0.3750000000000000000, 0.5000000000000000000, 0.6250000000000000000, 0.7500000000000000000, 0.8750000000000000000, 1.000000000000000000 ),
 .UNSPECIFIED. ) ;
#11442=CARTESIAN_POINT ( 'NONE',  ( 10.47718582084299932, -4.656536239972400182, -6.741111985563299491 ) ) ;
#11446=CARTESIAN_POINT ( 'NONE',  ( 11.18412378248529926, -4.549028353065900809, -6.461285588983000316 ) ) ;
#11476=CARTESIAN_POINT ( 'NONE',  ( 10.54272335273199879, -3.555125495332600138, -8.698083075453000745 ) ) ;
#11496=CARTESIAN_POINT ( 'NONE',  ( 11.84388784977539899, -5.255745690988000263, -7.428242901739219306 ) ) ;
#11512=CARTESIAN_POINT ( 'NONE',  ( 9.323602683899247623, -5.219044746006709978, -7.180752970636812726 ) ) ;
#11523=CARTESIAN_POINT ( 'NONE',  ( 10.76841504065829902, -3.085489673376300424, -6.818119527508899935 ) ) ;
#11529=CARTESIAN_POINT ( 'NONE',  ( 11.59999999999999787, -3.261098123302579754, -8.470724288896150256 ) ) ;
#11540=CARTESIAN_POINT ( 'NONE',  ( 9.857646554150999663, -3.513729974241599940, -8.378853663802400931 ) ) ;
#11567=B_SPLINE_CURVE_WITH_KNOTS ( 'NONE', 3,
 ( #22492, #12362, #1522, #23537, #66182, #18302, #39626, #60947, #33693, #22842, #13408, #29146, #65834, #7805, #28805, #13061, #44542, #50116 ),
 .UNSPECIFIED., .F., .F.,
 ( 4, 2, 2, 2, 2, 2, 2, 2, 4 ),
 ( 0.000000000000000000, 0.1250000000000003331, 0.2500000000000006661, 0.3750000000000009992, 0.5000000000000013323, 0.6250000000000009992, 0.7500000000000006661, 0.8750000000000003331, 1.000000000000000000 ),
 .UNSPECIFIED. ) ;
#11583=EDGE_CURVE ( 'NONE', #30840, #42489, #14398, .T. ) ;
#11584=CARTESIAN_POINT ( 'NONE',  ( 8.810863317747999801, -3.039136629551499880, -7.500000000073117512 ) ) ;
#11592=CARTESIAN_POINT ( 'NONE',  ( 11.13764426047339917, -3.386171819220400003, -8.461511872390000022 ) ) ;
#11593=ORIENTED_EDGE ( 'NONE', *, *, #10640, .T. ) ;
#11600=CARTESIAN_POINT ( 'NONE',  ( 9.696013540182335078, -3.000416447002272058, -6.731816600031361730 ) ) ;
#11601=CARTESIAN_POINT ( 'NONE',  ( 11.59999999999999964, -4.447112190091930373, -6.627718330236055166 ) ) ;
#11616=CARTESIAN_POINT ( 'NONE',  ( 9.529346873515667227, -3.836375382625533348, -8.749999999999998224 ) ) ;
#11656=CARTESIAN_POINT ( 'NONE',  ( 9.432025935145999185, -4.145841638824199649, -6.506233167833100239 ) ) ;
#11668=CARTESIAN_POINT ( 'NONE',  ( 10.40480513895999870, -3.220259576336399920, -7.066537524675499782 ) ) ;
#11678=CARTESIAN_POINT ( 'NONE',  ( 8.748004441081999261, -4.389076025353599420, -8.341443180570399463 ) ) ;
#11685=CARTESIAN_POINT ( 'NONE',  ( 11.13746005378019888, -2.838900981960999825, -6.879992063401499713 ) ) ;
#11711=CARTESIAN_POINT ( 'NONE',  ( 10.34292546752099895, -5.276153033933000280, -7.411581555133209598 ) ) ;
#11790=CARTESIAN_POINT ( 'NONE',  ( 10.25564828895399927, -3.119330945648699949, -7.981013126389099099 ) ) ;
#11793=ORIENTED_EDGE ( 'NONE', *, *, #44537, .T. ) ;
#11794=CARTESIAN_POINT ( 'NONE',  ( 10.63880513895979973, -2.849548954067000039, -6.860457220153399760 ) ) ;
#11824=CARTESIAN_POINT ( 'NONE',  ( 11.62579573085663043, -2.760622544769000264, -7.714452430741599365 ) ) ;
#11875=CARTESIAN_POINT ( 'NONE',  ( 11.55194988689359903, -3.419512757306400363, -8.638573882912000457 ) ) ;
#11880=CARTESIAN_POINT ( 'NONE',  ( 11.60000000000000320, -4.813068503488584504, -8.037608584222631691 ) ) ;
#11892=CARTESIAN_POINT ( 'NONE',  ( 8.973138961223998677, -3.053949131563199693, -8.139313957553699908 ) ) ;
#11910=CARTESIAN_POINT ( 'NONE',  ( 11.26902897915239876, -3.778278678798900447, -8.337339982364900592 ) ) ;
#11947=CARTESIAN_POINT ( 'NONE',  ( 10.27195525820100031, -4.120672149427799802, -6.227697122196000024 ) ) ;
#11954=CARTESIAN_POINT ( 'NONE',  ( 10.09393020684899867, -2.750000000000000000, -7.500000000000000000 ) ) ;
#11959=CARTESIAN_POINT ( 'NONE',  ( 11.46595122972049907, -3.656201404350900130, -6.704952129760900270 ) ) ;
#11979=VECTOR ( 'NONE', #34055, 1000.000000000000000 ) ;
#11991=EDGE_CURVE ( 'NONE', #17504, #44736, #45282, .T. ) ;
#12003=CARTESIAN_POINT ( 'NONE',  ( 10.65434687351636178, -2.749999999999998668, -7.336375382625537789 ) ) ;
#12010=CARTESIAN_POINT ( 'NONE',  ( 9.457355082327998375, -4.449513475323099598, -6.601790705997299114 ) ) ;
#12027=CARTESIAN_POINT ( 'NONE',  ( 10.52934687351650389, -3.836375382625533348, -8.749999999999998224 ) ) ;
#12041=CARTESIAN_POINT ( 'NONE',  ( 10.63880513895979973, -2.849548954067000039, -6.860457220153399760 ) ) ;
#12069=CARTESIAN_POINT ( 'NONE',  ( 9.887000818240000655, -5.131870447930000800, -8.096031607030200306 ) ) ;
#12098=DIRECTION ( 'NONE',  ( 1.000000000000000000, 0.000000000000000000, 0.000000000000000000 ) ) ;
#12148=CARTESIAN_POINT ( 'NONE',  ( 10.42795525820099911, -4.094749303624469761, -6.501013802764199490 ) ) ;
#12152=CARTESIAN_POINT ( 'NONE',  ( 11.59966954483535773, -3.361010663344000005, -6.514072057539499916 ) ) ;
#12181=CARTESIAN_POINT ( 'NONE',  ( 11.47810404293059960, -4.563346034752700398, -8.647151967355000579 ) ) ;
#12234=CARTESIAN_POINT ( 'NONE',  ( 11.45348876160960039, -4.885820101980599794, -8.421216112044099589 ) ) ;
#12250=CARTESIAN_POINT ( 'NONE',  ( 9.429063610504998749, -3.531653260805799999, -8.541338455964998744 ) ) ;
#12267=CARTESIAN_POINT ( 'NONE',  ( 10.89979975933730039, -3.180925410802600162, -7.218192605361100078 ) ) ;
#12299=EDGE_LOOP ( 'NONE', ( #15496, #10987, #67445, #66971, #39826 ) ) ;
#12355=EDGE_CURVE ( 'NONE', #2906, #40590, #12652, .T. ) ;
#12361=CARTESIAN_POINT ( 'NONE',  ( 8.722809814040999754, -3.385590752329799891, -8.294571108394100278 ) ) ;
#12362=CARTESIAN_POINT ( 'NONE',  ( 9.604346873516666605, -2.749999999999998224, -7.336375382625535124 ) ) ;
#12388=CARTESIAN_POINT ( 'NONE',  ( 10.92968717260509948, -4.687649763627899979, -8.622362941748999532 ) ) ;
#12415=DIRECTION ( 'NONE',  ( 0.000000000000000000, 0.8514543052404082157, -0.5244287998266055073 ) ) ;
#12462=CARTESIAN_POINT ( 'NONE',  ( 10.55068303964747578, -4.571908710946855692, -6.838932659516637536 ) ) ;
#12492=CARTESIAN_POINT ( 'NONE',  ( 11.76588784977539781, -5.120865761890000201, -7.435950347916509884 ) ) ;
#12525=CARTESIAN_POINT ( 'NONE',  ( 11.30579707368350029, -4.634832087857400751, -6.390809033205999690 ) ) ;
#12570=AXIS2_PLACEMENT_3D ( 'NONE', #39081, #49563, #7261 ) ;
#12578=CARTESIAN_POINT ( 'NONE',  ( 11.01456785386839954, -4.946394603182100447, -8.136888821800198457 ) ) ;
#12595=CARTESIAN_POINT ( 'NONE',  ( 8.971126402771000485, -3.060189502158800146, -7.145601175474399547 ) ) ;
#12611=CARTESIAN_POINT ( 'NONE',  ( 10.62903166480609940, -4.864052766304100217, -7.560921321260908989 ) ) ;
#12652=B_SPLINE_CURVE_WITH_KNOTS ( 'NONE', 3,
 ( #36061, #52483, #3219, #14408, #57377, #9480, #24886, #46562, #30823, #51794, #62290, #46903, #56709, #67868, #31179, #30480, #3891, #40967 ),
 .UNSPECIFIED., .F., .F.,
 ( 4, 2, 2, 2, 2, 2, 2, 2, 4 ),
 ( 0.000000000000000000, 0.1250000000000003331, 0.2500000000000006661, 0.3750000000000009992, 0.5000000000000013323, 0.6250000000000009992, 0.7500000000000006661, 0.8750000000000003331, 1.000000000000000000 ),
 .UNSPECIFIED. ) ;
#12660=ORIENTED_EDGE ( 'NONE', *, *, #63508, .F. ) ;
#12665=ADVANCED_FACE ( 'NONE', ( #29692 ), #50993, .T. ) ;
#12706=EDGE_CURVE ( 'NONE', #6018, #64952, #5988, .T. ) ;
#12709=CARTESIAN_POINT ( 'NONE',  ( 8.655265421554998895, -4.188500707411799695, -8.475084258675400051 ) ) ;
#12731=( LENGTH_UNIT ( ) NAMED_UNIT ( * ) SI_UNIT ( .MILLI., .METRE. ) );
#12748=( LENGTH_UNIT ( ) NAMED_UNIT ( * ) SI_UNIT ( .MILLI., .METRE. ) );
#12763=AXIS2_PLACEMENT_3D ( 'NONE', #34764, #66902, #8870 ) ;
#12843=ORIENTED_EDGE ( 'NONE', *, *, #2139, .T. ) ;
#12844=CARTESIAN_POINT ( 'NONE',  ( 11.11123293495519881, -4.891405920092699589, -7.464165716332529676 ) ) ;
#12859=CARTESIAN_POINT ( 'NONE',  ( 8.736413463905998711, -3.915843685459630574, -8.382409559052598880 ) ) ;
#12876=CARTESIAN_POINT ( 'NONE',  ( 10.39503166480599994, -5.274847857784000560, -7.589885038193400213 ) ) ;
#12880=CARTESIAN_POINT ( 'NONE',  ( 10.24457120343299898, -4.042028078047379402, -8.365991721916298474 ) ) ;
#12889=EDGE_LOOP ( 'NONE', ( #30341, #52691, #45642, #10308 ) ) ;
#12895=CARTESIAN_POINT ( 'NONE',  ( 11.67766954483535891, -3.284117569315500251, -6.395429936871999566 ) ) ;
#12900=ORIENTED_EDGE ( 'NONE', *, *, #40069, .T. ) ;
#12927=CARTESIAN_POINT ( 'NONE',  ( 11.12133729122639991, -4.865898216891100247, -7.477221318588949117 ) ) ;
#12928=CARTESIAN_POINT ( 'NONE',  ( 10.86687616594229944, -4.344946439135400240, -6.412662853391999818 ) ) ;
#12945=CARTESIAN_POINT ( 'NONE',  ( 9.047113844317999920, -3.746347404385800051, -6.528144732449299603 ) ) ;
#12965=CARTESIAN_POINT ( 'NONE',  ( 11.61364291764652812, -4.859654669415900408, -7.393734108507599601 ) ) ;
#13001=CARTESIAN_POINT ( 'NONE',  ( 10.17349413291699811, -2.837298848764000514, -6.969488574374499201 ) ) ;
#13056=CARTESIAN_POINT ( 'NONE',  ( 10.85226354018294792, -5.092232985442820770, -6.870476274536370553 ) ) ;
#13060=CARTESIAN_POINT ( 'NONE',  ( 8.644809814040998575, -3.301541394817099739, -8.403266072559899769 ) ) ;
#13061=CARTESIAN_POINT ( 'NONE',  ( 9.823096873516664829, -5.217465845835395299, -7.172815144550894750 ) ) ;
#13068=VECTOR ( 'NONE', #47290, 1000.000000000000000 ) ;
#13074=CARTESIAN_POINT ( 'NONE',  ( 11.59999999999999964, -4.000000000000000000, -7.500000000000000000 ) ) ;
#13097=( LENGTH_UNIT ( ) NAMED_UNIT ( * ) SI_UNIT ( .MILLI., .METRE. ) );
#13118=CARTESIAN_POINT ( 'NONE',  ( 10.46957120343300041, -4.062009413492949861, -8.777708647662999297 ) ) ;
#13167=CARTESIAN_POINT ( 'NONE',  ( 10.74760529021567734, -3.959614718189205185, -8.373188771871163283 ) ) ;
#13199=CARTESIAN_POINT ( 'NONE',  ( 11.56322412107030928, -3.945399343424460525, -6.467939235001000320 ) ) ;
#13233=CARTESIAN_POINT ( 'NONE',  ( 10.11792546752099931, -4.864937374655599278, -7.440072690703440017 ) ) ;
#13248=CARTESIAN_POINT ( 'NONE',  ( 10.97635090131019986, -3.000792947412299849, -8.118017011233499503 ) ) ;
#13264=VERTEX_POINT ( 'NONE', #22683 ) ;
#13280=CARTESIAN_POINT ( 'NONE',  ( 11.26902897915239876, -3.778278678798900447, -8.337339982364900592 ) ) ;
#13285=ORIENTED_EDGE ( 'NONE', *, *, #59704, .F. ) ;
#13299=CARTESIAN_POINT ( 'NONE',  ( 9.830304848515998728, -3.211495113978299898, -7.860510733857099197 ) ) ;
#13317=CARTESIAN_POINT ( 'NONE',  ( 11.58487348028854846, -4.882707455860599843, -7.977261354519500358 ) ) ;
#13348=CARTESIAN_POINT ( 'NONE',  ( 10.05041772631199848, -3.450375740502100275, -8.631352948887998977 ) ) ;
#13353=CARTESIAN_POINT ( 'NONE',  ( 8.691343736187999269, -4.374232398910099739, -8.309341309902798400 ) ) ;
#13360=CARTESIAN_POINT ( 'NONE',  ( 11.12133729122639991, -4.865898216891100247, -7.477221318588949117 ) ) ;
#13407=CARTESIAN_POINT ( 'NONE',  ( 9.556659112603998807, -4.496147888241900148, -8.528383061402999843 ) ) ;
#13408=CARTESIAN_POINT ( 'NONE',  ( 9.739763540183334456, -4.327184855449098144, -6.282534154164605589 ) ) ;
#13437=CARTESIAN_POINT ( 'NONE',  ( 10.68546886766499959, -4.566506264294200257, -6.470713638631999665 ) ) ;
#13461=CARTESIAN_POINT ( 'NONE',  ( 9.633709346416999608, -2.844451673749999632, -6.951281079990299538 ) ) ;
#13494=DIRECTION ( 'NONE',  ( 0.000000000000000000, 0.000000000000000000, -1.000000000000000000 ) ) ;
#13502=DIRECTION ( 'NONE',  ( -1.000000000000000000, 0.000000000000000000, 0.000000000000000000 ) ) ;
#13511=ORIENTED_EDGE ( 'NONE', *, *, #48532, .F. ) ;
#13532=CARTESIAN_POINT ( 'NONE',  ( 8.903317944506804693, -4.274905112035349397, -6.473766235688636073 ) ) ;
#13535=CARTESIAN_POINT ( 'NONE',  ( 9.925810748568999031, -5.172583146916751140, -8.000243450341617546 ) ) ;
#13540=CARTESIAN_POINT ( 'NONE',  ( 11.27745123989519982, -3.589787500396900199, -8.292221125039500151 ) ) ;
#13591=CARTESIAN_POINT ( 'NONE',  ( 10.43614141025499897, -3.450366949021700158, -8.478951440767898973 ) ) ;
#13621=CARTESIAN_POINT ( 'NONE',  ( 10.93656785386839836, -5.060279460151999587, -8.213529149347399638 ) ) ;
#13636=CARTESIAN_POINT ( 'NONE',  ( 10.15958376188599921, -4.731143729777899765, -7.965979387614599894 ) ) ;
#13652=CARTESIAN_POINT ( 'NONE',  ( 10.77256919669529900, -3.037654633983899899, -7.784327714719899483 ) ) ;
#13683=EDGE_CURVE ( 'NONE', #46774, #15621, #36800, .T. ) ;
#13696=CARTESIAN_POINT ( 'NONE',  ( 9.378875014952626543, -3.131883468830893857, -7.390885577342253931 ) ) ;
#13700=CARTESIAN_POINT ( 'NONE',  ( 10.43210941423799909, -3.358814833524500276, -6.917608226833099394 ) ) ;
#13740=CARTESIAN_POINT ( 'NONE',  ( 11.59999999999999964, -4.000000000000000000, -7.500000000000000000 ) ) ;
#13743=EDGE_CURVE ( 'NONE', #59745, #6314, #41734, .T. ) ;
#13744=CARTESIAN_POINT ( 'NONE',  ( 8.771455549952998254, -3.111370763671500228, -6.783011486330899231 ) ) ;
#13772=CARTESIAN_POINT ( 'NONE',  ( 10.81524174883999834, -4.028418853626810403, -8.533115712456000423 ) ) ;
#13798=CARTESIAN_POINT ( 'NONE',  ( 9.986304848515999311, -2.961576783819000358, -7.974775391194199869 ) ) ;
#13876=CARTESIAN_POINT ( 'NONE',  ( 11.02301463001509774, -3.452642973349600464, -6.623338154204899908 ) ) ;
#13908=CARTESIAN_POINT ( 'NONE',  ( 10.27195525820100031, -4.120672149427799802, -6.227697122196000024 ) ) ;
#13913=CARTESIAN_POINT ( 'NONE',  ( 8.927455549952998837, -3.325238030324599858, -6.955569812538500152 ) ) ;
#13927=CARTESIAN_POINT ( 'NONE',  ( 10.97124174884019965, -4.036194082918090231, -8.815770025351000072 ) ) ;
#13929=ORIENTED_EDGE ( 'NONE', *, *, #25310, .F. ) ;
#13935=EDGE_LOOP ( 'NONE', ( #45723, #48071, #38961, #44433 ) ) ;
#13958=CARTESIAN_POINT ( 'NONE',  ( 11.83518044953559922, -3.231951024059400268, -7.900497508315099893 ) ) ;
#13959=CARTESIAN_POINT ( 'NONE',  ( 10.41964694612699915, -5.186980343482999523, -7.973702485506099613 ) ) ;
#13974=EDGE_CURVE ( 'NONE', #65063, #50859, #65533, .T. ) ;
#13978=CARTESIAN_POINT ( 'NONE',  ( 9.553696787962998371, -3.827518619249500098, -6.510508982544899403 ) ) ;
#13990=EDGE_CURVE ( 'NONE', #64554, #59745, #39669, .T. ) ;
#13995=CARTESIAN_POINT ( 'NONE',  ( 10.55103166480599874, -5.000984463463999496, -7.570575893572789816 ) ) ;
#14038=CARTESIAN_POINT ( 'NONE',  ( 9.226900131858625898, -4.185762427694958987, -8.354999759870066711 ) ) ;
#14042=CARTESIAN_POINT ( 'NONE',  ( 11.78179573085659904, -3.026866171144600326, -7.668383662421899061 ) ) ;
#14058=ORIENTED_EDGE ( 'NONE', *, *, #55663, .F. ) ;
#14088=CARTESIAN_POINT ( 'NONE',  ( 10.10344474310099905, -2.862064370975999861, -8.052229793103100164 ) ) ;
#14117=CARTESIAN_POINT ( 'NONE',  ( 10.69057802013490033, -5.033226574983999946, -7.475947032624040034 ) ) ;
#14118=CARTESIAN_POINT ( 'NONE',  ( 11.59999999999999964, -2.912667852269566815, -6.982348652072319695 ) ) ;
#14130=CARTESIAN_POINT ( 'NONE',  ( 8.733215486276282746, -3.972057587790281730, -8.383215533252753815 ) ) ;
#14141=CARTESIAN_POINT ( 'NONE',  ( 9.380417874594000338, -5.177249570814000279, -8.000467616829000761 ) ) ;
#14143=STYLED_ITEM ( 'NONE', ( #19361 ), #23576 ) ;
#14219=CARTESIAN_POINT ( 'NONE',  ( 10.44125056272499918, -2.966599088466999934, -7.515315513715298934 ) ) ;
#14255=CARTESIAN_POINT ( 'NONE',  ( 9.611342523874998989, -4.857027829858100887, -7.368808371628100318 ) ) ;
#14269=CARTESIAN_POINT ( 'NONE',  ( 10.52799293566599914, -3.193321847920899792, -8.489570425681801424 ) ) ;
#14302=CARTESIAN_POINT ( 'NONE',  ( 11.17056785386839834, -4.718624889240500053, -7.983608166707499620 ) ) ;
#14303=CARTESIAN_POINT ( 'NONE',  ( 10.12426357027499790, -2.745128867668000350, -7.742104041724699570 ) ) ;
#14321=CARTESIAN_POINT ( 'NONE',  ( 9.095759580228998331, -4.843256805554699618, -7.298441312785299395 ) ) ;
#14338=CARTESIAN_POINT ( 'NONE',  ( 11.36333594839950045, -3.340240242524600056, -6.743912759487099784 ) ) ;
#14367=ADVANCED_FACE ( 'NONE', ( #33117 ), #64905, .F. ) ;
#14384=CARTESIAN_POINT ( 'NONE',  ( 9.758812222687625493, -3.837269700090108593, -8.359680823568968577 ) ) ;
#14388=CARTESIAN_POINT ( 'NONE',  ( 10.62903166480609940, -4.864052766304100217, -7.560921321260908989 ) ) ;
#14398=B_SPLINE_CURVE_WITH_KNOTS ( 'NONE', 3,
 ( #3709, #20489, #31333, #62782, #62445, #25046, #68030, #52302, #4051, #46378 ),
 .UNSPECIFIED., .F., .F.,
 ( 4, 2, 2, 2, 4 ),
 ( 0.000000000000000000, 0.2500000000000003331, 0.5000000000000006661, 0.7500000000000003331, 1.000000000000000000 ),
 .UNSPECIFIED. ) ;
#14402=AXIS2_PLACEMENT_3D ( 'NONE', #8234, #66266, #61031 ) ;
#14408=CARTESIAN_POINT ( 'NONE',  ( 10.63559687351579974, -2.907767014557175678, -6.870476274536380323 ) ) ;
#14415=CARTESIAN_POINT ( 'NONE',  ( 10.37581074856900187, -5.172583146916752028, -8.000243450341619322 ) ) ;
#14433=CARTESIAN_POINT ( 'NONE',  ( 9.024747021775999301, -4.858221690000700477, -8.253120162257399528 ) ) ;
#14453=VERTEX_POINT ( 'NONE', #8606 ) ;
#14461=CARTESIAN_POINT ( 'NONE',  ( 11.48011496860029901, -3.080230834057799960, -7.028661263734299780 ) ) ;
#14462=CARTESIAN_POINT ( 'NONE',  ( 11.60000000000000142, -3.195619894033323583, -6.677026092743741259 ) ) ;
#14507=DIRECTION ( 'NONE',  ( 0.000000000000000000, 1.000000000000000000, 0.000000000000000000 ) ) ;
#14581=CARTESIAN_POINT ( 'NONE',  ( 11.33570505509991655, -3.091015088729731186, -7.175001305235313431 ) ) ;
#14638=CARTESIAN_POINT ( 'NONE',  ( 10.40749413291699987, -3.211956830789300277, -7.140435631538599281 ) ) ;
#14639=CARTESIAN_POINT ( 'NONE',  ( 10.32118582084299874, -4.836160649475099937, -6.533484739457099622 ) ) ;
#14641=CARTESIAN_POINT ( 'NONE',  ( 11.59999999999999964, -4.000000000000000000, -7.500000000000000000 ) ) ;
#14655=CARTESIAN_POINT ( 'NONE',  ( 11.41544519387737289, -3.267573604823260869, -7.017892448335746103 ) ) ;
#14677=CARTESIAN_POINT ( 'NONE',  ( 10.92026088462129962, -3.997864853650589634, -6.496532863517000322 ) ) ;
#14721=CARTESIAN_POINT ( 'NONE',  ( 10.21473687196862734, -4.313773474582136558, -8.316748708918906274 ) ) ;
#14725=CARTESIAN_POINT ( 'NONE',  ( 10.30903300763299946, -3.402282662142699809, -8.126922218169600143 ) ) ;
#14732=CARTESIAN_POINT ( 'NONE',  ( 10.16476354018241501, -2.782534154164604256, -7.172815144550905408 ) ) ;
#14774=CARTESIAN_POINT ( 'NONE',  ( 9.655963142879999239, -2.748296264808000267, -7.236139910592400248 ) ) ;
#14800=CARTESIAN_POINT ( 'NONE',  ( 11.22567835872029995, -4.993948309075300074, -6.873560442659099046 ) ) ;
#14803=CARTESIAN_POINT ( 'NONE',  ( 8.929547492598356229, -3.266100554355691354, -8.304419251562590532 ) ) ;
#14807=ORIENTED_EDGE ( 'NONE', *, *, #34831, .T. ) ;
#14829=FACE_OUTER_BOUND ( 'NONE', #8119, .T. ) ;
#14900=CARTESIAN_POINT ( 'NONE',  ( 10.98656920625009903, -3.967932847735990531, -6.608450613814399688 ) ) ;
#14974=CARTESIAN_POINT ( 'NONE',  ( 11.43718179236249988, -4.209680326224799707, -6.518682001772900136 ) ) ;
#14994=CARTESIAN_POINT ( 'NONE',  ( 9.501025935145998247, -4.125890936441000356, -6.642177514500700042 ) ) ;
#15013=CARTESIAN_POINT ( 'NONE',  ( 11.21149010443640037, -2.862435565199000109, -7.585072163144589652 ) ) ;
#15059=CARTESIAN_POINT ( 'NONE',  ( 9.252229279041625176, -3.908861085869333785, -8.370187317335780364 ) ) ;
#15063=CARTESIAN_POINT ( 'NONE',  ( 11.55610404293055993, -4.502836909561000134, -8.523936114709998790 ) ) ;
#15066=AXIS2_PLACEMENT_3D ( 'NONE', #67066, #2078, #40845 ) ;
#15114=CARTESIAN_POINT ( 'NONE',  ( 9.681292290062998518, -2.893743561734000380, -6.857675253263499471 ) ) ;
#15125=AXIS2_PLACEMENT_3D ( 'NONE', #3292, #45947, #12415 ) ;
#15127=CARTESIAN_POINT ( 'NONE',  ( 11.07299956498199833, -2.792989229543000107, -7.825000000000000178 ) ) ;
#15178=CARTESIAN_POINT ( 'NONE',  ( 11.85979573085659844, -3.159987984332300215, -7.645349278262099979 ) ) ;
#15295=ORIENTED_EDGE ( 'NONE', *, *, #45316, .F. ) ;
#15315=CARTESIAN_POINT ( 'NONE',  ( 11.56914347478616634, -3.251273819902354312, -8.529874251157636422 ) ) ;
#15323=CARTESIAN_POINT ( 'NONE',  ( 10.99826088462129903, -3.998156935320088756, -6.633804182961699603 ) ) ;
#15362=CARTESIAN_POINT ( 'NONE',  ( 11.62994988689359843, -3.481863023525599843, -8.516279404258998653 ) ) ;
#15380=CARTESIAN_POINT ( 'NONE',  ( 10.55478570706233299, -2.868293641868291388, -8.113400509224881318 ) ) ;
#15405=CARTESIAN_POINT ( 'NONE',  ( 9.272783876522375124, -4.789858247946766845, -6.518107589053542483 ) ) ;
#15414=CARTESIAN_POINT ( 'NONE',  ( 11.60533460557258323, -3.815825449682300086, -8.625775273268001087 ) ) ;
#15429=CARTESIAN_POINT ( 'NONE',  ( 9.076468108405999047, -2.769196120524999749, -7.848577323721800170 ) ) ;
#15461=CARTESIAN_POINT ( 'NONE',  ( 8.592138961223998450, -2.940105638081000006, -8.216246114996598848 ) ) ;
#15483=CARTESIAN_POINT ( 'NONE',  ( 11.30579707368350029, -4.634832087857400751, -6.390809033205999690 ) ) ;
#15488=CARTESIAN_POINT ( 'NONE',  ( 10.39969598649000027, -3.111999510220800236, -8.028730309000598808 ) ) ;
#15496=ORIENTED_EDGE ( 'NONE', *, *, #38032, .F. ) ;
#15502=LINE ( 'NONE', #31584, #42996 ) ;
#15539=CARTESIAN_POINT ( 'NONE',  ( 10.21722949779699974, -3.442773960835399993, -8.335668797826500054 ) ) ;
#15553=CARTESIAN_POINT ( 'NONE',  ( 10.80502344389999791, -5.125258734743999511, -6.817099149379099110 ) ) ;
#15586=CARTESIAN_POINT ( 'NONE',  ( 9.414763540182331525, -5.217465845835395299, -7.827184855449099921 ) ) ;
#15588=CARTESIAN_POINT ( 'NONE',  ( 10.40480513895999870, -3.220259576336399920, -7.066537524675499782 ) ) ;
#15621=VERTEX_POINT ( 'NONE', #55275 ) ;
#15666=CARTESIAN_POINT ( 'NONE',  ( 10.80133863405319872, -3.465595476214000215, -8.181696703306599261 ) ) ;
#15669=EDGE_LOOP ( 'NONE', ( #581, #58969, #46029, #26329 ) ) ;
#15682=CARTESIAN_POINT ( 'NONE',  ( 9.374380199233998567, -3.139757597894699881, -7.391875284387199763 ) ) ;
#15703=CARTESIAN_POINT ( 'NONE',  ( 11.70379573085659786, -2.893744357957000357, -7.691418046581699919 ) ) ;
#15754=CARTESIAN_POINT ( 'NONE',  ( 11.65456516821461008, -3.197083038490000195, -8.310318115935698913 ) ) ;
#15757=CARTESIAN_POINT ( 'NONE',  ( 11.59999999999999964, -4.883784007588900522, -7.825000000000000178 ) ) ;
#15765=CARTESIAN_POINT ( 'NONE',  ( 9.864763540183249191, -5.217465845835395299, -7.827184855449096368 ) ) ;
#15768=CARTESIAN_POINT ( 'NONE',  ( 10.26492546752099955, -5.139081147506999514, -7.421078600323300023 ) ) ;
#15798=CARTESIAN_POINT ( 'NONE',  ( 9.605304848515999083, -2.836617618740000069, -8.031907719862799055 ) ) ;
#15818=CARTESIAN_POINT ( 'NONE',  ( 10.76841504065829902, -3.085489673376300424, -6.818119527508899935 ) ) ;
#15824=CARTESIAN_POINT ( 'NONE',  ( 9.810596873515665450, -4.629523725463621453, -6.407767014557176566 ) ) ;
#15871=CARTESIAN_POINT ( 'NONE',  ( 10.24255864497999902, -3.209241371122599773, -8.119307134446700047 ) ) ;
#15886=CARTESIAN_POINT ( 'NONE',  ( 11.27234208742519783, -4.554746427620499638, -8.372004648554700168 ) ) ;
#15973=CARTESIAN_POINT ( 'NONE',  ( 11.08810207955139937, -4.796537143354000499, -7.174999999999999822 ) ) ;
#15991=CARTESIAN_POINT ( 'NONE',  ( 9.383499245234512287, -5.249996043174973259, -7.336369100805424814 ) ) ;
#16002=CARTESIAN_POINT ( 'NONE',  ( 10.45672469555900008, -3.566534988568399900, -6.750062220519700062 ) ) ;
#16019=CARTESIAN_POINT ( 'NONE',  ( 11.57240408529958842, -4.732472998177641443, -7.017887023514779443 ) ) ;
#16026=ADVANCED_FACE ( 'NONE', ( #41087 ), #51234, .T. ) ;
#16037=CARTESIAN_POINT ( 'NONE',  ( 11.11302897915239818, -3.708003626182200030, -8.602736702002999891 ) ) ;
#16087=CARTESIAN_POINT ( 'NONE',  ( 10.84641504065830020, -3.195537720350400068, -6.900173947321999179 ) ) ;
#16106=CARTESIAN_POINT ( 'NONE',  ( 10.21225461470299933, -4.973404788313100511, -7.747639695388999215 ) ) ;
#16125=CARTESIAN_POINT ( 'NONE',  ( 11.18424042080583369, -3.455907502640803486, -6.342116603374312156 ) ) ;
#16137=CARTESIAN_POINT ( 'NONE',  ( 8.975960865537832234, -5.125960927305071024, -7.646523491995670163 ) ) ;
#16158=B_SPLINE_CURVE_WITH_KNOTS ( 'NONE', 3,
 ( #7135, #34063, #29168, #50476 ),
 .UNSPECIFIED., .F., .F.,
 ( 4, 4 ),
 ( 0.000000000000000000, 1.000000000000000000 ),
 .UNSPECIFIED. ) ;
#16160=CARTESIAN_POINT ( 'NONE',  ( 10.39918582084299992, -4.746348444722899629, -6.637298362509499228 ) ) ;
#16165=CARTESIAN_POINT ( 'NONE',  ( 10.69568717260499824, -4.466067913030199676, -8.260703168378098482 ) ) ;
#16166=CARTESIAN_POINT ( 'NONE',  ( 9.779346873515665450, -4.163624617374463988, -6.249999999999999112 ) ) ;
#16183=ORIENTED_EDGE ( 'NONE', *, *, #13990, .F. ) ;
#16216=CARTESIAN_POINT ( 'NONE',  ( 9.763317406968999634, -3.838745722419000028, -8.351883209406098629 ) ) ;
#16230=CARTESIAN_POINT ( 'NONE',  ( 10.48280513895999988, -3.096689368913399854, -6.997844089834400094 ) ) ;
#16288=VECTOR ( 'NONE', #3652, 1000.000000000000000 ) ;
#16308=CARTESIAN_POINT ( 'NONE',  ( 10.86301932002748138, -5.250000000000001776, -7.799851088612627770 ) ) ;
#16326=CARTESIAN_POINT ( 'NONE',  ( 11.59999999999999964, -4.883784007588900522, -7.825000000000000178 ) ) ;
#16341=ORIENTED_EDGE ( 'NONE', *, *, #12355, .F. ) ;
#16347=CARTESIAN_POINT ( 'NONE',  ( 10.32949413291699869, -3.087070836781100169, -7.083453279150199400 ) ) ;
#16351=CARTESIAN_POINT ( 'NONE',  ( 11.55300581613033906, -2.892415530317000272, -8.211208432468300344 ) ) ;
#16381=CARTESIAN_POINT ( 'NONE',  ( 10.59610807141099897, -3.947296672195129918, -8.639522915742999132 ) ) ;
#16386=CARTESIAN_POINT ( 'NONE',  ( 10.93210843320491499, -5.137688304401064165, -8.098394516494938244 ) ) ;
#16431=CARTESIAN_POINT ( 'NONE',  ( 11.33872066707849768, -3.141388196630700236, -6.980638253271099103 ) ) ;
#16447=CARTESIAN_POINT ( 'NONE',  ( 9.505051052051998184, -2.879444846832000415, -7.719295683256799379 ) ) ;
#16486=CARTESIAN_POINT ( 'NONE',  ( 9.114639751325487538, -2.815014287255568792, -7.959719964829115035 ) ) ;
#16501=CARTESIAN_POINT ( 'NONE',  ( 11.42887348028849992, -5.124210964533999935, -8.107837221875000111 ) ) ;
#16562=CARTESIAN_POINT ( 'NONE',  ( 9.280051052051998539, -3.014287398677499841, -7.692906630067099627 ) ) ;
#16576=CARTESIAN_POINT ( 'NONE',  ( 10.39969598649000027, -3.111999510220800236, -8.028730309000598808 ) ) ;
#16594=CARTESIAN_POINT ( 'NONE',  ( 10.34393020684899867, -5.250000000000000000, -7.500000000000000000 ) ) ;
#16651=CARTESIAN_POINT ( 'NONE',  ( 11.03482133862663517, -3.057020944820409536, -8.373613860257943742 ) ) ;
#16687=CARTESIAN_POINT ( 'NONE',  ( 10.79718447801629999, -2.996774412198000448, -7.477880487566260115 ) ) ;
#16691=CARTESIAN_POINT ( 'NONE',  ( 11.30878751119029957, -5.041025164610000608, -8.044634158732998586 ) ) ;
#16720=CARTESIAN_POINT ( 'NONE',  ( 10.49349279008999858, -4.332388355267299929, -8.734031750754999379 ) ) ;
#16742=CARTESIAN_POINT ( 'NONE',  ( 11.30367835872029936, -5.113555564477999305, -6.798177532456199934 ) ) ;
#16746=EDGE_CURVE ( 'NONE', #11095, #63961, #66082, .T. ) ;
#16768=CARTESIAN_POINT ( 'NONE',  ( 10.84226088462129844, -3.997572771977982775, -6.359261544073000039 ) ) ;
#16773=CARTESIAN_POINT ( 'NONE',  ( 11.59999999999999964, -4.817420948848700313, -7.174999999999999822 ) ) ;
#16786=CARTESIAN_POINT ( 'NONE',  ( 9.933633995697999097, -3.001718438313799808, -7.610798122400000310 ) ) ;
#16842=CARTESIAN_POINT ( 'NONE',  ( 10.12841772631199966, -3.509411006705700053, -8.509834072393999804 ) ) ;
#16851=CARTESIAN_POINT ( 'NONE',  ( 11.60000000000000142, -4.400439255161257002, -6.596661741119738132 ) ) ;
#16853=CARTESIAN_POINT ( 'NONE',  ( 11.68748876160954886, -4.600381688599499697, -8.124372018288600117 ) ) ;
#16899=CARTESIAN_POINT ( 'NONE',  ( 9.913279731609000223, -3.909869487835140323, -6.499640669006000238 ) ) ;
#16906=EDGE_CURVE ( 'NONE', #42489, #26585, #6757, .T. ) ;
#16912=CARTESIAN_POINT ( 'NONE',  ( 10.61257802013489737, -4.891884252872400474, -7.479237407015119743 ) ) ;
#16926=CARTESIAN_POINT ( 'NONE',  ( 10.88813259637009878, -5.155817667926999803, -8.129798612793599943 ) ) ;
#17031=CARTESIAN_POINT ( 'NONE',  ( 11.40841235500449891, -4.841138636481000290, -6.729431436870699557 ) ) ;
#17036=CARTESIAN_POINT ( 'NONE',  ( 11.05946005378019947, -2.963614890480000152, -6.946587256304699309 ) ) ;
#17065=CARTESIAN_POINT ( 'NONE',  ( 11.45348876160960039, -4.885820101980599794, -8.421216112044099589 ) ) ;
#17101=CARTESIAN_POINT ( 'NONE',  ( 10.14393020684899938, -2.750000000000000000, -7.500000000000000000 ) ) ;
#17116=CARTESIAN_POINT ( 'NONE',  ( 10.13662282008599824, -3.405288783432600219, -8.459250300176799797 ) ) ;
#17134=CARTESIAN_POINT ( 'NONE',  ( 9.327747021775998348, -4.858221690000700477, -8.253120162257399528 ) ) ;
#17152=CARTESIAN_POINT ( 'NONE',  ( 10.65364694612719809, -4.804498860841600383, -7.821061011719899980 ) ) ;
#17188=CARTESIAN_POINT ( 'NONE',  ( 10.56733863405299800, -3.211524470605299886, -8.505794571537999005 ) ) ;
#17201=CARTESIAN_POINT ( 'NONE',  ( 11.83518044953559922, -3.231951024059400268, -7.900497508315099893 ) ) ;
#17254=CARTESIAN_POINT ( 'NONE',  ( 9.077417874593999514, -4.924352284713100047, -7.892956936667999912 ) ) ;
#17269=CARTESIAN_POINT ( 'NONE',  ( 11.18923293495519822, -5.032672437899000428, -7.458486839450950256 ) ) ;
#17311=CARTESIAN_POINT ( 'NONE',  ( 10.11496314287999887, -2.748296264808000267, -7.236139910592400248 ) ) ;
#17386=CARTESIAN_POINT ( 'NONE',  ( 10.67410807141119911, -3.953638752893899877, -8.502397868920999358 ) ) ;
#17390=CARTESIAN_POINT ( 'NONE',  ( 11.01279632507519857, -3.375091146194399983, -8.658468685623999406 ) ) ;
#17417=VERTEX_POINT ( 'NONE', #50141 ) ;
#17422=CARTESIAN_POINT ( 'NONE',  ( 10.61656919669529842, -2.774362666861999838, -7.862118085997298778 ) ) ;
#17477=CARTESIAN_POINT ( 'NONE',  ( 10.47303166480599934, -5.137916160623999140, -7.580230465881790280 ) ) ;
#17481=VECTOR ( 'NONE', #38699, 1000.000000000000114 ) ;
#17482=CARTESIAN_POINT ( 'NONE',  ( 11.60000000000000142, -4.549997407263328242, -8.379764693824251154 ) ) ;
#17494=CARTESIAN_POINT ( 'NONE',  ( 10.36422949779699820, -3.442773960835399993, -8.335668797826500054 ) ) ;
#17504=VERTEX_POINT ( 'NONE', #62676 ) ;
#17511=CARTESIAN_POINT ( 'NONE',  ( 10.33364828895399867, -3.239803852721999888, -7.915211961479200475 ) ) ;
#17518=CARTESIAN_POINT ( 'NONE',  ( 11.03443712336079940, -2.942831166283299105, -7.175021320887989162 ) ) ;
#17534=COLOUR_RGB ( '', 0.72549020, 0.75294118, 0.79215686) ;
#17546=VECTOR ( 'NONE', #56127, 1000.000000000000000 ) ;
#17548=CARTESIAN_POINT ( 'NONE',  ( 10.05862282008599884, -3.333723918618700210, -8.574682153725998290 ) ) ;
#17612=CARTESIAN_POINT ( 'NONE',  ( 9.963938025973998691, -4.522194782554399772, -6.642005297568199573 ) ) ;
#17642=CARTESIAN_POINT ( 'NONE',  ( 11.76588784977539781, -5.120865761890000201, -7.435950347916509884 ) ) ;
#17659=AXIS2_PLACEMENT_3D ( 'NONE', #19171, #45751, #40495 ) ;
#17677=CARTESIAN_POINT ( 'NONE',  ( 11.00000000000000000, -3.008232475376599879, -7.174999999999999822 ) ) ;
#17701=CARTESIAN_POINT ( 'NONE',  ( 11.16486084871730000, -2.792989229543000107, -7.174999999999999822 ) ) ;
#17727=LINE ( 'NONE', #39050, #17481 ) ;
#17747=CARTESIAN_POINT ( 'NONE',  ( 11.26212378248529866, -4.615095948180499619, -6.336291382830999908 ) ) ;
#17777=CARTESIAN_POINT ( 'NONE',  ( 11.35502763632549872, -5.160433036184000066, -6.964545474268299508 ) ) ;
#17829=CARTESIAN_POINT ( 'NONE',  ( 10.17764828895399809, -2.998858038575999974, -8.046814291299300592 ) ) ;
#17843=EDGE_CURVE ( 'NONE', #44736, #3420, #53843, .T. ) ;
#17846=CARTESIAN_POINT ( 'NONE',  ( 10.13425461470299993, -4.840245908677600184, -7.713763321667399531 ) ) ;
#17863=CARTESIAN_POINT ( 'NONE',  ( 11.44133594839949986, -3.430493414882899827, -6.847343244997600387 ) ) ;
#17865=B_SPLINE_CURVE_WITH_KNOTS ( 'NONE', 3,
 ( #37772, #6292, #15765, #38111, #10512, #21349, #48614, #5269, #21685, #59437, #59785, #58750, #48958, #32202, #717, #47928, #369, #11199 ),
 .UNSPECIFIED., .F., .F.,
 ( 4, 2, 2, 2, 2, 2, 2, 2, 4 ),
 ( 0.000000000000000000, 0.1250000000000000000, 0.2500000000000000000, 0.3750000000000000000, 0.5000000000000000000, 0.6250000000000000000, 0.7500000000000000000, 0.8750000000000000000, 1.000000000000000000 ),
 .UNSPECIFIED. ) ;
#17876=CARTESIAN_POINT ( 'NONE',  ( 10.31021345716899873, -3.363461959113699606, -8.078719053813800954 ) ) ;
#17917=CARTESIAN_POINT ( 'NONE',  ( 8.599999952505998024, -4.749999993641800700, -7.500000000000000000 ) ) ;
#17952=CARTESIAN_POINT ( 'NONE',  ( 10.64393020684969926, -2.750000000000000000, -7.500000000000000000 ) ) ;
#17959=CARTESIAN_POINT ( 'NONE',  ( 10.18144474310099845, -2.984290294633999974, -7.992914665944799602 ) ) ;
#17963=CARTESIAN_POINT ( 'NONE',  ( 8.849999778957998942, -4.000000000000000000, -8.499999833805500060 ) ) ;
#17978=FILL_AREA_STYLE ('',( #44562 ) ) ;
#18080=CARTESIAN_POINT ( 'NONE',  ( 8.751496707488000126, -3.918323994020610268, -8.356402621895700378 ) ) ;
#18088=CARTESIAN_POINT ( 'NONE',  ( 11.40211496860029783, -3.206052520092899982, -7.093139000852099585 ) ) ;
#18120=CARTESIAN_POINT ( 'NONE',  ( 10.98579841651039857, -4.449968941611500028, -8.696179055230999211 ) ) ;
#18170=CARTESIAN_POINT ( 'NONE',  ( 11.29364426047339975, -3.533902447304699823, -8.230103870496201068 ) ) ;
#18171=CARTESIAN_POINT ( 'NONE',  ( 11.13764426047339917, -3.386171819220400003, -8.461511872390000022 ) ) ;
#18186=CARTESIAN_POINT ( 'NONE',  ( 9.477709346417000802, -3.092687088662700035, -7.069157126958599768 ) ) ;
#18203=CARTESIAN_POINT ( 'NONE',  ( 11.78594988689359901, -3.606563555963900214, -8.271690446953899212 ) ) ;
#18240=CARTESIAN_POINT ( 'NONE',  ( 10.93656785386839836, -5.060279460151999587, -8.213529149347399638 ) ) ;
#18295=CARTESIAN_POINT ( 'NONE',  ( 10.81059687351629961, -4.629523725463621453, -6.407767014557176566 ) ) ;
#18301=CARTESIAN_POINT ( 'NONE',  ( 8.898101285863999621, -4.735211557675400584, -6.626387721327399838 ) ) ;
#18302=CARTESIAN_POINT ( 'NONE',  ( 9.666846873516664829, -3.231816600031351516, -6.500416447002278275 ) ) ;
#18328=CARTESIAN_POINT ( 'NONE',  ( 10.76346886766499900, -4.634677072395899877, -6.346853961441000003 ) ) ;
#18341=DIRECTION ( 'NONE',  ( 1.000000000000000000, 0.000000000000000000, 0.000000000000000000 ) ) ;
#18356=CARTESIAN_POINT ( 'NONE',  ( 10.36825461470400001, -5.239722547583999912, -7.815392442832299835 ) ) ;
#18407=ORIENTED_EDGE ( 'NONE', *, *, #13974, .F. ) ;
#18430=CARTESIAN_POINT ( 'NONE',  ( 10.00551210286899995, -4.217228369037729685, -8.756187319522087620 ) ) ;
#18435=CARTESIAN_POINT ( 'NONE',  ( 11.59603632436369125, -4.842640371965599932, -7.303218851299499548 ) ) ;
#18464=CARTESIAN_POINT ( 'NONE',  ( 9.843930206850000530, -5.250000000000000000, -7.500000000000000000 ) ) ;
#18467=CARTESIAN_POINT ( 'NONE',  ( 10.19391290906799874, -4.548591194283900130, -8.171383386399000415 ) ) ;
#18483=CARTESIAN_POINT ( 'NONE',  ( 10.93479632507519916, -3.442212747724900268, -8.534037301706000278 ) ) ;
#18519=CARTESIAN_POINT ( 'NONE',  ( 10.78887616594230003, -4.386455737425299262, -6.281817606595999415 ) ) ;
#18532=CARTESIAN_POINT ( 'NONE',  ( 10.26090035061499961, -3.768906505327899836, -8.335645555860798694 ) ) ;
#18550=CARTESIAN_POINT ( 'NONE',  ( 11.09672200990539892, -4.817867935977999672, -7.214709569664399247 ) ) ;
#18586=CARTESIAN_POINT ( 'NONE',  ( 10.37041638348499895, -5.241705141469999774, -7.197535585171899619 ) ) ;
#18600=CARTESIAN_POINT ( 'NONE',  ( 11.65871932425156920, -4.147141405561299621, -8.492622906483498824 ) ) ;
#18644=CARTESIAN_POINT ( 'NONE',  ( 8.872772138681998655, -4.424886761933599644, -6.440186012775000357 ) ) ;
#18659=CARTESIAN_POINT ( 'NONE',  ( 10.44601354018326944, -4.999583552997726166, -8.268183399968640046 ) ) ;
#18671=CARTESIAN_POINT ( 'NONE',  ( 11.56322412107030928, -3.945399343424460525, -6.467939235001000320 ) ) ;
#18698=CARTESIAN_POINT ( 'NONE',  ( 9.962988259787000089, -4.167373623506299474, -8.768215461831999846 ) ) ;
#18725=FACE_OUTER_BOUND ( 'NONE', #48647, .T. ) ;
#18779=CARTESIAN_POINT ( 'NONE',  ( 10.81524174883999834, -4.028418853626810403, -8.533115712456000423 ) ) ;
#18830=CARTESIAN_POINT ( 'NONE',  ( 11.52166954483529793, -3.437903757373499847, -6.632714178206799538 ) ) ;
#18859=CARTESIAN_POINT ( 'NONE',  ( 11.39210538575740017, -3.157545584346100220, -7.298582155985900322 ) ) ;
#18860=CARTESIAN_POINT ( 'NONE',  ( 10.96118313518939935, -4.792748567750200195, -8.502430091786999711 ) ) ;
#18872=CARTESIAN_POINT ( 'NONE',  ( 11.37077408945316925, -5.183263708087437749, -7.913130250469239790 ) ) ;
#18877=CARTESIAN_POINT ( 'NONE',  ( 9.376392757686998536, -3.322036695224600322, -8.241085728986799808 ) ) ;
#18895=CARTESIAN_POINT ( 'NONE',  ( 11.16641369783139837, -4.050626550392200542, -8.502191501283999031 ) ) ;
#18940=CARTESIAN_POINT ( 'NONE',  ( 10.94903032197929882, -3.496160833528699996, -6.795411691360399686 ) ) ;
#18983=CARTESIAN_POINT ( 'NONE',  ( 9.100734463322998735, -3.881063085044400118, -8.635600483553998785 ) ) ;
#19010=CARTESIAN_POINT ( 'NONE',  ( 11.14767835872009982, -4.874341053673500568, -6.948943352864199952 ) ) ;
#19020=DIRECTION ( 'NONE',  ( 0.000000000000000000, 0.000000000000000000, 1.000000000000000000 ) ) ;
#19032=CARTESIAN_POINT ( 'NONE',  ( 9.583051052052001140, -2.744602294987000146, -7.745684736446600382 ) ) ;
#19109=CARTESIAN_POINT ( 'NONE',  ( 11.18923293495519822, -5.032672437899000428, -7.458486839450950256 ) ) ;
#19125=CARTESIAN_POINT ( 'NONE',  ( 11.00000000000000000, -2.920245322398999921, -7.825000000000000178 ) ) ;
#19144=CARTESIAN_POINT ( 'NONE',  ( 9.383380199233998908, -3.139757597894699881, -7.391875284387199763 ) ) ;
#19159=CARTESIAN_POINT ( 'NONE',  ( 10.68546886766499959, -4.566506264294200257, -6.470713638631999665 ) ) ;
#19171=CARTESIAN_POINT ( 'NONE',  ( 11.59999999999999964, -4.000000000000000000, -7.500000000000000000 ) ) ;
#19191=CARTESIAN_POINT ( 'NONE',  ( 11.28118179236249929, -4.267047616085000605, -6.250199235344999771 ) ) ;
#19208=CARTESIAN_POINT ( 'NONE',  ( 8.844480666858999030, -3.665111009453500213, -8.446938520915798776 ) ) ;
#19224=CARTESIAN_POINT ( 'NONE',  ( 10.57564694612699974, -4.931992688388300294, -7.871941502982999772 ) ) ;
#19269=CARTESIAN_POINT ( 'NONE',  ( 9.150912690312626552, -4.805207160112336950, -7.842306439064141266 ) ) ;
#19274=CARTESIAN_POINT ( 'NONE',  ( 10.65364694612719809, -4.804498860841600383, -7.821061011719899980 ) ) ;
#19287=ORIENTED_EDGE ( 'NONE', *, *, #35371, .T. ) ;
#19319=CARTESIAN_POINT ( 'NONE',  ( 9.860608878791998322, -4.258572737033900601, -6.387851364408000165 ) ) ;
#19351=CARTESIAN_POINT ( 'NONE',  ( 10.73213259636989925, -4.907524392912299582, -7.994504989494399361 ) ) ;
#19361=PRESENTATION_STYLE_ASSIGNMENT (( #23234 ) ) ;
#19376=CARTESIAN_POINT ( 'NONE',  ( 9.025809814041000578, -3.217492037304399588, -8.511961036725999463 ) ) ;
#19448=DIRECTION ( 'NONE',  ( -1.000000000000000000, 0.000000000000000000, 0.000000000000000000 ) ) ;
#19455=CARTESIAN_POINT ( 'NONE',  ( 11.60477869730532774, -4.467447516829900600, -6.578238193496799724 ) ) ;
#19468=CARTESIAN_POINT ( 'NONE',  ( 11.45284386393252696, -3.097320422761385750, -7.175013233162909287 ) ) ;
#19490=CARTESIAN_POINT ( 'NONE',  ( 10.17349413291699811, -2.837298848764000514, -6.969488574374499201 ) ) ;
#19495=CARTESIAN_POINT ( 'NONE',  ( 9.636671671056999955, -4.855035690642299784, -7.643603315539799326 ) ) ;
#19508=CARTESIAN_POINT ( 'NONE',  ( 11.13746005378019888, -2.838900981960999825, -6.879992063401499713 ) ) ;
#19540=CARTESIAN_POINT ( 'NONE',  ( 11.24441369783139777, -4.043700988887960257, -8.365094684940499903 ) ) ;
#19541=CARTESIAN_POINT ( 'NONE',  ( 10.46887750876899936, -4.692271380433699512, -8.574279626736998949 ) ) ;
#19578=CARTESIAN_POINT ( 'NONE',  ( 11.41256651104150066, -3.901000349726440053, -6.501426055769400136 ) ) ;
#19620=CARTESIAN_POINT ( 'NONE',  ( 9.936116252963625328, -3.418844976054905782, -6.845942581217610012 ) ) ;
#19622=B_SPLINE_CURVE_WITH_KNOTS ( 'NONE', 3,
 ( #26562, #15380, #30771, #20275 ),
 .UNSPECIFIED., .F., .F.,
 ( 4, 4 ),
 ( 0.000000000000000000, 1.000000000000000000 ),
 .UNSPECIFIED. ) ;
#19626=CARTESIAN_POINT ( 'NONE',  ( 11.04749144726329924, -4.500836215462999945, -6.793273974143599681 ) ) ;
#19673=CARTESIAN_POINT ( 'NONE',  ( 9.936596320338999533, -5.057167065956000407, -7.068569539041399175 ) ) ;
#19702=CARTESIAN_POINT ( 'NONE',  ( 11.10101463001529964, -3.377766160221900016, -6.503413421344399481 ) ) ;
#19757=ORIENTED_EDGE ( 'NONE', *, *, #55663, .T. ) ;
#19802=ORIENTED_EDGE ( 'NONE', *, *, #1845, .F. ) ;
#19815=CARTESIAN_POINT ( 'NONE',  ( 8.751496707488000126, -3.918323994020610268, -8.356402621895700378 ) ) ;
#19881=CARTESIAN_POINT ( 'NONE',  ( 11.02287616594229824, -4.261927842557799551, -6.674353346984900348 ) ) ;
#19882=CARTESIAN_POINT ( 'NONE',  ( 10.29657053952199952, -4.502253688815499366, -6.324815923923999605 ) ) ;
#19897=CARTESIAN_POINT ( 'NONE',  ( 11.43114108301961451, -3.379311755690166841, -6.880598518631704685 ) ) ;
#19898=ORIENTED_EDGE ( 'NONE', *, *, #43714, .F. ) ;
#19900=CARTESIAN_POINT ( 'NONE',  ( 9.779646554150998483, -3.580250267348600079, -8.258629096756299859 ) ) ;
#19918=CARTESIAN_POINT ( 'NONE',  ( 11.31410538575739899, -3.024036709177600368, -7.266662245194900116 ) ) ;
#19959=CARTESIAN_POINT ( 'NONE',  ( 9.150818738817875442, -3.048937241343601112, -6.673278530809400699 ) ) ;
#19966=CARTESIAN_POINT ( 'NONE',  ( 9.885457958598628636, -3.143868186573851364, -7.319526769407151079 ) ) ;
#19971=CARTESIAN_POINT ( 'NONE',  ( 10.57980110216399972, -4.739241740354600552, -7.048535450274799885 ) ) ;
#20017=CARTESIAN_POINT ( 'NONE',  ( 9.098721904869998767, -2.884547197234000215, -8.126218358304999612 ) ) ;
#20041=CARTESIAN_POINT ( 'NONE',  ( 10.60746886766490071, -4.498335456194499926, -6.594573315824700188 ) ) ;
#20042=CARTESIAN_POINT ( 'NONE',  ( 11.60000000000000142, -3.812684744683584981, -6.446733142248666226 ) ) ;
#20070=ORIENTED_EDGE ( 'NONE', *, *, #47854, .T. ) ;
#20177=EDGE_CURVE ( 'NONE', #43301, #42419, #61773, .T. ) ;
#20192=DIRECTION ( 'NONE',  ( 0.000000000000000000, 1.000000000000000000, 0.000000000000000000 ) ) ;
#20218=CARTESIAN_POINT ( 'NONE',  ( 10.72749279009019929, -4.225282629687599822, -8.336388861178200216 ) ) ;
#20257=CARTESIAN_POINT ( 'NONE',  ( 11.28949010443639978, -2.999324937259999935, -7.574834962826040297 ) ) ;
#20270=LINE ( 'NONE', #30428, #31062 ) ;
#20275=CARTESIAN_POINT ( 'NONE',  ( 10.59393020684899867, -2.750000000000000000, -7.500000000000000000 ) ) ;
#20303=CARTESIAN_POINT ( 'NONE',  ( 9.682824781140627834, -4.607703288839251954, -8.129467220476902511 ) ) ;
#20307=CARTESIAN_POINT ( 'NONE',  ( 11.62994988689359843, -3.481863023525599843, -8.516279404258998653 ) ) ;
#20338=CARTESIAN_POINT ( 'NONE',  ( 11.20158531382784162, -3.727547057523674212, -6.250000000000000000 ) ) ;
#20357=CARTESIAN_POINT ( 'NONE',  ( 8.642797255587998606, -2.721932483203000075, -7.445890648716809501 ) ) ;
#20375=ORIENTED_EDGE ( 'NONE', *, *, #13974, .T. ) ;
#20383=CARTESIAN_POINT ( 'NONE',  ( 11.15278751119019773, -4.790480620979200133, -7.913556523549700294 ) ) ;
#20466=VECTOR ( 'NONE', #56678, 1000.000000000000000 ) ;
#20489=CARTESIAN_POINT ( 'NONE',  ( 11.32240614981507676, -3.267563509902000174, -7.982093918858203629 ) ) ;
#20505=CARTESIAN_POINT ( 'NONE',  ( 11.16486084871730000, -2.792989229543000107, -7.174999999999999822 ) ) ;
#20553=CARTESIAN_POINT ( 'NONE',  ( 9.164757945270768147, -2.782574339883950199, -7.172825509854745540 ) ) ;
#20556=ORIENTED_EDGE ( 'NONE', *, *, #48532, .T. ) ;
#20562=CARTESIAN_POINT ( 'NONE',  ( 10.82595391537419971, -3.283439621430300104, -7.986661909549199301 ) ) ;
#20581=CARTESIAN_POINT ( 'NONE',  ( 8.842468108405999061, -3.165798890946399879, -7.736255015838599647 ) ) ;
#20602=CARTESIAN_POINT ( 'NONE',  ( 10.57149279008999798, -4.296686446741600385, -8.601484120896000007 ) ) ;
#20642=CARTESIAN_POINT ( 'NONE',  ( 9.262620115046999558, -4.656877754660387225, -6.424592926396654136 ) ) ;
#20649=CARTESIAN_POINT ( 'NONE',  ( 9.480191603681626944, -3.849750744317739670, -6.638050216028796413 ) ) ;
#20653=CARTESIAN_POINT ( 'NONE',  ( 11.21564426047340035, -3.460037133261700149, -8.345807871442598724 ) ) ;
#20669=CARTESIAN_POINT ( 'NONE',  ( 9.834329965421998665, -4.793057006135000186, -8.321459087847200564 ) ) ;
#20701=CARTESIAN_POINT ( 'NONE',  ( 8.744113844317999096, -3.676949563211899807, -6.262250912840999106 ) ) ;
#20722=CARTESIAN_POINT ( 'NONE',  ( 10.30072469555899950, -3.429147315060100176, -6.512367818249299667 ) ) ;
#20728=CARTESIAN_POINT ( 'NONE',  ( 10.29399293566599916, -3.453258297007899991, -8.170700474995699736 ) ) ;
#20778=CARTESIAN_POINT ( 'NONE',  ( 8.733265421555000074, -4.162714371335800578, -8.341695632489900092 ) ) ;
#20794=CARTESIAN_POINT ( 'NONE',  ( 10.72702344389999851, -5.004394439171999664, -6.890449684422599752 ) ) ;
#20808=CARTESIAN_POINT ( 'NONE',  ( 9.573096873516668381, -2.782534154164605589, -7.827184855449103473 ) ) ;
#20826=CARTESIAN_POINT ( 'NONE',  ( 9.446013540182333301, -4.999583552997726166, -8.268183399968640046 ) ) ;
#20880=CARTESIAN_POINT ( 'NONE',  ( 10.84606641549978256, -3.161700962939955506, -7.747677868960886727 ) ) ;
#20908=CARTESIAN_POINT ( 'NONE',  ( 10.28441772631199846, -3.627481539113199815, -8.266796319406900295 ) ) ;
#20930=CARTESIAN_POINT ( 'NONE',  ( 9.577013376692997682, -4.772923352651200268, -7.107192877568799361 ) ) ;
#20947=CARTESIAN_POINT ( 'NONE',  ( 8.789886373836322875, -3.999992178805580334, -8.439846342473931173 ) ) ;
#20950=CARTESIAN_POINT ( 'NONE',  ( 10.39918582084299992, -4.746348444722899629, -6.637298362509499228 ) ) ;
#20972=EDGE_LOOP ( 'NONE', ( #12900, #48079 ) ) ;
#20999=CARTESIAN_POINT ( 'NONE',  ( 10.62487750876920067, -4.543557328885200697, -8.343502390669698343 ) ) ;
#21006=CARTESIAN_POINT ( 'NONE',  ( 10.37309687351658383, -5.217465845835394411, -7.172815144550898303 ) ) ;
#21014=CARTESIAN_POINT ( 'NONE',  ( 10.29025461470400060, -5.106563667948999630, -7.781516069110699263 ) ) ;
#21046=CARTESIAN_POINT ( 'NONE',  ( 9.124051052051999733, -2.744602294987000146, -7.745684736446600382 ) ) ;
#21060=CARTESIAN_POINT ( 'NONE',  ( 11.15221028326116048, -4.908903471848705458, -7.175011397899978327 ) ) ;
#21067=CARTESIAN_POINT ( 'NONE',  ( 10.20226357027499908, -2.879914860223000250, -7.716099591766099053 ) ) ;
#21073=CARTESIAN_POINT ( 'NONE',  ( 11.11123293495519881, -4.891405920092699589, -7.464165716332529676 ) ) ;
#21085=EDGE_LOOP ( 'NONE', ( #64491, #41170, #61189, #20556, #3739, #60291, #3298, #3031, #23702, #10333, #12843 ) ) ;
#21125=CARTESIAN_POINT ( 'NONE',  ( 9.358051052051999719, -3.149129950522900234, -7.666517576877299511 ) ) ;
#21141=CARTESIAN_POINT ( 'NONE',  ( 10.56591429142999949, -3.980313504646230349, -6.466681092390999197 ) ) ;
#21178=LINE ( 'NONE', #37261, #64992 ) ;
#21208=EDGE_CURVE ( 'NONE', #47368, #54348, #43328, .T. ) ;
#21222=CARTESIAN_POINT ( 'NONE',  ( 10.91991225946278199, -3.299232917623651229, -6.977491532540834207 ) ) ;
#21242=CARTESIAN_POINT ( 'NONE',  ( 11.52285868696541726, -3.940189611494480992, -8.771870505746530711 ) ) ;
#21251=CARTESIAN_POINT ( 'NONE',  ( 11.65871932425156920, -4.147141405561299621, -8.492622906483498824 ) ) ;
#21287=CARTESIAN_POINT ( 'NONE',  ( 11.53148876160955005, -4.790673964186999534, -8.322268080792200706 ) ) ;
#21336=CARTESIAN_POINT ( 'NONE',  ( 10.89564560330029863, -3.692495237344800341, -6.544808043482999160 ) ) ;
#21347=EDGE_CURVE ( 'NONE', #11095, #54418, #48267, .T. ) ;
#21349=CARTESIAN_POINT ( 'NONE',  ( 9.916846873516377059, -4.768183399968644487, -8.499583552997725278 ) ) ;
#21352=CARTESIAN_POINT ( 'NONE',  ( 10.03696314287999947, -2.882742046518000034, -7.264481182560499128 ) ) ;
#21378=CARTESIAN_POINT ( 'NONE',  ( 9.002376473208929752, -4.922128563344212893, -8.207577963560542145 ) ) ;
#21383=CARTESIAN_POINT ( 'NONE',  ( 9.529317406968999649, -3.762080884004200154, -8.756892549790999070 ) ) ;
#21401=CARTESIAN_POINT ( 'NONE',  ( 10.81764560330029923, -3.650429500487800460, -6.414140625063999401 ) ) ;
#21407=CARTESIAN_POINT ( 'NONE',  ( 11.59999999999999964, -5.499854772664000357, -7.825000000000000178 ) ) ;
#21436=FACE_OUTER_BOUND ( 'NONE', #22353, .T. ) ;
#21447=CARTESIAN_POINT ( 'NONE',  ( 10.50595525820100029, -4.081787880721680750, -6.637672143048099827 ) ) ;
#21458=CARTESIAN_POINT ( 'NONE',  ( 9.484696787962999309, -3.851113559088000127, -6.645868410478299459 ) ) ;
#21473=CARTESIAN_POINT ( 'NONE',  ( 11.44366954483529852, -3.514796851401900124, -6.751356298874699569 ) ) ;
#21587=CARTESIAN_POINT ( 'NONE',  ( 10.84641504065830020, -3.195537720350400068, -6.900173947321999179 ) ) ;
#21623=CARTESIAN_POINT ( 'NONE',  ( 10.89149144726329865, -4.659577337894599935, -6.569275630703699242 ) ) ;
#21666=CARTESIAN_POINT ( 'NONE',  ( 8.796304629759626792, -3.464785522094639969, -8.192154231972200051 ) ) ;
#21670=CARTESIAN_POINT ( 'NONE',  ( 10.37872469555899890, -3.497841151814999883, -6.631215019384099740 ) ) ;
#21685=CARTESIAN_POINT ( 'NONE',  ( 9.958513540182876156, -4.163624617374470205, -8.749999999999998224 ) ) ;
#21689=CARTESIAN_POINT ( 'NONE',  ( 10.08560887879199797, -4.227457260387500249, -6.521682313853199631 ) ) ;
#21712=DIRECTION ( 'NONE',  ( 0.000000000000000000, -1.000000000000000000, 0.000000000000000000 ) ) ;
#21741=CARTESIAN_POINT ( 'NONE',  ( 11.47810404293059960, -4.563346034752700398, -8.647151967355000579 ) ) ;
#21747=CARTESIAN_POINT ( 'NONE',  ( 11.44366954483529852, -3.514796851401900124, -6.751356298874699569 ) ) ;
#21801=CARTESIAN_POINT ( 'NONE',  ( 9.659988259785999176, -4.131418345883800747, -8.495776841814999258 ) ) ;
#21816=CARTESIAN_POINT ( 'NONE',  ( 11.52677869730533011, -4.403502086956500250, -6.704332466833498927 ) ) ;
#21848=CARTESIAN_POINT ( 'NONE',  ( 11.11486084871780022, -2.792989229543000107, -7.174999999999999822 ) ) ;
#21931=CARTESIAN_POINT ( 'NONE',  ( 11.50687348028854906, -5.003459210197000573, -8.042549288197099244 ) ) ;
#21935=CARTESIAN_POINT ( 'NONE',  ( 11.09590547754519996, -2.684394667508000154, -7.541753805330609239 ) ) ;
#21967=CARTESIAN_POINT ( 'NONE',  ( 10.32533997688000049, -3.756890902898200046, -6.385465081946999355 ) ) ;
#21988=CARTESIAN_POINT ( 'NONE',  ( 11.34523293495530005, -5.315205473512000012, -7.447129085684729866 ) ) ;
#22017=CARTESIAN_POINT ( 'NONE',  ( 11.30995122972050027, -3.547233695387300045, -6.452959986593999275 ) ) ;
#22021=CARTESIAN_POINT ( 'NONE',  ( 11.59999999999999787, -4.831023649631404737, -7.997379651729213279 ) ) ;
#22032=CARTESIAN_POINT ( 'NONE',  ( 9.555709346417000205, -2.968569381205999669, -7.010219103474399915 ) ) ;
#22075=CARTESIAN_POINT ( 'NONE',  ( 10.31021345716899873, -3.363461959113699606, -8.078719053813800954 ) ) ;
#22087=CARTESIAN_POINT ( 'NONE',  ( 10.98995257254739855, -5.095356924909000718, -7.818564472783199548 ) ) ;
#22149=CARTESIAN_POINT ( 'NONE',  ( 8.849455549952999434, -3.218304396998100003, -6.869290649434700136 ) ) ;
#22163=CARTESIAN_POINT ( 'NONE',  ( 11.14767835872009982, -4.874341053673500568, -6.948943352864199952 ) ) ;
#22171=FACE_OUTER_BOUND ( 'NONE', #54599, .T. ) ;
#22178=CARTESIAN_POINT ( 'NONE',  ( 11.51145123989532948, -3.394760891061399999, -8.668865425277999748 ) ) ;
#22272=DIRECTION ( 'NONE',  ( -1.000000000000000000, 0.000000000000000000, 0.000000000000000000 ) ) ;
#22282=CARTESIAN_POINT ( 'NONE',  ( 10.60026222744819790, -4.774534945026900346, -8.138001937130599828 ) ) ;
#22286=CARTESIAN_POINT ( 'NONE',  ( 10.55569598648999907, -2.869047858956000230, -8.173387776112500447 ) ) ;
#22314=CARTESIAN_POINT ( 'NONE',  ( 11.03502897915239878, -3.672866099873000056, -8.735435061820998826 ) ) ;
#22353=EDGE_LOOP ( 'NONE', ( #11593, #19757, #30804 ) ) ;
#22355=CARTESIAN_POINT ( 'NONE',  ( 9.333766445374624965, -5.249999999999997335, -7.340348008080749054 ) ) ;
#22367=CARTESIAN_POINT ( 'NONE',  ( 10.37457053952199892, -4.448306506338299826, -6.451042711717000167 ) ) ;
#22381=CARTESIAN_POINT ( 'NONE',  ( 10.41488779216199845, -3.070969952137800441, -7.835030859477799758 ) ) ;
#22389=EDGE_CURVE ( 'NONE', #54418, #54024, #31954, .T. ) ;
#22391=CARTESIAN_POINT ( 'NONE',  ( 8.807788144226000426, -3.909067355573210278, -8.453461841935100196 ) ) ;
#22427=CARTESIAN_POINT ( 'NONE',  ( 11.08810207955139937, -4.796537143354000499, -7.174999999999999822 ) ) ;
#22432=CARTESIAN_POINT ( 'NONE',  ( 10.44426222744799837, -4.986443098259000450, -8.312555471636301263 ) ) ;
#22437=CARTESIAN_POINT ( 'NONE',  ( 8.755358248830999557, -3.910012670022149806, -8.350279134800100422 ) ) ;
#22443=CARTESIAN_POINT ( 'NONE',  ( 11.56441235500451015, -4.638700978900200056, -6.914884925939399629 ) ) ;
#22474=EDGE_CURVE ( 'NONE', #32857, #47524, #46932, .T. ) ;
#22491=CARTESIAN_POINT ( 'NONE',  ( 8.798797255587999189, -2.996487526130999779, -7.457514444071209780 ) ) ;
#22492=CARTESIAN_POINT ( 'NONE',  ( 9.593930206849998754, -2.750000000000000000, -7.500000000000000000 ) ) ;
#22504=CARTESIAN_POINT ( 'NONE',  ( 10.28014141025500017, -3.582647672488299850, -8.243346240911998635 ) ) ;
#22522=CARTESIAN_POINT ( 'NONE',  ( 10.22934687351566829, -4.163624617374463099, -6.249999999999998224 ) ) ;
#22547=CARTESIAN_POINT ( 'NONE',  ( 10.56244474310100045, -2.862064370975999861, -8.052229793103100164 ) ) ;
#22581=DIRECTION ( 'NONE',  ( 1.000000000000000000, 0.000000000000000000, 0.000000000000000000 ) ) ;
#22595=CARTESIAN_POINT ( 'NONE',  ( 10.37837607040047594, -3.132032243413395367, -7.396454632467190926 ) ) ;
#22622=CARTESIAN_POINT ( 'NONE',  ( 10.62487750876920067, -4.543557328885200697, -8.343502390669698343 ) ) ;
#22626=CARTESIAN_POINT ( 'NONE',  ( 11.34523293495530005, -5.315205473512000012, -7.447129085684729866 ) ) ;
#22656=CARTESIAN_POINT ( 'NONE',  ( 10.91195257254739914, -5.227167235646000165, -7.856899084262298771 ) ) ;
#22666=EDGE_LOOP ( 'NONE', ( #8591, #27454, #16341, #55726, #20070, #4254, #344, #50599, #63801, #35462 ) ) ;
#22680=CARTESIAN_POINT ( 'NONE',  ( 11.42834208742529967, -4.706521750018099581, -8.610579932818998472 ) ) ;
#22683=CARTESIAN_POINT ( 'NONE',  ( 9.048601287889788125, -3.999999532294070459, -8.698595322193611423 ) ) ;
#22709=CARTESIAN_POINT ( 'NONE',  ( 11.06379841651039797, -4.401637675674300532, -8.567697191971999970 ) ) ;
#22726=CARTESIAN_POINT ( 'NONE',  ( 9.201101285863998669, -4.735211557675400584, -6.626387721327399838 ) ) ;
#22742=CARTESIAN_POINT ( 'NONE',  ( 10.99826088462129903, -3.998156935320088756, -6.633804182961699603 ) ) ;
#22754=CARTESIAN_POINT ( 'NONE',  ( 9.041999884715581359, -4.156896875802718050, -8.691999950321772417 ) ) ;
#22759=CARTESIAN_POINT ( 'NONE',  ( 10.84393020684979980, -5.250000000000000000, -7.500000000000000000 ) ) ;
#22760=CARTESIAN_POINT ( 'NONE',  ( 11.18220574173929904, -2.863826994586552210, -6.911917091190550089 ) ) ;
#22772=CARTESIAN_POINT ( 'NONE',  ( 8.736413463905998711, -3.915843685459630574, -8.382409559052598880 ) ) ;
#22778=CARTESIAN_POINT ( 'NONE',  ( 10.12426357027499790, -2.745128867668000350, -7.742104041724699570 ) ) ;
#22791=CARTESIAN_POINT ( 'NONE',  ( 11.85979573085659844, -3.159987984332300215, -7.645349278262099979 ) ) ;
#22841=CARTESIAN_POINT ( 'NONE',  ( 9.254721904869999349, -3.124169273628900179, -7.991693846894699860 ) ) ;
#22842=CARTESIAN_POINT ( 'NONE',  ( 9.729346873516668381, -4.163624617374463099, -6.249999999999998224 ) ) ;
#22845=LINE ( 'NONE', #17963, #61868 ) ;
#22870=CARTESIAN_POINT ( 'NONE',  ( 10.55569598648999907, -2.869047858956000230, -8.173387776112500447 ) ) ;
#22895=CARTESIAN_POINT ( 'NONE',  ( 9.861671671056999600, -5.261543809652999393, -7.711876388024100137 ) ) ;
#22913=PRODUCT_DEFINITION_FORMATION_WITH_SPECIFIED_SOURCE ( 'ANY', '', #61747, .NOT_KNOWN. ) ;
#22935=ORIENTED_EDGE ( 'NONE', *, *, #21208, .T. ) ;
#22960=CARTESIAN_POINT ( 'NONE',  ( 9.321001730958842657, -4.768205771526717207, -6.500403846372137195 ) ) ;
#22963=ORIENTED_EDGE ( 'NONE', *, *, #29463, .T. ) ;
#22974=CARTESIAN_POINT ( 'NONE',  ( 11.13746005378019888, -2.838900981960999825, -6.879992063401499713 ) ) ;
#22976=ADVANCED_FACE ( 'NONE', ( #63052 ), #35727, .F. ) ;
#23005=CARTESIAN_POINT ( 'NONE',  ( 10.69041504065829962, -2.975441626403999784, -6.736065107693399945 ) ) ;
#23021=VERTEX_POINT ( 'NONE', #18464 ) ;
#23056=CARTESIAN_POINT ( 'NONE',  ( 10.25149413291699929, -2.962184842772000337, -7.026470926762800495 ) ) ;
#23075=CARTESIAN_POINT ( 'NONE',  ( 10.28622949779699880, -3.519000825516800379, -8.221351791991999391 ) ) ;
#23093=CARTESIAN_POINT ( 'NONE',  ( 10.30903300763299946, -3.402282662142699809, -8.126922218169600143 ) ) ;
#23130=CARTESIAN_POINT ( 'NONE',  ( 11.03502897915239878, -3.672866099873000056, -8.735435061820998826 ) ) ;
#23134=CARTESIAN_POINT ( 'NONE',  ( 8.719734573340000239, -4.222669097051499953, -8.352506367884300786 ) ) ;
#23185=CARTESIAN_POINT ( 'NONE',  ( 10.72726354018300121, -3.370476274536371442, -6.407767014557179230 ) ) ;
#23190=UNCERTAINTY_MEASURE_WITH_UNIT (LENGTH_MEASURE( 1.000000000000000082E-05 ), #12731, 'distance_accuracy_value', 'NONE');
#23192=CARTESIAN_POINT ( 'NONE',  ( 8.646822372493998543, -4.288705740401799638, -8.444453017408701356 ) ) ;
#23210=CARTESIAN_POINT ( 'NONE',  ( 10.49809687351654297, -4.327184855449103473, -8.717465845835393523 ) ) ;
#23234=SURFACE_STYLE_USAGE ( .BOTH. , #1913 ) ;
#23250=CARTESIAN_POINT ( 'NONE',  ( 10.21627973160999936, -3.885210315895700095, -6.225948307210999566 ) ) ;
#23329=CARTESIAN_POINT ( 'NONE',  ( 11.48011496860029901, -3.080230834057799960, -7.028661263734299780 ) ) ;
#23349=EDGE_CURVE ( 'NONE', #54348, #42489, #59292, .T. ) ;
#23360=CARTESIAN_POINT ( 'NONE',  ( 10.25149413291699929, -2.962184842772000337, -7.026470926762800495 ) ) ;
#23364=CARTESIAN_POINT ( 'NONE',  ( 10.29522949779699914, -3.519000825516800379, -8.221351791991999391 ) ) ;
#23413=CARTESIAN_POINT ( 'NONE',  ( 11.40841235500449891, -4.841138636481000290, -6.729431436870699557 ) ) ;
#23417=CARTESIAN_POINT ( 'NONE',  ( 11.60000000000000320, -3.890364666909557734, -8.637585274955608128 ) ) ;
#23428=CARTESIAN_POINT ( 'NONE',  ( 9.731000818238999983, -4.888721525563999748, -7.967991827203400490 ) ) ;
#23446=CARTESIAN_POINT ( 'NONE',  ( 11.49056651104150006, -3.914543207408039738, -6.638028001068500217 ) ) ;
#23478=CARTESIAN_POINT ( 'NONE',  ( 10.69041504065829962, -2.975441626403999784, -6.736065107693399945 ) ) ;
#23490=FACE_OUTER_BOUND ( 'NONE', #62156, .T. ) ;
#23493=CARTESIAN_POINT ( 'NONE',  ( 11.36486084871759950, -5.207010770456999893, -7.825000000000000178 ) ) ;
#23513=CARTESIAN_POINT ( 'NONE',  ( 10.50333291544900050, -3.468906853242413657, -8.658936933361777832 ) ) ;
#23536=CARTESIAN_POINT ( 'NONE',  ( 9.708633995697999453, -2.865156490077000129, -7.625954975973699312 ) ) ;
#23537=CARTESIAN_POINT ( 'NONE',  ( 9.635596873516670158, -2.907767014557175678, -6.870476274536380323 ) ) ;
#23562=CARTESIAN_POINT ( 'NONE',  ( 10.97124174884019965, -4.036194082918090231, -8.815770025351000072 ) ) ;
#23565=CARTESIAN_POINT ( 'NONE',  ( 11.59999999999999964, -4.000000000000000000, -7.500000000000000000 ) ) ;
#23576=ADVANCED_BREP_SHAPE_REPRESENTATION ( '', ( #31992, #9676 ), #756 ) ;
#23599=EDGE_CURVE ( 'NONE', #28041, #6018, #67707, .T. ) ;
#23623=FACE_OUTER_BOUND ( 'NONE', #63264, .T. ) ;
#23658=CARTESIAN_POINT ( 'NONE',  ( 8.857090631127384484, -3.380484464318182614, -6.695274228472992917 ) ) ;
#23667=CARTESIAN_POINT ( 'NONE',  ( 10.35814141025499957, -3.516507310755200066, -8.361148840840000318 ) ) ;
#23702=ORIENTED_EDGE ( 'NONE', *, *, #7257, .F. ) ;
#23719=CARTESIAN_POINT ( 'NONE',  ( 10.72191429142990060, -3.974927396630719922, -6.183971186511000084 ) ) ;
#23753=CARTESIAN_POINT ( 'NONE',  ( 11.33041235500449950, -4.942357465271699724, -6.636704692336500067 ) ) ;
#23765=CARTESIAN_POINT ( 'NONE',  ( 11.46550210169813511, -4.058074521742473628, -8.807012707104282967 ) ) ;
#23769=CARTESIAN_POINT ( 'NONE',  ( 8.895138961223999274, -3.167792625045000143, -8.062381800110799190 ) ) ;
#23786=CARTESIAN_POINT ( 'NONE',  ( 11.76133460557259980, -3.860150918677800025, -8.354833838171700222 ) ) ;
#23795=EDGE_CURVE ( 'NONE', #35633, #36490, #42595, .T. ) ;
#23821=CARTESIAN_POINT ( 'NONE',  ( 10.88733729122639993, -5.277570687708000641, -7.466391690027689876 ) ) ;
#23883=CARTESIAN_POINT ( 'NONE',  ( 9.809950584426999853, -3.546800160410199965, -6.451980747609000311 ) ) ;
#23897=LINE ( 'NONE', #33707, #11979 ) ;
#23910=CARTESIAN_POINT ( 'NONE',  ( 10.44999293566599974, -3.279967330949900450, -8.383280442119700027 ) ) ;
#23988=ORIENTED_EDGE ( 'NONE', *, *, #27471, .F. ) ;
#24016=CARTESIAN_POINT ( 'NONE',  ( 11.48522412107029922, -3.952868550833580130, -6.609122077774299164 ) ) ;
#24065=CARTESIAN_POINT ( 'NONE',  ( 11.09590547754519996, -2.684394667508000154, -7.541753805330609239 ) ) ;
#24099=CARTESIAN_POINT ( 'NONE',  ( 11.34287482311539996, -3.196874704906699893, -7.824481664695199790 ) ) ;
#24113=CARTESIAN_POINT ( 'NONE',  ( 8.819151519676999840, -3.978278301382419890, -8.504175633905001419 ) ) ;
#24130=CARTESIAN_POINT ( 'NONE',  ( 11.09256785386839894, -4.832509746210599921, -8.060248494254899754 ) ) ;
#24157=CARTESIAN_POINT ( 'NONE',  ( 11.01811411617009817, -5.026960591456000493, -7.825000000000000178 ) ) ;
#24171=CARTESIAN_POINT ( 'NONE',  ( 8.710288521113000115, -4.352953559891299840, -8.284550957747498501 ) ) ;
#24179=CARTESIAN_POINT ( 'NONE',  ( 11.48641235500450009, -4.739919807690899489, -6.822158181405299615 ) ) ;
#24216=CARTESIAN_POINT ( 'NONE',  ( 10.66476354018302608, -2.782534154164604256, -7.172815144550905408 ) ) ;
#24226=CARTESIAN_POINT ( 'NONE',  ( 10.06324205624999912, -4.409476560233800413, -8.565862728991998409 ) ) ;
#24227=CONICAL_SURFACE ( 'NONE', #42098, 0.9999998338055000602, 0.7853981908209605178 ) ;
#24239=FACE_OUTER_BOUND ( 'NONE', #63273, .T. ) ;
#24253=CARTESIAN_POINT ( 'NONE',  ( 11.67403632436368888, -4.976178716761900489, -7.272033745815799755 ) ) ;
#24264=( NAMED_UNIT ( * ) SI_UNIT ( $, .STERADIAN. ) SOLID_ANGLE_UNIT ( ) );
#24272=EDGE_CURVE ( 'NONE', #8437, #30840, #56833, .T. ) ;
#24282=CARTESIAN_POINT ( 'NONE',  ( 10.39157120343299923, -4.055348968344419269, -8.640469672413999547 ) ) ;
#24342=CARTESIAN_POINT ( 'NONE',  ( 9.396013540183334456, -4.999583552997726166, -8.268183399968641822 ) ) ;
#24352=CARTESIAN_POINT ( 'NONE',  ( 8.936337454063531638, -4.868096831666449908, -6.831783586538417552 ) ) ;
#24360=CARTESIAN_POINT ( 'NONE',  ( 10.72702344389999851, -5.004394439171999664, -6.890449684422599752 ) ) ;
#24396=CARTESIAN_POINT ( 'NONE',  ( 9.180747021775998107, -4.651672637235799712, -8.071865996877098937 ) ) ;
#24408=APPLICATION_CONTEXT ( 'automotive_design' ) ;
#24412=CARTESIAN_POINT ( 'NONE',  ( 11.55811496860034815, -2.954409148022000053, -6.964183526617899744 ) ) ;
#24445=CARTESIAN_POINT ( 'NONE',  ( 10.69041504065829962, -2.975441626403999784, -6.736065107693399945 ) ) ;
#24462=CARTESIAN_POINT ( 'NONE',  ( 10.32844474310100047, -3.228742141949900279, -7.874284411628199365 ) ) ;
#24480=CARTESIAN_POINT ( 'NONE',  ( 10.62487750876920067, -4.543557328885200697, -8.343502390669698343 ) ) ;
#24500=EDGE_LOOP ( 'NONE', ( #31411, #44369, #67026, #37033, #30892, #18407, #10399, #28007, #47766, #11793, #33177, #27509 ) ) ;
#24503=EDGE_CURVE ( 'NONE', #46988, #54418, #55057, .T. ) ;
#24523=CARTESIAN_POINT ( 'NONE',  ( 9.809470517051625649, -3.358100414793015354, -8.094556297950068924 ) ) ;
#24527=CARTESIAN_POINT ( 'NONE',  ( 11.07210672858429845, -4.692204557952299737, -6.979277962544199632 ) ) ;
#24554=CARTESIAN_POINT ( 'NONE',  ( 10.35987047770899672, -5.250000000000000000, -7.750389189149368363 ) ) ;
#24574=CARTESIAN_POINT ( 'NONE',  ( 9.404684229509999938, -4.804883439508000897, -6.690125258578699885 ) ) ;
#24603=CARTESIAN_POINT ( 'NONE',  ( 11.72433327354039889, -4.983220429128399687, -6.856888818507299810 ) ) ;
#24612=FILL_AREA_STYLE_COLOUR ( '', #17534 ) ;
#24629=CARTESIAN_POINT ( 'NONE',  ( 9.481734463323000739, -3.866750753272200303, -8.772253522581999974 ) ) ;
#24706=CARTESIAN_POINT ( 'NONE',  ( 10.43614141025499897, -3.450366949021700158, -8.478951440767898973 ) ) ;
#24727=CARTESIAN_POINT ( 'NONE',  ( 11.57299956498156845, -2.792989229543000107, -7.825000000000000178 ) ) ;
#24738=CARTESIAN_POINT ( 'NONE',  ( 10.26788779216199821, -3.070969952137800441, -7.835030859477799758 ) ) ;
#24753=CARTESIAN_POINT ( 'NONE',  ( 10.88813259637009878, -5.155817667926999803, -8.129798612793599943 ) ) ;
#24782=FACE_OUTER_BOUND ( 'NONE', #54424, .T. ) ;
#24783=CARTESIAN_POINT ( 'NONE',  ( 10.19810941423799910, -3.053977294209000437, -6.640722727400100389 ) ) ;
#24799=CARTESIAN_POINT ( 'NONE',  ( 11.57299956498156845, -2.792989229543000107, -7.825000000000000178 ) ) ;
#24802=CARTESIAN_POINT ( 'NONE',  ( 9.247734463322998977, -3.909687748588960066, -8.362294405496898619 ) ) ;
#24821=CARTESIAN_POINT ( 'NONE',  ( 10.50180110216399854, -4.856393875115199599, -6.976989117212499814 ) ) ;
#24848=CONICAL_SURFACE ( 'NONE', #12570, 0.9999998338055000602, 0.7853981908209605178 ) ;
#24854=VERTEX_POINT ( 'NONE', #51120 ) ;
#24864=CARTESIAN_POINT ( 'NONE',  ( 9.100254395947628083, -4.850975458930337325, -7.296596368717002790 ) ) ;
#24868=CARTESIAN_POINT ( 'NONE',  ( 11.09672200990539892, -4.817867935977999672, -7.214709569664399247 ) ) ;
#24875=CARTESIAN_POINT ( 'NONE',  ( 11.20596535229475776, -4.908912176279685013, -7.824984935920127782 ) ) ;
#24886=CARTESIAN_POINT ( 'NONE',  ( 10.67726354018259727, -3.370476274536371442, -6.407767014557179230 ) ) ;
#24893=CARTESIAN_POINT ( 'NONE',  ( 10.47145237372899906, -3.956267952212243255, -8.774080944853650976 ) ) ;
#24911=CARTESIAN_POINT ( 'NONE',  ( 9.455342523874998406, -5.128664655368000425, -7.327226901081999699 ) ) ;
#24941=CARTESIAN_POINT ( 'NONE',  ( 11.39189666366029918, -4.052152326617509459, -8.673729056199000809 ) ) ;
#24955=CARTESIAN_POINT ( 'NONE',  ( 8.734814475091132735, -3.943962993865710587, -8.383485082298649971 ) ) ;
#24989=CARTESIAN_POINT ( 'NONE',  ( 11.59999999999999964, -4.000000000000000000, -7.500000000000000000 ) ) ;
#25002=DIRECTION ( 'NONE',  ( 0.000000000000000000, 1.000000000000000000, 0.000000000000000000 ) ) ;
#25046=CARTESIAN_POINT ( 'NONE',  ( 11.22823073745748168, -4.169674042210387732, -8.360328963510957223 ) ) ;
#25123=CARTESIAN_POINT ( 'NONE',  ( 11.56441235500451015, -4.638700978900200056, -6.914884925939399629 ) ) ;
#25124=CARTESIAN_POINT ( 'NONE',  ( 10.98579841651039857, -4.449968941611500028, -8.696179055230999211 ) ) ;
#25128=CARTESIAN_POINT ( 'NONE',  ( 11.33810207955129812, -3.203462856645999945, -7.825000000000000178 ) ) ;
#25141=CARTESIAN_POINT ( 'NONE',  ( 8.918455549952998496, -3.325238030324599858, -6.955569812538500152 ) ) ;
#25159=CARTESIAN_POINT ( 'NONE',  ( 10.64949279009019989, -4.260984538213099526, -8.468936491037499792 ) ) ;
#25203=CARTESIAN_POINT ( 'NONE',  ( 10.26539516633362759, -3.766791217824746241, -8.343294540545050708 ) ) ;
#25207=CARTESIAN_POINT ( 'NONE',  ( 10.50595525820100029, -4.081787880721680750, -6.637672143048099827 ) ) ;
#25213=CARTESIAN_POINT ( 'NONE',  ( 10.21684687351595677, -3.231816600031351516, -6.500416447002277387 ) ) ;
#25255=CARTESIAN_POINT ( 'NONE',  ( 9.706621437244999484, -3.150324864944999970, -6.543738240676099771 ) ) ;
#25286=CARTESIAN_POINT ( 'NONE',  ( 10.81013259637009938, -5.031671030421000168, -8.062151801142800167 ) ) ;
#25287=CARTESIAN_POINT ( 'NONE',  ( 11.60000000000000142, -3.064876132552084353, -6.791171049664777470 ) ) ;
#25288=CARTESIAN_POINT ( 'NONE',  ( 9.099999931440999390, -2.753634353389999845, -7.404749409716440134 ) ) ;
#25298=CARTESIAN_POINT ( 'NONE',  ( 8.736413463905998711, -3.915843685459630574, -8.382409559052598880 ) ) ;
#25310=EDGE_CURVE ( 'NONE', #37989, #23021, #11567, .T. ) ;
#25342=CARTESIAN_POINT ( 'NONE',  ( 8.599999952505998024, -4.000000000000000000, -7.500000000000000000 ) ) ;
#25377=LINE ( 'NONE', #41806, #10928 ) ;
#25399=DIRECTION ( 'NONE',  ( -0.5000000000000150990, 0.08222066253632250021, -0.8621135439442261239 ) ) ;
#25406=CARTESIAN_POINT ( 'NONE',  ( 8.717397846562217723, -4.245312990446880264, -8.340771899786949106 ) ) ;
#25452=CARTESIAN_POINT ( 'NONE',  ( 11.32299956498189886, -5.207010770456999893, -7.174999999999999822 ) ) ;
#25464=CARTESIAN_POINT ( 'NONE',  ( 10.87518447801629939, -3.134012688501500055, -7.480906371072489236 ) ) ;
#25466=CYLINDRICAL_SURFACE ( 'NONE', #42260, 1.250000000000000222 ) ;
#25505=CARTESIAN_POINT ( 'NONE',  ( 10.37872469555899890, -3.497841151814999883, -6.631215019384099740 ) ) ;
#25552=CARTESIAN_POINT ( 'NONE',  ( 9.176241837494625742, -4.657637647145090654, -8.077100505959180055 ) ) ;
#25556=CARTESIAN_POINT ( 'NONE',  ( 11.02287616594229824, -4.261927842557799551, -6.674353346984900348 ) ) ;
#25605=CARTESIAN_POINT ( 'NONE',  ( 9.731950584426998674, -3.492264136285500253, -6.325866838823999139 ) ) ;
#25659=DIRECTION ( 'NONE',  ( 0.000000000000000000, -1.000000000000000000, 0.000000000000000000 ) ) ;
#25724=CARTESIAN_POINT ( 'NONE',  ( 11.16486084871730000, -2.792989229543000107, -7.174999999999999822 ) ) ;
#25730=CARTESIAN_POINT ( 'NONE',  ( 10.44635971519499940, -3.540377183549800133, -6.735384833238199143 ) ) ;
#25808=CARTESIAN_POINT ( 'NONE',  ( 11.11718313518939816, -4.622449961306399402, -8.287087605365499599 ) ) ;
#25829=CARTESIAN_POINT ( 'NONE',  ( 9.399709346416997846, -3.216804796119200116, -7.128095150442700145 ) ) ;
#25847=CARTESIAN_POINT ( 'NONE',  ( 10.28026357027499849, -3.014700852776899698, -7.690095141806899903 ) ) ;
#25848=ORIENTED_EDGE ( 'NONE', *, *, #27814, .T. ) ;
#25895=CARTESIAN_POINT ( 'NONE',  ( 9.910787105781626138, -3.243350240173176413, -7.060667085372605456 ) ) ;
#25899=CARTESIAN_POINT ( 'NONE',  ( 11.48225819896749833, -5.120994791668000090, -7.711331004020999913 ) ) ;
#25913=CARTESIAN_POINT ( 'NONE',  ( 9.884988259786998910, -4.149395984695000372, -8.631996151823999597 ) ) ;
#25945=CARTESIAN_POINT ( 'NONE',  ( 9.858596320338998353, -5.184381781355999586, -7.016653143730500197 ) ) ;
#25975=CARTESIAN_POINT ( 'NONE',  ( 11.60988784977536348, -4.851105903694400645, -7.451365240271489832 ) ) ;
#26025=VECTOR ( 'NONE', #28390, 1000.000000000000000 ) ;
#26026=CARTESIAN_POINT ( 'NONE',  ( 10.14124205625000030, -4.360201998293100623, -8.437601616732200327 ) ) ;
#26041=ADVANCED_FACE ( 'NONE', ( #60781 ), #51345, .F. ) ;
#26044=CARTESIAN_POINT ( 'NONE',  ( 11.43345123989529810, -3.459769760840400110, -8.543317325199000223 ) ) ;
#26125=EDGE_CURVE ( 'NONE', #26585, #42419, #23897, .T. ) ;
#26146=ORIENTED_EDGE ( 'NONE', *, *, #10142, .T. ) ;
#26160=CARTESIAN_POINT ( 'NONE',  ( 11.04333729122639873, -5.003122373830000136, -7.473611442402849470 ) ) ;
#26178=CARTESIAN_POINT ( 'NONE',  ( 8.724265421554999733, -4.162714371335800578, -8.341695632489900092 ) ) ;
#26198=CARTESIAN_POINT ( 'NONE',  ( 10.44841638348500013, -5.108333310975999630, -7.230023356477299323 ) ) ;
#26222=ADVANCED_FACE ( 'NONE', ( #24239 ), #34404, .T. ) ;
#26244=CARTESIAN_POINT ( 'NONE',  ( 8.897621218489625505, -3.181327125463422334, -7.191281694476484354 ) ) ;
#26249=CARTESIAN_POINT ( 'NONE',  ( 10.21462282008599942, -3.476853648246800432, -8.343818446627699004 ) ) ;
#26260=VERTEX_POINT ( 'NONE', #15127 ) ;
#26262=CARTESIAN_POINT ( 'NONE',  ( 8.949822372493999367, -4.367693913457399546, -8.702849744394999476 ) ) ;
#26280=CARTESIAN_POINT ( 'NONE',  ( 9.082867883171827472, -3.217326796159980518, -8.474986547786114599 ) ) ;
#26295=CARTESIAN_POINT ( 'NONE',  ( 8.516151519676999015, -3.972335373863620234, -8.778912113473998247 ) ) ;
#26316=CARTESIAN_POINT ( 'NONE',  ( 11.03918313518939875, -4.707599264529200411, -8.394758848575399668 ) ) ;
#26324=CARTESIAN_POINT ( 'NONE',  ( 9.821013540182335078, -4.768183399968640934, -6.500416447002272946 ) ) ;
#26329=ORIENTED_EDGE ( 'NONE', *, *, #58744, .T. ) ;
#26375=CARTESIAN_POINT ( 'NONE',  ( 9.889963142879999225, -3.151633609938700342, -7.321163726496699553 ) ) ;
#26403=ORIENTED_EDGE ( 'NONE', *, *, #13990, .T. ) ;
#26425=CARTESIAN_POINT ( 'NONE',  ( 10.28014141025500017, -3.582647672488299850, -8.243346240911998635 ) ) ;
#26479=ORIENTED_EDGE ( 'NONE', *, *, #17843, .T. ) ;
#26503=CARTESIAN_POINT ( 'NONE',  ( 10.55518582084299872, -4.566724035220099509, -6.844925608615599621 ) ) ;
#26544=CARTESIAN_POINT ( 'NONE',  ( 11.45764291764649911, -5.132124077409000229, -7.360052904210999891 ) ) ;
#26562=CARTESIAN_POINT ( 'NONE',  ( 10.53521345716899837, -3.075109701058799772, -8.340879262988799780 ) ) ;
#26585=VERTEX_POINT ( 'NONE', #49004 ) ;
#26591=CARTESIAN_POINT ( 'NONE',  ( 8.772923981633081070, -3.689545703815815703, -8.314671747086004316 ) ) ;
#26596=CARTESIAN_POINT ( 'NONE',  ( 11.11718313518939816, -4.622449961306399402, -8.287087605365499599 ) ) ;
#26604=CARTESIAN_POINT ( 'NONE',  ( 8.810863317747999801, -3.039136629551499880, -7.500000000073117512 ) ) ;
#26612=CARTESIAN_POINT ( 'NONE',  ( 9.127126402770999292, -2.803062940908000122, -7.048639765412399782 ) ) ;
#26645=CARTESIAN_POINT ( 'NONE',  ( 8.870759580228998686, -5.244164909883999748, -7.202614619576299226 ) ) ;
#26666=CARTESIAN_POINT ( 'NONE',  ( 10.37457053952199892, -4.448306506338299826, -6.451042711717000167 ) ) ;
#26674=CARTESIAN_POINT ( 'NONE',  ( 10.36325056272499978, -3.107965259299500183, -7.513220396995270001 ) ) ;
#26676=CARTESIAN_POINT ( 'NONE',  ( 11.60000000000000142, -4.254640155007241020, -6.522131813714045379 ) ) ;
#26677=CONICAL_SURFACE ( 'NONE', #14402, 0.9346783463124002100, 0.7853981908209605178 ) ;
#26712=ORIENTED_EDGE ( 'NONE', *, *, #44763, .T. ) ;
#26713=CARTESIAN_POINT ( 'NONE',  ( 11.29364426047339975, -3.533902447304699823, -8.230103870496201068 ) ) ;
#26718=VECTOR ( 'NONE', #48813, 1000.000000000000114 ) ;
#26724=CARTESIAN_POINT ( 'NONE',  ( 8.978113844317999082, -3.781046324972699768, -6.661091642253600398 ) ) ;
#26737=CARTESIAN_POINT ( 'NONE',  ( 11.31900581613029821, -3.249313226592100534, -7.982035256002799173 ) ) ;
#26755=CARTESIAN_POINT ( 'NONE',  ( 9.583513540183334456, -2.750000000000000000, -7.663624617374468428 ) ) ;
#26760=EDGE_CURVE ( 'NONE', #10029, #47524, #10706, .T. ) ;
#26855=CARTESIAN_POINT ( 'NONE',  ( 11.69559063708295987, -2.913481137622000006, -7.805482129094999166 ) ) ;
#26887=CARTESIAN_POINT ( 'NONE',  ( 11.48225819896749833, -5.120994791668000090, -7.711331004020999913 ) ) ;
#26936=CARTESIAN_POINT ( 'NONE',  ( 11.19102897915239936, -3.743141152489600110, -8.470038342183499935 ) ) ;
#26953=CARTESIAN_POINT ( 'NONE',  ( 9.581038493598999395, -3.173653894988100355, -6.712036445818600150 ) ) ;
#26983=CARTESIAN_POINT ( 'NONE',  ( 11.41486084871699802, -5.207010770456999893, -7.825000000000000178 ) ) ;
#27003=CARTESIAN_POINT ( 'NONE',  ( 11.50271932425157040, -4.187398418774900044, -8.764198628556998827 ) ) ;
#27007=CARTESIAN_POINT ( 'NONE',  ( 8.726787239609997471, -4.219532685969900498, -8.340498368324299250 ) ) ;
#27009=CARTESIAN_POINT ( 'NONE',  ( 11.48522412107029922, -3.952868550833580130, -6.609122077774299164 ) ) ;
#27044=CARTESIAN_POINT ( 'NONE',  ( 11.59999999999999964, -4.000000000000000000, -7.500000000000000000 ) ) ;
#27063=CARTESIAN_POINT ( 'NONE',  ( 9.558671671056998775, -4.990538396979200542, -7.666361006367900188 ) ) ;
#27077=CARTESIAN_POINT ( 'NONE',  ( 10.48791429142999831, -3.983006558652820051, -6.608036045330599961 ) ) ;
#27087=CARTESIAN_POINT ( 'NONE',  ( 8.706426979769998908, -4.358851904410700584, -8.276078370613198842 ) ) ;
#27095=CARTESIAN_POINT ( 'NONE',  ( 10.19809687351566829, -3.672815144550895639, -6.282534154164608253 ) ) ;
#27109=EDGE_CURVE ( 'NONE', #35633, #35196, #17727, .T. ) ;
#27181=CARTESIAN_POINT ( 'NONE',  ( 9.248087964304163577, -3.672831456759381830, -6.282577178243119675 ) ) ;
#27194=CARTESIAN_POINT ( 'NONE',  ( 10.64949279009019989, -4.260984538213099526, -8.468936491037499792 ) ) ;
#27198=CARTESIAN_POINT ( 'NONE',  ( 11.83003632436370012, -5.243255406354000669, -7.209663534847899236 ) ) ;
#27227=CARTESIAN_POINT ( 'NONE',  ( 11.01456785386839954, -4.946394603182100447, -8.136888821800198457 ) ) ;
#27279=CARTESIAN_POINT ( 'NONE',  ( 11.03918313518939875, -4.707599264529200411, -8.394758848575399668 ) ) ;
#27295=CARTESIAN_POINT ( 'NONE',  ( 8.871822372493998188, -4.328199826929600036, -8.573651380901999630 ) ) ;
#27345=CARTESIAN_POINT ( 'NONE',  ( 10.25149413291699929, -2.962184842772000337, -7.026470926762800495 ) ) ;
#27367=CARTESIAN_POINT ( 'NONE',  ( 9.591846873515667227, -3.000416447002275167, -8.268183399968643599 ) ) ;
#27403=CARTESIAN_POINT ( 'NONE',  ( 9.482684229509999341, -4.708027397558999461, -6.787581931282099745 ) ) ;
#27418=CARTESIAN_POINT ( 'NONE',  ( 11.23078751119019891, -4.915752892793999962, -7.979095341142500075 ) ) ;
#27436=CARTESIAN_POINT ( 'NONE',  ( 10.11476354018233081, -2.782534154164604256, -7.172815144550903632 ) ) ;
#27454=ORIENTED_EDGE ( 'NONE', *, *, #42441, .F. ) ;
#27460=B_SPLINE_CURVE_WITH_KNOTS ( 'NONE', 3,
 ( #63262, #59661, #62919, #64888 ),
 .UNSPECIFIED., .F., .F.,
 ( 4, 4 ),
 ( 0.8163836489557126930, 1.000000000000000000 ),
 .UNSPECIFIED. ) ;
#27471=EDGE_CURVE ( 'NONE', #3420, #37989, #63601, .T. ) ;
#27482=DIRECTION ( 'NONE',  ( -1.000000000000000000, 0.000000000000000000, 0.000000000000000000 ) ) ;
#27489=LINE ( 'NONE', #64185, #26718 ) ;
#27509=ORIENTED_EDGE ( 'NONE', *, *, #65013, .F. ) ;
#27525=AXIS2_PLACEMENT_3D ( 'NONE', #54746, #12098, #56122 ) ;
#27536=CARTESIAN_POINT ( 'NONE',  ( 11.43302763632549990, -5.035790660926999784, -7.022058766158599141 ) ) ;
#27561=CARTESIAN_POINT ( 'NONE',  ( 11.33810207955129812, -3.203462856645999945, -7.825000000000000178 ) ) ;
#27569=CARTESIAN_POINT ( 'NONE',  ( 11.40425819896749893, -5.255890247626999745, -7.736761623643599428 ) ) ;
#27622=CARTESIAN_POINT ( 'NONE',  ( 10.52226222744799955, -4.880489021643899861, -8.225278704382400718 ) ) ;
#27641=CARTESIAN_POINT ( 'NONE',  ( 9.454392757686999715, -3.229293331742300044, -8.342464052342599246 ) ) ;
#27671=CARTESIAN_POINT ( 'NONE',  ( 11.59999999999999964, -2.935681553670999921, -8.155535082817699788 ) ) ;
#27696=CARTESIAN_POINT ( 'NONE',  ( 10.64118447801629941, -2.722297859592000435, -7.471828720557429193 ) ) ;
#27758=CARTESIAN_POINT ( 'NONE',  ( 9.229392757687000071, -3.322036695224600322, -8.241085728986799808 ) ) ;
#27774=CARTESIAN_POINT ( 'NONE',  ( 11.23589666366019912, -4.039600775206940497, -8.391246537305399045 ) ) ;
#27781=CARTESIAN_POINT ( 'NONE',  ( 8.783078676347997771, -4.247267730859300094, -8.446684196061099215 ) ) ;
#27787=B_SPLINE_CURVE_WITH_KNOTS ( 'NONE', 3,
 ( #30539, #51850, #14118, #35442, #25287, #52197, #3607, #41023, #14462, #35782, #57097, #41371, #9196, #67926, #20042, #36120, #47989, #58474, #64735, #26676, #43782, #16851, #11601, #10579, #59159, #91, #6357, #58817, #53232, #780 ),
 .UNSPECIFIED., .F., .F.,
 ( 4, 2, 1, 1, 2, 2, 2, 2, 2, 2, 2, 2, 2, 2, 2, 4 ),
 ( 0.000000000000000000, 0.1250000000000011102, 0.1875000000000016653, 0.2187500000000019429, 0.2343750000000018874, 0.2500000000000018319, 0.3750000000000014433, 0.4375000000000012212, 0.5000000000000009992, 0.5625000000000007772, 0.6250000000000005551, 0.6875000000000003331, 0.7500000000000001110, 0.8124999999999998890, 0.8749999999999996669, 1.000000000000000000 ),
 .UNSPECIFIED. ) ;
#27788=CARTESIAN_POINT ( 'NONE',  ( 10.80502344389999791, -5.125258734743999511, -6.817099149379099110 ) ) ;
#27814=EDGE_CURVE ( 'NONE', #64952, #2109, #32649, .T. ) ;
#27841=ORIENTED_EDGE ( 'NONE', *, *, #12706, .F. ) ;
#27888=CARTESIAN_POINT ( 'NONE',  ( 11.30995122972050027, -3.547233695387300045, -6.452959986593999275 ) ) ;
#27892=CARTESIAN_POINT ( 'NONE',  ( 10.93479632507519916, -3.442212747724900268, -8.534037301706000278 ) ) ;
#27921=CARTESIAN_POINT ( 'NONE',  ( 11.08425954179440076, -3.017023678917100327, -8.316745941391600283 ) ) ;
#27928=EDGE_CURVE ( 'NONE', #46774, #10029, #4280, .T. ) ;
#27943=CARTESIAN_POINT ( 'NONE',  ( 11.83003632436370012, -5.243255406354000669, -7.209663534847899236 ) ) ;
#27967=CARTESIAN_POINT ( 'NONE',  ( 10.39393020684999946, -5.250000000000000000, -7.500000000000000000 ) ) ;
#27972=CARTESIAN_POINT ( 'NONE',  ( 10.39918582084299992, -4.746348444722899629, -6.637298362509499228 ) ) ;
#27988=CARTESIAN_POINT ( 'NONE',  ( 8.880265421554998539, -4.214287043487900064, -8.608472884860999486 ) ) ;
#28005=CARTESIAN_POINT ( 'NONE',  ( 10.40749413291699987, -3.211956830789300277, -7.140435631538599281 ) ) ;
#28007=ORIENTED_EDGE ( 'NONE', *, *, #55842, .F. ) ;
#28040=CARTESIAN_POINT ( 'NONE',  ( 10.22272469555899832, -3.360453478306600239, -6.393520617113999549 ) ) ;
#28041=VERTEX_POINT ( 'NONE', #27967 ) ;
#28098=CARTESIAN_POINT ( 'NONE',  ( 9.584000818238999742, -4.888721525563999748, -7.967991827203400490 ) ) ;
#28118=( NAMED_UNIT ( * ) PLANE_ANGLE_UNIT ( ) SI_UNIT ( $, .RADIAN. ) );
#28127=CARTESIAN_POINT ( 'NONE',  ( 10.26059687351567007, -4.629523725463621453, -6.407767014557177454 ) ) ;
#28189=CARTESIAN_POINT ( 'NONE',  ( 10.88210843320517007, -5.137688304401064165, -8.098394516494941797 ) ) ;
#28217=CARTESIAN_POINT ( 'NONE',  ( 9.216839207166819037, -3.231820996160964743, -6.500433908363888236 ) ) ;
#28226=CARTESIAN_POINT ( 'NONE',  ( 11.01872200990539952, -4.947480442174099657, -7.169497859994799605 ) ) ;
#28230=CARTESIAN_POINT ( 'NONE',  ( 11.42834208742529967, -4.706521750018099581, -8.610579932818998472 ) ) ;
#28260=CARTESIAN_POINT ( 'NONE',  ( 10.17764828895399809, -2.998858038575999974, -8.046814291299300592 ) ) ;
#28309=CARTESIAN_POINT ( 'NONE',  ( 10.54687750876899877, -4.617914354660699772, -8.458891008702400072 ) ) ;
#28328=CARTESIAN_POINT ( 'NONE',  ( 9.403734463322997783, -3.881063085044400118, -8.635600483553998785 ) ) ;
#28350=CARTESIAN_POINT ( 'NONE',  ( 10.57980110216399972, -4.739241740354600552, -7.048535450274799885 ) ) ;
#28387=CARTESIAN_POINT ( 'NONE',  ( 10.71503032197929883, -3.256621462143499901, -6.460430507351999196 ) ) ;
#28390=DIRECTION ( 'NONE',  ( -1.000000000000000000, 0.000000000000000000, 0.000000000000000000 ) ) ;
#28450=CARTESIAN_POINT ( 'NONE',  ( 8.748138961223999033, -3.167792625045000143, -8.062381800110799190 ) ) ;
#28466=CARTESIAN_POINT ( 'NONE',  ( 10.56059687351646481, -3.370476274536376771, -8.592232985442823434 ) ) ;
#28520=CARTESIAN_POINT ( 'NONE',  ( 10.39393020684999946, -5.250000000000000000, -7.500000000000000000 ) ) ;
#28560=ORIENTED_EDGE ( 'NONE', *, *, #60528, .F. ) ;
#28567=DIRECTION ( 'NONE',  ( 0.000000000000000000, 0.000000000000000000, 1.000000000000000000 ) ) ;
#28615=CARTESIAN_POINT ( 'NONE',  ( 11.25656651104150008, -3.873914634362100262, -6.228222165170999247 ) ) ;
#28666=CARTESIAN_POINT ( 'NONE',  ( 10.81764560330029923, -3.650429500487800460, -6.414140625063999401 ) ) ;
#28683=CARTESIAN_POINT ( 'NONE',  ( 9.705671671056999017, -4.990538396979200542, -7.666361006367900188 ) ) ;
#28687=AXIS2_PLACEMENT_3D ( 'NONE', #11403, #64879, #34133 ) ;
#28702=CARTESIAN_POINT ( 'NONE',  ( 11.39210538575740017, -3.157545584346100220, -7.298582155985900322 ) ) ;
#28739=CARTESIAN_POINT ( 'NONE',  ( 10.91195257254739914, -5.227167235646000165, -7.856899084262298771 ) ) ;
#28801=UNCERTAINTY_MEASURE_WITH_UNIT (LENGTH_MEASURE( 1.000000000000000082E-05 ), #13097, 'distance_accuracy_value', 'NONE');
#28804=CARTESIAN_POINT ( 'NONE',  ( 9.227380199234000102, -2.867101906753999785, -7.357604921762999517 ) ) ;
#28805=CARTESIAN_POINT ( 'NONE',  ( 9.802263540183334456, -5.092232985442821658, -6.870476274536374994 ) ) ;
#28833=CARTESIAN_POINT ( 'NONE',  ( 11.84388784977539899, -5.255745690988000263, -7.428242901739219306 ) ) ;
#28842=ORIENTED_EDGE ( 'NONE', *, *, #63221, .T. ) ;
#28892=LINE ( 'NONE', #60683, #17546 ) ;
#28924=CARTESIAN_POINT ( 'NONE',  ( 11.59999999999999964, -2.613168764257999932, -7.174999999999999822 ) ) ;
#28931=CARTESIAN_POINT ( 'NONE',  ( 8.883506238772763908, -3.863849893416519077, -6.466493704552774169 ) ) ;
#28940=CARTESIAN_POINT ( 'NONE',  ( 11.06967835872019812, -4.754733798270200928, -7.024326263066900111 ) ) ;
#28969=CARTESIAN_POINT ( 'NONE',  ( 10.32118582084299874, -4.836160649475099937, -6.533484739457099622 ) ) ;
#28989=CARTESIAN_POINT ( 'NONE',  ( 10.89324174884020024, -4.032306468273969990, -8.674442868902998427 ) ) ;
#29032=CARTESIAN_POINT ( 'NONE',  ( 11.39043504475232815, -5.070797187771876047, -8.202738646980327175 ) ) ;
#29036=CARTESIAN_POINT ( 'NONE',  ( 10.03293802597399953, -4.450760089576400347, -6.759376420744099612 ) ) ;
#29052=CARTESIAN_POINT ( 'NONE',  ( 10.75210807141120029, -3.959980833595939664, -8.365272822098500427 ) ) ;
#29077=CARTESIAN_POINT ( 'NONE',  ( 11.05336220499919797, -4.965402920923000174, -7.825000000000000178 ) ) ;
#29099=CARTESIAN_POINT ( 'NONE',  ( 11.85159063708299954, -3.174974693948799942, -7.731961446576300467 ) ) ;
#29145=CARTESIAN_POINT ( 'NONE',  ( 9.657975701332999208, -3.162316589966200020, -8.275900091855099561 ) ) ;
#29146=CARTESIAN_POINT ( 'NONE',  ( 9.760596873516668381, -4.629523725463621453, -6.407767014557177454 ) ) ;
#29150=DIRECTION ( 'NONE',  ( -1.000000000000000000, 0.000000000000000000, 0.000000000000000000 ) ) ;
#29160=CARTESIAN_POINT ( 'NONE',  ( 10.63351354018304740, -2.750000000000000000, -7.663624617374467540 ) ) ;
#29168=CARTESIAN_POINT ( 'NONE',  ( 11.53192018828833731, -4.908970299435360118, -7.175001928748123703 ) ) ;
#29172=CARTESIAN_POINT ( 'NONE',  ( 11.35034208742529849, -4.630634088820300143, -8.491292290686200062 ) ) ;
#29196=CARTESIAN_POINT ( 'NONE',  ( 10.01364655415099847, -3.380689388027600106, -8.619302797893999113 ) ) ;
#29276=CARTESIAN_POINT ( 'NONE',  ( 11.52677869730533011, -4.403502086956500250, -6.704332466833498927 ) ) ;
#29326=CARTESIAN_POINT ( 'NONE',  ( 11.26723293495529887, -5.173938955706000264, -7.452807962566580180 ) ) ;
#29335=ORIENTED_EDGE ( 'NONE', *, *, #27109, .F. ) ;
#29360=CARTESIAN_POINT ( 'NONE',  ( 11.07210672858429845, -4.692204557952299737, -6.979277962544199632 ) ) ;
#29361=CARTESIAN_POINT ( 'NONE',  ( 11.37964291764649971, -5.268358781405000357, -7.343212302062899433 ) ) ;
#29379=CARTESIAN_POINT ( 'NONE',  ( 9.680342523874998051, -4.992846242613000030, -7.348017636355000270 ) ) ;
#29398=CARTESIAN_POINT ( 'NONE',  ( 11.73256516821459883, -3.293702443348299980, -8.212808089543500500 ) ) ;
#29444=CARTESIAN_POINT ( 'NONE',  ( 10.13559687351567007, -2.907767014557175678, -6.870476274536380323 ) ) ;
#29448=CARTESIAN_POINT ( 'NONE',  ( 11.56025819896753859, -4.986099335708799707, -7.685900384398899554 ) ) ;
#29463=EDGE_CURVE ( 'NONE', #17417, #23021, #58289, .T. ) ;
#29475=CARTESIAN_POINT ( 'NONE',  ( 10.45551210286900279, -4.217228369037729685, -8.756187319522085843 ) ) ;
#29498=CARTESIAN_POINT ( 'NONE',  ( 9.987254614702999689, -5.106563667948999630, -7.781516069110699263 ) ) ;
#29527=CARTESIAN_POINT ( 'NONE',  ( 11.26723293495529887, -5.173938955706000264, -7.452807962566580180 ) ) ;
#29553=CARTESIAN_POINT ( 'NONE',  ( 9.228442991499999692, -4.080527519162810535, -6.223324745230999433 ) ) ;
#29620=CARTESIAN_POINT ( 'NONE',  ( 8.969356963619999235, -5.119357025014000584, -7.499999999914821025 ) ) ;
#29628=CARTESIAN_POINT ( 'NONE',  ( 10.64391429142989765, -3.977620450637519678, -6.325326139450999641 ) ) ;
#29679=CARTESIAN_POINT ( 'NONE',  ( 11.59966954483535773, -3.361010663344000005, -6.514072057539499916 ) ) ;
#29692=FACE_OUTER_BOUND ( 'NONE', #37796, .T. ) ;
#29711=CARTESIAN_POINT ( 'NONE',  ( 11.21979841651039855, -4.304975143798100312, -8.310733465454200442 ) ) ;
#29712=CARTESIAN_POINT ( 'NONE',  ( 10.64118447801629941, -2.722297859592000435, -7.471828720557429193 ) ) ;
#29727=CARTESIAN_POINT ( 'NONE',  ( 9.503038493598998215, -3.273092657276900130, -6.806856425099999441 ) ) ;
#29745=CARTESIAN_POINT ( 'NONE',  ( 11.68333460557258796, -3.837988184179999873, -8.490304555719900392 ) ) ;
#29760=DIRECTION ( 'NONE',  ( -1.000000000000000000, 0.000000000000000000, 0.000000000000000000 ) ) ;
#29795=CARTESIAN_POINT ( 'NONE',  ( 11.36749010443639918, -3.136214309321499805, -7.564597762509089662 ) ) ;
#29838=DIRECTION ( 'NONE',  ( 1.000000000000000000, 0.000000000000000000, 0.000000000000000000 ) ) ;
#29841=CARTESIAN_POINT ( 'NONE',  ( 9.683304848515998486, -2.961576783819000358, -7.974775391194199869 ) ) ;
#29868=CARTESIAN_POINT ( 'NONE',  ( 11.43345123989529810, -3.459769760840400110, -8.543317325199000223 ) ) ;
#29879=SURFACE_STYLE_FILL_AREA ( #8531 ) ;
#29894=CARTESIAN_POINT ( 'NONE',  ( 9.935646554150999066, -3.447209681134600245, -8.499078230848398974 ) ) ;
#29971=CARTESIAN_POINT ( 'NONE',  ( 11.23078751119019891, -4.915752892793999962, -7.979095341142500075 ) ) ;
#30005=CARTESIAN_POINT ( 'NONE',  ( 8.750151519676999001, -3.981249765141819719, -8.366807394121199337 ) ) ;
#30009=B_SPLINE_CURVE_WITH_KNOTS ( 'NONE', 3,
 ( #64958, #1007, #42623, #5553, #42965, #662, #64272, #16386, #48902, #37716 ),
 .UNSPECIFIED., .F., .F.,
 ( 4, 2, 2, 2, 4 ),
 ( 0.000000000000000000, 0.2499999999999997780, 0.4999999999999995559, 0.7499999999999997780, 1.000000000000000000 ),
 .UNSPECIFIED. ) ;
#30021=CARTESIAN_POINT ( 'NONE',  ( 11.30878751119029957, -5.041025164610000608, -8.044634158732998586 ) ) ;
#30041=EDGE_LOOP ( 'NONE', ( #14058, #8679, #58620, #36655, #49617 ) ) ;
#30043=EDGE_CURVE ( 'NONE', #54684, #37989, #54604, .T. ) ;
#30052=CARTESIAN_POINT ( 'NONE',  ( 10.91195257254739914, -5.227167235646000165, -7.856899084262298771 ) ) ;
#30067=CARTESIAN_POINT ( 'NONE',  ( 9.148430433047000321, -4.854750075120300323, -6.972511033848699746 ) ) ;
#30086=CARTESIAN_POINT ( 'NONE',  ( 11.51102763632551884, -4.911148285670300595, -7.079572058049399708 ) ) ;
#30129=CARTESIAN_POINT ( 'NONE',  ( 9.404204162135625822, -3.209635909649031671, -7.124690962532754135 ) ) ;
#30133=CARTESIAN_POINT ( 'NONE',  ( 11.21979841651039855, -4.304975143798100312, -8.310733465454200442 ) ) ;
#30176=CARTESIAN_POINT ( 'NONE',  ( 9.607317406968999052, -3.787635830142400462, -8.621889436328999068 ) ) ;
#30202=CARTESIAN_POINT ( 'NONE',  ( 10.64391429142989765, -3.977620450637519678, -6.325326139450999641 ) ) ;
#30280=ORIENTED_EDGE ( 'NONE', *, *, #55318, .T. ) ;
#30341=ORIENTED_EDGE ( 'NONE', *, *, #61403, .T. ) ;
#30351=CARTESIAN_POINT ( 'NONE',  ( 11.22567835872029995, -4.993948309075300074, -6.873560442659099046 ) ) ;
#30379=CARTESIAN_POINT ( 'NONE',  ( 11.73671932425159881, -4.127012898954600217, -8.356835045446798560 ) ) ;
#30380=CARTESIAN_POINT ( 'NONE',  ( 10.76426088462129904, -3.997280690308189666, -6.221990224628999755 ) ) ;
#30399=CARTESIAN_POINT ( 'NONE',  ( 9.298392757686999133, -3.414780058706900157, -8.139707405630899117 ) ) ;
#30415=CARTESIAN_POINT ( 'NONE',  ( 10.69872335273220010, -3.650693637952500126, -8.440710326446700051 ) ) ;
#30428=CARTESIAN_POINT ( 'NONE',  ( 11.59999999999999964, -2.792989229543000107, -7.825000000000000178 ) ) ;
#30459=CARTESIAN_POINT ( 'NONE',  ( 9.302887573405627109, -3.409423315843189251, -8.145562893180322561 ) ) ;
#30464=CARTESIAN_POINT ( 'NONE',  ( 11.31825954179440075, -3.333768806796900019, -8.053565341712399572 ) ) ;
#30469=CARTESIAN_POINT ( 'NONE',  ( 10.22726354018266370, -3.370476274536371442, -6.407767014557179230 ) ) ;
#30480=CARTESIAN_POINT ( 'NONE',  ( 10.82309687351639660, -5.217465845835395299, -7.172815144550894750 ) ) ;
#30487=CARTESIAN_POINT ( 'NONE',  ( 10.51927318630899855, -3.243547362524661359, -8.526145288591962412 ) ) ;
#30509=CARTESIAN_POINT ( 'NONE',  ( 9.428000818238999159, -5.131870447930000800, -8.096031607030200306 ) ) ;
#30538=CARTESIAN_POINT ( 'NONE',  ( 11.52166954483529793, -3.437903757373499847, -6.632714178206799538 ) ) ;
#30539=CARTESIAN_POINT ( 'NONE',  ( 11.59999999999999964, -2.820501972398000046, -7.174999999999999822 ) ) ;
#30540=CARTESIAN_POINT ( 'NONE',  ( 9.075651506909604649, -2.765563590215046830, -7.567790861611047859 ) ) ;
#30625=VERTEX_POINT ( 'NONE', #62434 ) ;
#30632=CARTESIAN_POINT ( 'NONE',  ( 8.599999952505998024, -4.000000000000000000, -8.249999993641800700 ) ) ;
#30635=CARTESIAN_POINT ( 'NONE',  ( 9.404346873515669003, -5.250000000000000888, -7.663624617374465764 ) ) ;
#30690=CYLINDRICAL_SURFACE ( 'NONE', #65189, 1.250000000000000222 ) ;
#30716=CARTESIAN_POINT ( 'NONE',  ( 11.41256651104150066, -3.901000349726440053, -6.501426055769400136 ) ) ;
#30755=CARTESIAN_POINT ( 'NONE',  ( 11.43718179236249988, -4.209680326224799707, -6.518682001772900136 ) ) ;
#30756=ORIENTED_EDGE ( 'NONE', *, *, #27814, .F. ) ;
#30771=CARTESIAN_POINT ( 'NONE',  ( 10.57435795695566583, -2.750000000000000000, -7.807440182398264206 ) ) ;
#30798=CARTESIAN_POINT ( 'NONE',  ( 9.277558426223626142, -3.641115516887601267, -8.297956262399157623 ) ) ;
#30802=CARTESIAN_POINT ( 'NONE',  ( 10.70287750876920008, -4.469200303112399908, -8.228113772635300194 ) ) ;
#30804=ORIENTED_EDGE ( 'NONE', *, *, #2139, .F. ) ;
#30823=CARTESIAN_POINT ( 'NONE',  ( 10.70851354018270207, -3.836375382625528019, -6.250000000000001776 ) ) ;
#30840=VERTEX_POINT ( 'NONE', #25128 ) ;
#30851=ORIENTED_EDGE ( 'NONE', *, *, #16746, .F. ) ;
#30853=CARTESIAN_POINT ( 'NONE',  ( 8.845430433046999497, -5.088604610742000212, -6.828193190755800224 ) ) ;
#30892=ORIENTED_EDGE ( 'NONE', *, *, #2910, .T. ) ;
#30987=CARTESIAN_POINT ( 'NONE',  ( 9.477263540182331525, -4.629523725463626782, -8.592232985442821658 ) ) ;
#30990=CARTESIAN_POINT ( 'NONE',  ( 10.65413259636999932, -4.783377755405500587, -7.926858177843299380 ) ) ;
#31062=VECTOR ( 'NONE', #57322, 1000.000000000000000 ) ;
#31069=CARTESIAN_POINT ( 'NONE',  ( 11.28949010443639978, -2.999324937259999935, -7.574834962826040297 ) ) ;
#31089=CARTESIAN_POINT ( 'NONE',  ( 9.728988259786000015, -4.113440707072600233, -8.359557531806398600 ) ) ;
#31109=CARTESIAN_POINT ( 'NONE',  ( 11.26072066707849828, -3.023932655881500065, -6.909591111168198907 ) ) ;
#31111=CARTESIAN_POINT ( 'NONE',  ( 10.10478570706233370, -2.868293641868291388, -8.113400509224881318 ) ) ;
#31151=CARTESIAN_POINT ( 'NONE',  ( 9.181310023244000362, -3.426978632899654542, -6.377665258770703005 ) ) ;
#31157=CARTESIAN_POINT ( 'NONE',  ( 9.657495633957626779, -4.774169056067385952, -7.907669647568630111 ) ) ;
#31162=CARTESIAN_POINT ( 'NONE',  ( 10.32949413291699869, -3.087070836781100169, -7.083453279150199400 ) ) ;
#31176=CARTESIAN_POINT ( 'NONE',  ( 10.34091290906799898, -4.722468360609500593, -8.384179803770500428 ) ) ;
#31179=CARTESIAN_POINT ( 'NONE',  ( 10.80226354018299872, -5.092232985442821658, -6.870476274536374994 ) ) ;
#31207=CARTESIAN_POINT ( 'NONE',  ( 8.997405316140000053, -4.271593136661399726, -8.750048621292000561 ) ) ;
#31213=CARTESIAN_POINT ( 'NONE',  ( 8.710288521113000115, -4.352953559891299840, -8.284550957747498501 ) ) ;
#31232=CARTESIAN_POINT ( 'NONE',  ( 10.37199293566600034, -3.366612813978900220, -8.276990458557699881 ) ) ;
#31280=CARTESIAN_POINT ( 'NONE',  ( 9.864633995697998259, -3.138280386550500012, -7.595641268826199166 ) ) ;
#31309=CARTESIAN_POINT ( 'NONE',  ( 9.510596873516666605, -3.370476274536376771, -8.592232985442825210 ) ) ;
#31329=CARTESIAN_POINT ( 'NONE',  ( 10.82035090130999855, -3.241273085157000189, -7.969278253227299658 ) ) ;
#31333=CARTESIAN_POINT ( 'NONE',  ( 11.30671024775549149, -3.379344054882541304, -8.119376818724932221 ) ) ;
#31342=CARTESIAN_POINT ( 'NONE',  ( 11.59999999999999964, -2.820501972398000046, -7.174999999999999822 ) ) ;
#31406=CARTESIAN_POINT ( 'NONE',  ( 10.89979975933730039, -3.180925410802600162, -7.218192605361100078 ) ) ;
#31411=ORIENTED_EDGE ( 'NONE', *, *, #64786, .F. ) ;
#31415=B_SPLINE_CURVE_WITH_KNOTS ( 'NONE', 3,
 ( #5637, #22754, #48294, #44103, #54925, #21378, #42711, #64016, #16137, #58782 ),
 .UNSPECIFIED., .F., .F.,
 ( 4, 2, 2, 2, 4 ),
 ( 0.3934091950370091628, 0.5450568962777566639, 0.6967045975185042206, 0.8483522987592517772, 1.000000000000000000 ),
 .UNSPECIFIED. ) ;
#31426=CARTESIAN_POINT ( 'NONE',  ( 8.715822372493999382, -4.249211653873900651, -8.315254653915399530 ) ) ;
#31443=CARTESIAN_POINT ( 'NONE',  ( 10.86687616594229944, -4.344946439135400240, -6.412662853391999818 ) ) ;
#31465=ORIENTED_EDGE ( 'NONE', *, *, #52580, .F. ) ;
#31492=CARTESIAN_POINT ( 'NONE',  ( 11.14179841651039915, -4.353306409735099969, -8.439215328713499886 ) ) ;
#31499=CARTESIAN_POINT ( 'NONE',  ( 10.38351354018329253, -5.249999999999998224, -7.336375382625530683 ) ) ;
#31507=CARTESIAN_POINT ( 'NONE',  ( 10.46755864497999866, -3.101067942814400347, -8.204026508301600629 ) ) ;
#31525=CARTESIAN_POINT ( 'NONE',  ( 11.13220574173980992, -2.863826994586552654, -6.911917091190554530 ) ) ;
#31539=ORIENTED_EDGE ( 'NONE', *, *, #58744, .F. ) ;
#31541=CARTESIAN_POINT ( 'NONE',  ( 8.566809814040999171, -3.217492037304399588, -8.511961036725999463 ) ) ;
#31547=CARTESIAN_POINT ( 'NONE',  ( 8.789886373836322875, -3.999992178805580334, -8.439846342473931173 ) ) ;
#31563=DIRECTION ( 'NONE',  ( 0.000000000000000000, 0.000000000000000000, 1.000000000000000000 ) ) ;
#31564=CARTESIAN_POINT ( 'NONE',  ( 10.74379975933729980, -2.921317947059999920, -7.128873141726999485 ) ) ;
#31569=PLANE ( 'NONE',  #9890 ) ;
#31570=CARTESIAN_POINT ( 'NONE',  ( 9.873096873515667227, -5.217465845835394411, -7.172815144550898303 ) ) ;
#31584=CARTESIAN_POINT ( 'NONE',  ( 10.89393020684959978, -5.250000000000000000, -7.500000000000000000 ) ) ;
#31620=CARTESIAN_POINT ( 'NONE',  ( 9.434038493598999153, -3.372531419565699906, -6.901676404381399621 ) ) ;
#31634=CARTESIAN_POINT ( 'NONE',  ( 10.90346005378009941, -3.213042707518099839, -7.079777642108599167 ) ) ;
#31641=CARTESIAN_POINT ( 'NONE',  ( 8.755786719645998417, -4.065290607273509771, -8.402920843186199917 ) ) ;
#31650=CARTESIAN_POINT ( 'NONE',  ( 9.416846873516664829, -4.768183399968644487, -8.499583552997725278 ) ) ;
#31655=ADVANCED_FACE ( 'NONE', ( #41862 ), #30690, .T. ) ;
#31669=CARTESIAN_POINT ( 'NONE',  ( 9.633513540182331525, -2.750000000000000000, -7.663624617374467540 ) ) ;
#31698=ORIENTED_EDGE ( 'NONE', *, *, #4863, .F. ) ;
#31722=CARTESIAN_POINT ( 'NONE',  ( 10.77222057153667656, -3.695719232113590547, -8.319452754344771606 ) ) ;
#31753=CARTESIAN_POINT ( 'NONE',  ( 10.65364694612719809, -4.804498860841600383, -7.821061011719899980 ) ) ;
#31771=CARTESIAN_POINT ( 'NONE',  ( 9.349051052051999378, -3.149129950522900234, -7.666517576877299511 ) ) ;
#31775=MECHANICAL_DESIGN_GEOMETRIC_PRESENTATION_REPRESENTATION('',(#472),#1625);
#31788=CARTESIAN_POINT ( 'NONE',  ( 11.13764426047339917, -3.386171819220400003, -8.461511872390000022 ) ) ;
#31839=CARTESIAN_POINT ( 'NONE',  ( 10.42795525820099911, -4.094749303624469761, -6.501013802764199490 ) ) ;
#31845=CARTESIAN_POINT ( 'NONE',  ( 10.32101354018304207, -4.768183399968640934, -6.500416447002272946 ) ) ;
#31855=CARTESIAN_POINT ( 'NONE',  ( 9.659038493598998798, -3.074215132699300135, -6.617216466537199970 ) ) ;
#31891=CARTESIAN_POINT ( 'NONE',  ( 9.174709346416998201, -2.844451673749999632, -6.951281079990299538 ) ) ;
#31910=CARTESIAN_POINT ( 'NONE',  ( 10.62072335273219892, -3.602909566644000083, -8.569396700949999612 ) ) ;
#31916=CARTESIAN_POINT ( 'NONE',  ( 10.65413259636999932, -4.783377755405500587, -7.926858177843299380 ) ) ;
#31954=B_SPLINE_CURVE_WITH_KNOTS ( 'NONE', 3,
 ( #5461, #14581, #68385, #20505 ),
 .UNSPECIFIED., .F., .F.,
 ( 4, 4 ),
 ( 0.000000000000000000, 1.000000000000000000 ),
 .UNSPECIFIED. ) ;
#31957=CARTESIAN_POINT ( 'NONE',  ( 11.36749010443639918, -3.136214309321499805, -7.564597762509089662 ) ) ;
#31971=CARTESIAN_POINT ( 'NONE',  ( 9.155417874594000693, -4.797903641662700558, -7.839201596587598964 ) ) ;
#31985=CARTESIAN_POINT ( 'NONE',  ( 11.60988784977536348, -4.851105903694400645, -7.451365240271489832 ) ) ;
#31992=MANIFOLD_SOLID_BREP ( 'Stock-MAS-678-1', #53734 ) ;
#31994=CARTESIAN_POINT ( 'NONE',  ( 8.790860954911998704, -3.902433532469449684, -8.421893466755800972 ) ) ;
#32004=CARTESIAN_POINT ( 'NONE',  ( 9.479346873516668381, -3.836375382625532904, -8.749999999999998224 ) ) ;
#32062=CARTESIAN_POINT ( 'NONE',  ( 10.99664311227126312, -3.555960431980461411, -8.706333095531745059 ) ) ;
#32084=DIRECTION ( 'NONE',  ( -1.000000000000000000, 0.000000000000000000, 0.000000000000000000 ) ) ;
#32091=CARTESIAN_POINT ( 'NONE',  ( 9.373082992855460205, -5.217431357650287538, -7.172827875665086061 ) ) ;
#32100=CARTESIAN_POINT ( 'NONE',  ( 11.31410538575739899, -3.024036709177600368, -7.266662245194900116 ) ) ;
#32118=CARTESIAN_POINT ( 'NONE',  ( 11.52531641787287775, -4.339035680702311382, -6.691293037684439504 ) ) ;
#32136=ADVANCED_FACE ( 'NONE', ( #66545 ), #8171, .T. ) ;
#32139=CARTESIAN_POINT ( 'NONE',  ( 10.81764560330029923, -3.650429500487800460, -6.414140625063999401 ) ) ;
#32187=CARTESIAN_POINT ( 'NONE',  ( 10.64949279009019989, -4.260984538213099526, -8.468936491037499792 ) ) ;
#32200=B_SPLINE_CURVE_WITH_KNOTS ( 'NONE', 3,
 ( #41667, #31525, #64008, #16125, #20338, #37451, #47950, #68915, #52848, #62971 ),
 .UNSPECIFIED., .F., .F.,
 ( 4, 2, 2, 2, 4 ),
 ( 0.000000000000000000, 0.2500000000000001665, 0.5000000000000003331, 0.7500000000000001110, 1.000000000000000000 ),
 .UNSPECIFIED. ) ;
#32202=CARTESIAN_POINT ( 'NONE',  ( 10.04184687351587613, -3.000416447002275611, -8.268183399968640046 ) ) ;
#32205=CARTESIAN_POINT ( 'NONE',  ( 10.18692546752099837, -5.002009261081000524, -7.430575645513339822 ) ) ;
#32239=CARTESIAN_POINT ( 'NONE',  ( 11.28627509987130040, -4.272452942476324900, -6.250000000000000000 ) ) ;
#32258=CARTESIAN_POINT ( 'NONE',  ( 10.32533997688000049, -3.756890902898200046, -6.385465081946999355 ) ) ;
#32314=CARTESIAN_POINT ( 'NONE',  ( 9.560684229509998744, -4.611171355610000688, -6.885038603985500494 ) ) ;
#32329=CARTESIAN_POINT ( 'NONE',  ( 11.02812378248509795, -4.416893162838900544, -6.711274001288999536 ) ) ;
#32403=FACE_OUTER_BOUND ( 'NONE', #12299, .T. ) ;
#32440=CARTESIAN_POINT ( 'NONE',  ( 10.35410941423799791, -3.257202320419700037, -6.825313060354999628 ) ) ;
#32446=CARTESIAN_POINT ( 'NONE',  ( 11.64122412107036908, -3.937930136014310190, -6.326756392227999015 ) ) ;
#32476=CARTESIAN_POINT ( 'NONE',  ( 10.49764694612699856, -5.059486515935999407, -7.922821994243300914 ) ) ;
#32523=CARTESIAN_POINT ( 'NONE',  ( 10.28026357027499849, -3.014700852776899698, -7.690095141806899903 ) ) ;
#32540=CARTESIAN_POINT ( 'NONE',  ( 9.984292290062997566, -3.131390070940299974, -6.995659746333000584 ) ) ;
#32591=CARTESIAN_POINT ( 'NONE',  ( 11.26072066707849828, -3.023932655881500065, -6.909591111168198907 ) ) ;
#32604=ADVANCED_FACE ( 'NONE', ( #51182 ), #45931, .T. ) ;
#32615=DIRECTION ( 'NONE',  ( -1.000000000000000000, 0.000000000000000000, -3.164702532202999971E-14 ) ) ;
#32649=B_SPLINE_CURVE_WITH_KNOTS ( 'NONE', 3,
 ( #59238, #5753, #27436, #29444, #55996, #6442, #50750, #27095, #8100, #22522, #49099, #28127, #48410, #48758, #516, #64470, #43164, #16594 ),
 .UNSPECIFIED., .F., .F.,
 ( 4, 2, 2, 2, 2, 2, 2, 2, 4 ),
 ( 0.000000000000000000, 0.1250000000000003331, 0.2500000000000006661, 0.3750000000000009992, 0.5000000000000013323, 0.6250000000000009992, 0.7500000000000006661, 0.8750000000000003331, 1.000000000000000000 ),
 .UNSPECIFIED. ) ;
#32650=CARTESIAN_POINT ( 'NONE',  ( 9.204063610504999104, -3.588011994494999968, -8.416028484082099581 ) ) ;
#32660=CARTESIAN_POINT ( 'NONE',  ( 10.99999975383417627, -5.062986770486452848, -7.366608021396839234 ) ) ;
#32666=CARTESIAN_POINT ( 'NONE',  ( 11.31389666366019853, -4.045876550911099656, -8.532487796751999198 ) ) ;
#32754=ORIENTED_EDGE ( 'NONE', *, *, #42441, .T. ) ;
#32783=CARTESIAN_POINT ( 'NONE',  ( 11.65456516821461008, -3.197083038490000195, -8.310318115935698913 ) ) ;
#32787=CARTESIAN_POINT ( 'NONE',  ( 10.80502344389999791, -5.125258734743999511, -6.817099149379099110 ) ) ;
#32793=EDGE_CURVE ( 'NONE', #60220, #43301, #36651, .T. ) ;
#32815=CARTESIAN_POINT ( 'NONE',  ( 10.29657053952199952, -4.502253688815499366, -6.324815923923999605 ) ) ;
#32857=VERTEX_POINT ( 'NONE', #5092 ) ;
#32867=CARTESIAN_POINT ( 'NONE',  ( 10.62072335273219892, -3.602909566644000083, -8.569396700949999612 ) ) ;
#32883=CARTESIAN_POINT ( 'NONE',  ( 9.832317406968998696, -3.813190776280700245, -8.486886322867700727 ) ) ;
#32935=CARTESIAN_POINT ( 'NONE',  ( 11.40425819896749893, -5.255890247626999745, -7.736761623643599428 ) ) ;
#32995=CARTESIAN_POINT ( 'NONE',  ( 9.609329965421999020, -4.697624103824200148, -8.222608407156599242 ) ) ;
#33008=CARTESIAN_POINT ( 'NONE',  ( 10.69057802013490033, -5.033226574983999946, -7.475947032624040034 ) ) ;
#33025=CARTESIAN_POINT ( 'NONE',  ( 10.72191429142990060, -3.974927396630719922, -6.183971186511000084 ) ) ;
#33050=CARTESIAN_POINT ( 'NONE',  ( 10.19095058442699830, -3.492264136285500253, -6.325866838823999139 ) ) ;
#33065=LINE ( 'NONE', #28520, #42684 ) ;
#33070=B_SPLINE_CURVE_WITH_KNOTS ( 'NONE', 3,
 ( #68430, #63183, #20553, #52710, #959, #28217, #6183, #27181, #1299, #64564, #43613, #6881, #22960, #33119, #261, #32091, #15991, #59680 ),
 .UNSPECIFIED., .F., .F.,
 ( 4, 2, 2, 2, 2, 2, 2, 2, 4 ),
 ( 0.1494581667962512628, 0.2557758959467200111, 0.3620936250971887316, 0.4684113542476574521, 0.5747290833981262281, 0.6810468125485945601, 0.7873645416990631141, 0.8936822708495314460, 1.000000000000000000 ),
 .UNSPECIFIED. ) ;
#33117=FACE_OUTER_BOUND ( 'NONE', #58985, .T. ) ;
#33119=CARTESIAN_POINT ( 'NONE',  ( 9.341834235717470847, -4.999591705763744898, -6.731799792051353037 ) ) ;
#33130=CARTESIAN_POINT ( 'NONE',  ( 11.35918179236250047, -4.238363971154499588, -6.384440618559000136 ) ) ;
#33134=CARTESIAN_POINT ( 'NONE',  ( 11.01790547754519878, -2.825704134258000266, -7.537269019642879542 ) ) ;
#33135=ORIENTED_EDGE ( 'NONE', *, *, #57177, .T. ) ;
#33163=CARTESIAN_POINT ( 'NONE',  ( 10.22687885159599830, -2.867290578374000365, -7.364871923548499844 ) ) ;
#33177=ORIENTED_EDGE ( 'NONE', *, *, #6375, .T. ) ;
#33214=CARTESIAN_POINT ( 'NONE',  ( 11.52733460557258915, -3.793662715184400014, -8.761245990815998752 ) ) ;
#33232=CARTESIAN_POINT ( 'NONE',  ( 8.998468108405997867, -2.901397043998999781, -7.811136554427399403 ) ) ;
#33249=CARTESIAN_POINT ( 'NONE',  ( 11.85159063708299954, -3.174974693948799942, -7.731961446576300467 ) ) ;
#33285=CARTESIAN_POINT ( 'NONE',  ( 10.96118313518939935, -4.792748567750200195, -8.502430091786999711 ) ) ;
#33289=CARTESIAN_POINT ( 'NONE',  ( 9.643930206848999376, -2.750000000000000000, -7.500000000000000000 ) ) ;
#33346=CARTESIAN_POINT ( 'NONE',  ( 9.634659112603999986, -4.436443689698799986, -8.404632083253700259 ) ) ;
#33367=SURFACE_STYLE_USAGE ( .BOTH. , #65507 ) ;
#33374=CARTESIAN_POINT ( 'NONE',  ( 11.46989666366029859, -4.058428102321880004, -8.814970315645998866 ) ) ;
#33377=FACE_OUTER_BOUND ( 'NONE', #20972, .T. ) ;
#33401=CARTESIAN_POINT ( 'NONE',  ( 9.937659112603999034, -4.555852086785099786, -8.652134039551000910 ) ) ;
#33476=CARTESIAN_POINT ( 'NONE',  ( 11.67918044953561996, -2.988516238873000219, -8.027436060358800418 ) ) ;
#33480=CARTESIAN_POINT ( 'NONE',  ( 11.22056920625029974, -3.952687217764870198, -6.184582852561999466 ) ) ;
#33511=CARTESIAN_POINT ( 'NONE',  ( 11.10887482311539998, -2.815046254222000055, -7.978749413531599721 ) ) ;
#33559=CARTESIAN_POINT ( 'NONE',  ( 11.35918179236250047, -4.238363971154499588, -6.384440618559000136 ) ) ;
#33576=CARTESIAN_POINT ( 'NONE',  ( 9.682355082327998019, -4.511005581663400044, -6.478918346312998899 ) ) ;
#33582=ORIENTED_EDGE ( 'NONE', *, *, #43714, .T. ) ;
#33595=CARTESIAN_POINT ( 'NONE',  ( 11.34287482311539996, -3.196874704906699893, -7.824481664695199790 ) ) ;
#33644=CARTESIAN_POINT ( 'NONE',  ( 11.63825819896753977, -4.851203879749700576, -7.660469764776300039 ) ) ;
#33692=CARTESIAN_POINT ( 'NONE',  ( 9.153405316139998860, -4.213249376011100722, -8.481512610189300361 ) ) ;
#33693=CARTESIAN_POINT ( 'NONE',  ( 9.708513540183332680, -3.836375382625528019, -6.250000000000001776 ) ) ;
#33707=CARTESIAN_POINT ( 'NONE',  ( 11.00000000000000000, -5.058572498595999889, -7.825000000000000178 ) ) ;
#33722=CARTESIAN_POINT ( 'NONE',  ( 11.22056920625029974, -3.952687217764870198, -6.184582852561999466 ) ) ;
#33820=CARTESIAN_POINT ( 'NONE',  ( 8.837278925393345475, -3.116678102649797832, -6.987098574663185069 ) ) ;
#33827=CARTESIAN_POINT ( 'NONE',  ( 11.68277869730536977, -4.531392946702499813, -6.452143920160000157 ) ) ;
#33856=CARTESIAN_POINT ( 'NONE',  ( 10.78887616594230003, -4.386455737425299262, -6.281817606595999415 ) ) ;
#33861=FACE_OUTER_BOUND ( 'NONE', #24500, .T. ) ;
#33908=CARTESIAN_POINT ( 'NONE',  ( 11.08841369783139896, -4.057552111898620417, -8.639288317626999003 ) ) ;
#33923=CARTESIAN_POINT ( 'NONE',  ( 9.021784697134998865, -3.454948069423500190, -6.656340890368899643 ) ) ;
#33933=LINE ( 'NONE', #22391, #45038 ) ;
#33942=CARTESIAN_POINT ( 'NONE',  ( 10.82595391537419971, -3.283439621430300104, -7.986661909549199301 ) ) ;
#33953=EDGE_LOOP ( 'NONE', ( #4405, #41919, #55214 ) ) ;
#33977=CARTESIAN_POINT ( 'NONE',  ( 10.83810672858429847, -5.021298157087000114, -6.731711997412900494 ) ) ;
#34043=CARTESIAN_POINT ( 'NONE',  ( 10.03992546752099990, -5.002009261081000524, -7.430575645513339822 ) ) ;
#34055=DIRECTION ( 'NONE',  ( 0.000000000000000000, 1.000000000000000000, 0.000000000000000000 ) ) ;
#34063=CARTESIAN_POINT ( 'NONE',  ( 11.46021572556888657, -5.045751188959975764, -7.175002613693187925 ) ) ;
#34133=DIRECTION ( 'NONE',  ( 0.000000000000000000, 1.000000000000000000, 0.000000000000000000 ) ) ;
#34141=CARTESIAN_POINT ( 'NONE',  ( 10.57529832096847677, -4.746004694577873551, -7.044405226132214537 ) ) ;
#34171=CARTESIAN_POINT ( 'NONE',  ( 10.89324174884020024, -4.032306468273969990, -8.674442868902998427 ) ) ;
#34175=AXIS2_PLACEMENT_3D ( 'NONE', #24989, #62392, #14507 ) ;
#34191=CARTESIAN_POINT ( 'NONE',  ( 11.04752711762115780, -2.837609288610280167, -7.824990536777686856 ) ) ;
#34203=CARTESIAN_POINT ( 'NONE',  ( 11.18272066707849888, -2.906477115133000222, -6.838543969064300398 ) ) ;
#34224=CARTESIAN_POINT ( 'NONE',  ( 11.63611496860034933, -2.828587461987000395, -6.899705789500199415 ) ) ;
#34254=CARTESIAN_POINT ( 'NONE',  ( 11.16225954179439839, -3.122605388210700106, -8.229019074832200076 ) ) ;
#34273=CARTESIAN_POINT ( 'NONE',  ( 8.793822372493998785, -4.288705740401799638, -8.444453017408701356 ) ) ;
#34289=CARTESIAN_POINT ( 'NONE',  ( 11.56441235500451015, -4.638700978900200056, -6.914884925939399629 ) ) ;
#34314=CARTESIAN_POINT ( 'NONE',  ( 11.14975833414749928, -4.796537143354000499, -7.825000000000000178 ) ) ;
#34327=CARTESIAN_POINT ( 'NONE',  ( 10.14887885159599890, -2.730985436695000157, -7.348611220446799486 ) ) ;
#34389=CARTESIAN_POINT ( 'NONE',  ( 8.619480666858999385, -3.619299191678599925, -8.576476893896000320 ) ) ;
#34404=CYLINDRICAL_SURFACE ( 'NONE', #44392, 1.250000000000000222 ) ;
#34447=CARTESIAN_POINT ( 'NONE',  ( 10.16562143724499911, -3.150324864944999970, -6.543738240676099771 ) ) ;
#34496=CARTESIAN_POINT ( 'NONE',  ( 10.42760663304247615, -3.352948950021445995, -6.912280214781111098 ) ) ;
#34526=CARTESIAN_POINT ( 'NONE',  ( 10.60746886766490071, -4.498335456194499926, -6.594573315824700188 ) ) ;
#34544=EDGE_CURVE ( 'NONE', #55747, #10029, #33933, .T. ) ;
#34559=CARTESIAN_POINT ( 'NONE',  ( 10.34588779216199939, -3.198058499272899979, -7.789199634454999632 ) ) ;
#34573=CARTESIAN_POINT ( 'NONE',  ( 10.44999293566599974, -3.279967330949900450, -8.383280442119700027 ) ) ;
#34606=CARTESIAN_POINT ( 'NONE',  ( 11.09672200990539892, -4.817867935977999672, -7.214709569664399247 ) ) ;
#34623=CARTESIAN_POINT ( 'NONE',  ( 9.804975701332999449, -3.363922674822000136, -8.089163458558500608 ) ) ;
#34640=CARTESIAN_POINT ( 'NONE',  ( 11.11718313518939816, -4.622449961306399402, -8.287087605365499599 ) ) ;
#34686=CARTESIAN_POINT ( 'NONE',  ( 11.58487348028854846, -4.882707455860599843, -7.977261354519500358 ) ) ;
#34725=CARTESIAN_POINT ( 'NONE',  ( 10.87309687351627652, -5.217465845835394411, -7.172815144550898303 ) ) ;
#34730=CARTESIAN_POINT ( 'NONE',  ( 10.01258376188599897, -4.962881317320600338, -8.113672563022399586 ) ) ;
#34734=CARTESIAN_POINT ( 'NONE',  ( 8.599999999999999645, -4.000000000000000000, -7.500000000000000000 ) ) ;
#34758=CARTESIAN_POINT ( 'NONE',  ( 11.51656039236534923, -2.826501801118000312, -7.557111631074219460 ) ) ;
#34761=DIRECTION ( 'NONE',  ( -1.000000000000000000, 0.000000000000000000, 0.000000000000000000 ) ) ;
#34764=CARTESIAN_POINT ( 'NONE',  ( 11.59999999999999964, -4.000000000000000000, -7.500000000000000000 ) ) ;
#34784=CARTESIAN_POINT ( 'NONE',  ( 9.431076168958000494, -4.649151400100800302, -8.602264418015000302 ) ) ;
#34831=EDGE_CURVE ( 'NONE', #30840, #47368, #7419, .T. ) ;
#34842=CARTESIAN_POINT ( 'NONE',  ( 9.354346873516664829, -5.250000000000000000, -7.663624617374463099 ) ) ;
#34854=CARTESIAN_POINT ( 'NONE',  ( 9.909870477708999204, -5.250000000000000888, -7.750389189149368363 ) ) ;
#34859=CARTESIAN_POINT ( 'NONE',  ( 11.23589666366019912, -4.039600775206940497, -8.391246537305399045 ) ) ;
#34880=EDGE_CURVE ( 'NONE', #30625, #6314, #8307, .T. ) ;
#34883=DIRECTION ( 'NONE',  ( -1.000000000000000000, 0.000000000000000000, 2.886579864060000134E-14 ) ) ;
#34911=CARTESIAN_POINT ( 'NONE',  ( 11.48011496860029901, -3.080230834057799960, -7.028661263734299780 ) ) ;
#34944=CARTESIAN_POINT ( 'NONE',  ( 11.44133594839949986, -3.430493414882899827, -6.847343244997600387 ) ) ;
#34945=CARTESIAN_POINT ( 'NONE',  ( 11.15810538575740019, -2.757018958839999812, -7.202822423614300362 ) ) ;
#34959=ORIENTED_EDGE ( 'NONE', *, *, #16906, .T. ) ;
#34961=CARTESIAN_POINT ( 'NONE',  ( 9.427051052051998781, -3.014287398677499841, -7.692906630067099627 ) ) ;
#34980=CARTESIAN_POINT ( 'NONE',  ( 11.33872066707849768, -3.141388196630700236, -6.980638253271099103 ) ) ;
#35028=EDGE_CURVE ( 'NONE', #10153, #35633, #65122, .T. ) ;
#35030=CARTESIAN_POINT ( 'NONE',  ( 11.53564291764652872, -4.995889373412399692, -7.376893506359599506 ) ) ;
#35077=CARTESIAN_POINT ( 'NONE',  ( 8.670138961223999630, -3.053949131563199693, -8.139313957553699908 ) ) ;
#35105=CARTESIAN_POINT ( 'NONE',  ( 10.77368717260499942, -4.539928529895099985, -8.381256426168800289 ) ) ;
#35128=CARTESIAN_POINT ( 'NONE',  ( 9.960975701332998256, -3.162316589966200020, -8.275900091855099561 ) ) ;
#35196=VERTEX_POINT ( 'NONE', #6491 ) ;
#35207=CARTESIAN_POINT ( 'NONE',  ( 10.98146005378009882, -3.088328798999600000, -7.013182449205100255 ) ) ;
#35229=CARTESIAN_POINT ( 'NONE',  ( 11.37299956498129916, -5.207010770456999893, -7.174999999999999822 ) ) ;
#35240=CARTESIAN_POINT ( 'NONE',  ( 9.003442991499998271, -4.054579081944059915, -6.634708680083400090 ) ) ;
#35254=CARTESIAN_POINT ( 'NONE',  ( 11.51656039236534923, -2.826501801118000312, -7.557111631074219460 ) ) ;
#35287=CARTESIAN_POINT ( 'NONE',  ( 10.39503166480599994, -5.274847857784000560, -7.589885038193400213 ) ) ;
#35303=CARTESIAN_POINT ( 'NONE',  ( 9.275076168957998135, -4.509700402263200125, -8.365475476407400635 ) ) ;
#35320=CARTESIAN_POINT ( 'NONE',  ( 10.29262282008599882, -3.548418513060800361, -8.228386593078399258 ) ) ;
#35357=ORIENTED_EDGE ( 'NONE', *, *, #24503, .F. ) ;
#35369=CARTESIAN_POINT ( 'NONE',  ( 11.34287482311539996, -3.196874704906699893, -7.824481664695199790 ) ) ;
#35371=EDGE_CURVE ( 'NONE', #6018, #15621, #68277, .T. ) ;
#35414=CARTESIAN_POINT ( 'NONE',  ( 9.885938025973999288, -4.593629475532499562, -6.524634174392399899 ) ) ;
#35441=CARTESIAN_POINT ( 'NONE',  ( 10.48280513895999988, -3.096689368913399854, -6.997844089834400094 ) ) ;
#35442=CARTESIAN_POINT ( 'NONE',  ( 11.59999999999999609, -3.011522968892933250, -6.852161599766354527 ) ) ;
#35462=ORIENTED_EDGE ( 'NONE', *, *, #20177, .T. ) ;
#35497=AXIS2_PLACEMENT_3D ( 'NONE', #13740, #29838, #45895 ) ;
#35547=CARTESIAN_POINT ( 'NONE',  ( 10.39969598649000027, -3.111999510220800236, -8.028730309000598808 ) ) ;
#35597=CARTESIAN_POINT ( 'NONE',  ( 10.51414141025500015, -3.384226587288500010, -8.596754040696000132 ) ) ;
#35629=CARTESIAN_POINT ( 'NONE',  ( 11.61364291764652812, -4.859654669415900408, -7.393734108507599601 ) ) ;
#35630=CARTESIAN_POINT ( 'NONE',  ( 10.09964828895399869, -2.878385131502000149, -8.112615456209400833 ) ) ;
#35631=CARTESIAN_POINT ( 'NONE',  ( 11.59999999999999964, -2.792989229543000107, -7.825000000000000178 ) ) ;
#35632=EDGE_LOOP ( 'NONE', ( #5835, #26712, #13285, #7284, #52003, #46869 ) ) ;
#35633=VERTEX_POINT ( 'NONE', #17917 ) ;
#35646=CARTESIAN_POINT ( 'NONE',  ( 8.994442991499997930, -4.054579081944059915, -6.634708680083400090 ) ) ;
#35659=DIRECTION ( 'NONE',  ( -1.000000000000000000, 0.000000000000000000, -1.275169027325000072E-14 ) ) ;
#35661=CARTESIAN_POINT ( 'NONE',  ( 10.87103032197929942, -3.416314376401300201, -6.683751296690399357 ) ) ;
#35699=CARTESIAN_POINT ( 'NONE',  ( 9.099999931440999390, -2.753634353389999845, -7.404749409716440134 ) ) ;
#35704=CARTESIAN_POINT ( 'NONE',  ( 8.948279512853625661, -3.525202972512352595, -6.765085003841553757 ) ) ;
#35708=CARTESIAN_POINT ( 'NONE',  ( 10.55518582084299872, -4.566724035220099509, -6.844925608615599621 ) ) ;
#35713=CARTESIAN_POINT ( 'NONE',  ( 10.39393020684999946, -5.250000000000000000, -7.500000000000000000 ) ) ;
#35727=B_SPLINE_SURFACE_WITH_KNOTS ( 'NONE', 3, 3, ( 
 ( #15178, #33249, #49314, #44091, #18203, #23786, #45122, #5376, #54912, #49666, #55611, #12965, #39879, #34289, #2126, #50018, #23446, #1427, #17863, #2462, #28702, #31957, #33595, #60163, #26713, #11910, #7357, #1775, #38837, #54568, #60502, #6665, #18550, #66083, #130, #61196, #22742, #38484, #59807, #43739, #12267, #44442, #65035, #33942, #50363, #7712, #29052, #7015, #66429, #65740, #17152, #12611, #44783, #28350, #48027, #39526, #21447, #60850, #65389, #55263, #28005, #39179, #53274, #17511, #23093, #35320, #46834 ),
 ( #61537, #62219, #67115, #29398, #8400, #29745, #46492, #50707, #8741, #13317, #8056, #56638, #30086, #40898, #9411, #30755, #19578, #68140, #14338, #34980, #19918, #20257, #41243, #51048, #61879, #51726, #18895, #2804, #34640, #24130, #62555, #67798, #3149, #3485, #3821, #45465, #14677, #9078, #35661, #40221, #66779, #56297, #13652, #4168, #56976, #30415, #40550, #25159, #24480, #45803, #19224, #13995, #51389, #24821, #46147, #35993, #52062, #57309, #25505, #67453, #41583, #55951, #25847, #42618, #53452, #58344, #36339 ),
 ( #15703, #52761, #5205, #5547, #15362, #53790, #63586, #69176, #21287, #62893, #26887, #26544, #41927, #63926, #47523, #9759, #58011, #10112, #48202, #31109, #10447, #15013, #57653, #37032, #31788, #16037, #59039, #11141, #37369, #27227, #58689, #36688, #307, #48551, #21623, #31443, #42284, #32139, #68478, #52414, #4507, #47176, #42959, #64266, #4854, #53105, #16381, #20602, #37711, #10793, #32476, #63235, #26198, #68829, #20950, #5886, #654, #21967, #47869, #39095, #23360, #33163, #2378, #28260, #59722, #49579, #43306 ),
 ( #11824, #6229, #54132, #7276, #49231, #54480, #60077, #12181, #17065, #6581, #27569, #48897, #17777, #1002, #12525, #64613, #28615, #54827, #60420, #34203, #50276, #44699, #33511, #27921, #64951, #22314, #43656, #18120, #1340, #38397, #22656, #6926, #44354, #2040, #65655, #33856, #55172, #1688, #44000, #23005, #65307, #59375, #17422, #38750, #49929, #11476, #65995, #16720, #38050, #39439, #60759, #12876, #55521, #7623, #28969, #32815, #13908, #2721, #67366, #3738, #19490, #45380, #56207, #51304, #55866, #39789, #45036 ) ),
 .UNSPECIFIED., .F., .F., .F.,
 ( 4, 4 ),
 ( 4, 1, 1, 1, 1, 1, 1, 1, 1, 1, 1, 1, 1, 1, 1, 1, 1, 1, 1, 1, 1, 1, 1, 1, 1, 1, 1, 1, 1, 1, 1, 1, 1, 1, 1, 1, 1, 1, 1, 1, 1, 1, 1, 1, 1, 1, 1, 1, 1, 1, 1, 1, 1, 1, 1, 1, 1, 1, 1, 1, 1, 1, 1, 1, 4 ),
 ( -0.02000000000000000042, 1.020000000000000018 ),
 ( 0.008747244164287000176, 0.02453926110774999961, 0.04033127805120999970, 0.05612329499467000327, 0.07191531193812999989, 0.08770732888158999652, 0.1034993458251000087, 0.1192913627684999978, 0.1350833797120000179, 0.1508753966553999792, 0.1666674135988999994, 0.1824594305423999918, 0.1982514474858000086, 0.2140434644293000011, 0.2298354813727000179, 0.2456274983162000103, 0.2614195152596999749, 0.2772115322030999640, 0.2930035491465999842, 0.3087955660900000288, 0.3245875830334999934, 0.3403795999769999581, 0.3561716169204000026, 0.3719636338639000228, 0.3877556508073999875, 0.4035476677507999765, 0.4193396846942999967, 0.4351317016376999858, 0.4509237185811999504, 0.4667157355247000261, 0.4825077524681000152, 0.4982997694115999798, 0.5140917863550000799, 0.5298838032985000446, 0.5456758202420000092, 0.5614678371854000538, 0.5772598541289000185, 0.5930518710723000630, 0.6088438880158000277, 0.6246359049592999924, 0.6404279219027000369, 0.6562199388462000016, 0.6720119557896999662, 0.6878039727331000108, 0.7035959896765999755, 0.7193880066200000201, 0.7351800235634999847, 0.7509720405069999494, 0.7667640574504001050, 0.7825560743939000696, 0.7983480913373000032, 0.8141401082808000789, 0.8299321252243000435, 0.8457241421676999771, 0.8615161591112000528, 0.8773081760545999863, 0.8931001929981000620, 0.9088922099416000266, 0.9246842268849999602, 0.9404762438285000359, 0.9562682607720000005, 0.9720602777153999341, 0.9878522946589000098, 1.003644311601999961, 1.019436328545999970 ),
 .UNSPECIFIED. ) ;
#35754=CARTESIAN_POINT ( 'NONE',  ( 10.01057120343299900, -4.062009413492949861, -8.777708647662999297 ) ) ;
#35781=CARTESIAN_POINT ( 'NONE',  ( 10.97635090131019986, -3.000792947412299849, -8.118017011233499503 ) ) ;
#35782=CARTESIAN_POINT ( 'NONE',  ( 11.59999999999999964, -3.304217902137881691, -6.595854147058992645 ) ) ;
#35826=CARTESIAN_POINT ( 'NONE',  ( 11.12299956498149811, -2.792989229543000107, -7.825000000000000178 ) ) ;
#35946=CARTESIAN_POINT ( 'NONE',  ( 11.58457173739308743, -3.062774903199518839, -8.361882233189922076 ) ) ;
#35956=CARTESIAN_POINT ( 'NONE',  ( 11.60948876160955479, -4.695527826393099957, -8.223320049540498999 ) ) ;
#35957=CARTESIAN_POINT ( 'NONE',  ( 10.07503300763299947, -3.118110956362800223, -8.424978748982498544 ) ) ;
#35958=DIRECTION ( 'NONE',  ( 0.000000000000000000, 1.000000000000000000, 0.000000000000000000 ) ) ;
#35971=CARTESIAN_POINT ( 'NONE',  ( 11.39975833414730033, -3.203462856645999945, -7.174999999999999822 ) ) ;
#35974=CARTESIAN_POINT ( 'NONE',  ( 9.475696787962998968, -3.851113559088000127, -6.645868410478299459 ) ) ;
#35991=CARTESIAN_POINT ( 'NONE',  ( 10.64393020684969926, -2.750000000000000000, -7.500000000000000000 ) ) ;
#35993=CARTESIAN_POINT ( 'NONE',  ( 10.45257053952200010, -4.394359323863099576, -6.577269499510100204 ) ) ;
#36036=CARTESIAN_POINT ( 'NONE',  ( 9.708153928322625248, -4.380187932396833794, -8.288028809740389136 ) ) ;
#36040=CARTESIAN_POINT ( 'NONE',  ( 11.24441369783139777, -4.043700988887960257, -8.365094684940499903 ) ) ;
#36061=CARTESIAN_POINT ( 'NONE',  ( 10.59393020684899867, -2.750000000000000000, -7.500000000000000000 ) ) ;
#36075=CARTESIAN_POINT ( 'NONE',  ( 10.53521345716899837, -3.075109701058799772, -8.340879262988799780 ) ) ;
#36092=CARTESIAN_POINT ( 'NONE',  ( 10.06122949779699915, -3.290320231472799950, -8.564302809495998758 ) ) ;
#36119=CARTESIAN_POINT ( 'NONE',  ( 10.98656920625009903, -3.967932847735990531, -6.608450613814399688 ) ) ;
#36120=CARTESIAN_POINT ( 'NONE',  ( 11.60000000000000142, -3.927017550833200588, -6.447388989144585025 ) ) ;
#36198=B_SPLINE_CURVE_WITH_KNOTS ( 'NONE', 3,
 ( #4942, #52845, #26280, #47606, #68563, #46575 ),
 .UNSPECIFIED., .F., .F.,
 ( 4, 2, 4 ),
 ( 0.000000000000000000, 0.1967045975185045814, 0.3934091950370091628 ),
 .UNSPECIFIED. ) ;
#36224=CARTESIAN_POINT ( 'NONE',  ( 10.94501463001509833, -3.527519786474400121, -6.743262887067199784 ) ) ;
#36256=AXIS2_PLACEMENT_3D ( 'NONE', #23565, #34761, #66208 ) ;
#36297=CARTESIAN_POINT ( 'NONE',  ( 10.48133997687999930, -3.815400206859000054, -6.653701289769800020 ) ) ;
#36339=CARTESIAN_POINT ( 'NONE',  ( 10.20641772631199906, -3.568446272909699957, -8.388315195900499788 ) ) ;
#36382=CARTESIAN_POINT ( 'NONE',  ( 9.074925248765625341, -4.744576382809566617, -7.040502144637257764 ) ) ;
#36386=CARTESIAN_POINT ( 'NONE',  ( 11.06795257254739973, -4.963546614172099858, -7.780229861306499295 ) ) ;
#36403=CARTESIAN_POINT ( 'NONE',  ( 9.709696787963999043, -3.780328739572700325, -6.239790126677999815 ) ) ;
#36434=CARTESIAN_POINT ( 'NONE',  ( 9.276025935145998602, -4.185743043590700374, -6.234344474498000110 ) ) ;
#36490=VERTEX_POINT ( 'NONE', #48788 ) ;
#36513=CARTESIAN_POINT ( 'NONE',  ( 10.16657120343299958, -4.048688523195909994, -8.503230697164999796 ) ) ;
#36564=CARTESIAN_POINT ( 'NONE',  ( 9.623096873515669003, -2.782534154164605145, -7.827184855449101697 ) ) ;
#36567=CARTESIAN_POINT ( 'NONE',  ( 10.29399293566599916, -3.453258297007899991, -8.170700474995699736 ) ) ;
#36582=CARTESIAN_POINT ( 'NONE',  ( 10.59393020684899867, -2.750000000000000000, -7.500000000000000000 ) ) ;
#36588=CARTESIAN_POINT ( 'NONE',  ( 8.724507172011824352, -4.124235577930278396, -8.374507226493388856 ) ) ;
#36639=CARTESIAN_POINT ( 'NONE',  ( 11.49200216175158396, -4.419830582853482071, -8.702070774814039567 ) ) ;
#36649=CARTESIAN_POINT ( 'NONE',  ( 11.46179707368349909, -4.498457171163099844, -6.629085939160999530 ) ) ;
#36651=B_SPLINE_CURVE_WITH_KNOTS ( 'NONE', 3,
 ( #44100, #65399, #17518, #38847 ),
 .UNSPECIFIED., .F., .F.,
 ( 4, 4 ),
 ( 0.000000000000000000, 1.000000000000000000 ),
 .UNSPECIFIED. ) ;
#36655=ORIENTED_EDGE ( 'NONE', *, *, #21208, .F. ) ;
#36688=CARTESIAN_POINT ( 'NONE',  ( 10.96533729122639933, -5.140346530769000388, -7.470001566214039990 ) ) ;
#36741=CARTESIAN_POINT ( 'NONE',  ( 10.69872335273220010, -3.650693637952500126, -8.440710326446700051 ) ) ;
#36756=CARTESIAN_POINT ( 'NONE',  ( 10.36624205625100004, -4.409476560233800413, -8.565862728991998409 ) ) ;
#36786=CARTESIAN_POINT ( 'NONE',  ( 9.301355082327999568, -4.572497688003699601, -6.356045986629998978 ) ) ;
#36800=LINE ( 'NONE', #41010, #13068 ) ;
#36809=CARTESIAN_POINT ( 'NONE',  ( 11.21149010443640037, -2.862435565199000109, -7.585072163144589652 ) ) ;
#36815=CARTESIAN_POINT ( 'NONE',  ( 11.52677869730533011, -4.403502086956500250, -6.704332466833498927 ) ) ;
#36866=CARTESIAN_POINT ( 'NONE',  ( 8.800809814040999157, -3.469640109842400122, -8.185876144228299012 ) ) ;
#36867=EDGE_CURVE ( 'NONE', #42419, #26260, #68890, .T. ) ;
#36869=B_SPLINE_SURFACE_WITH_KNOTS ( 'NONE', 3, 3, ( 
 ( #66741, #56942, #13958, #55919, #61840, #40858, #30379, #8023, #51687, #39840, #3113, #35629, #3785, #25123, #2772, #9038, #66049, #61162, #34944, #46109, #18859, #8367, #24099, #67415, #18170, #13280, #19540, #29711, #39492, #14302, #60814, #12927, #34606, #29360, #50673, #19881, #15323, #67755, #47485, #68101, #31406, #25464, #46456, #20562, #15666, #41209, #47141, #20218, #5514, #69143, #31753, #10411, #68791, #41545, #26503, #58309, #41889, #36297, #16002, #62519, #14638, #4128, #63888, #42246, #37331, #9720, #20908 ),
 ( #10756, #57617, #53071, #63194, #46797, #9371, #21251, #5170, #35956, #47834, #57972, #63551, #57270, #68442, #36649, #14974, #30716, #42580, #52026, #58655, #32100, #31069, #62856, #52375, #10070, #36995, #53417, #4470, #25808, #52721, #4818, #26160, #28226, #48861, #273, #64230, #6546, #64577, #37675, #21587, #59005, #16687, #38716, #54445, #65272, #42925, #17386, #27194, #22622, #22282, #60035, #54097, #64917, #6193, #11442, #38015, #12148, #11105, #1307, #32440, #16347, #53756, #970, #11790, #43966, #49541, #59340 ),
 ( #48513, #26855, #33476, #32783, #48168, #5853, #622, #54791, #43623, #21931, #43269, #6890, #27536, #17031, #59689, #33130, #38364, #27888, #49200, #32591, #47982, #36809, #84, #37483, #11592, #37148, #59150, #64039, #26316, #10229, #22087, #11253, #6348, #53905, #58810, #43073, #58128, #21401, #42735, #15818, #31564, #772, #52883, #43432, #64726, #31910, #4982, #47644, #10914, #48320, #6005, #425, #37828, #42398, #16160, #26666, #54246, #32258, #20722, #68954, #27345, #53224, #21067, #42050, #63705, #5324, #16842 ),
 ( #48667, #58465, #38164, #53567, #59494, #5662, #27003, #21741, #64380, #16501, #32935, #10571, #47298, #68602, #15483, #63355, #60541, #2162, #55646, #55987, #54950, #2496, #44128, #60885, #65068, #23130, #55298, #7393, #33285, #18240, #28739, #23821, #45158, #33977, #50055, #65426, #49348, #50396, #28387, #23478, #39914, #27696, #66120, #54601, #17188, #49012, #44817, #38519, #7746, #22432, #66464, #39215, #18586, #39561, #61232, #59840, #11947, #6699, #28040, #1463, #13001, #34327, #22778, #1119, #43774, #17548, #13348 ) ),
 .UNSPECIFIED., .F., .F., .F.,
 ( 4, 4 ),
 ( 4, 1, 1, 1, 1, 1, 1, 1, 1, 1, 1, 1, 1, 1, 1, 1, 1, 1, 1, 1, 1, 1, 1, 1, 1, 1, 1, 1, 1, 1, 1, 1, 1, 1, 1, 1, 1, 1, 1, 1, 1, 1, 1, 1, 1, 1, 1, 1, 1, 1, 1, 1, 1, 1, 1, 1, 1, 1, 1, 1, 1, 1, 1, 1, 4 ),
 ( -0.02000000000000000042, 1.020000000000000018 ),
 ( 0.008747244164287000176, 0.02453926110774999961, 0.04033127805120999970, 0.05612329499467000327, 0.07191531193812999989, 0.08770732888158999652, 0.1034993458251000087, 0.1192913627684999978, 0.1350833797120000179, 0.1508753966553999792, 0.1666674135988999994, 0.1824594305423999918, 0.1982514474858000086, 0.2140434644293000011, 0.2298354813727000179, 0.2456274983162000103, 0.2614195152596999749, 0.2772115322030999640, 0.2930035491465999842, 0.3087955660900000288, 0.3245875830334999934, 0.3403795999769999581, 0.3561716169204000026, 0.3719636338639000228, 0.3877556508073999875, 0.4035476677507999765, 0.4193396846942999967, 0.4351317016376999858, 0.4509237185811999504, 0.4667157355247000261, 0.4825077524681000152, 0.4982997694115999798, 0.5140917863550000799, 0.5298838032985000446, 0.5456758202420000092, 0.5614678371854000538, 0.5772598541289000185, 0.5930518710723000630, 0.6088438880158000277, 0.6246359049592999924, 0.6404279219027000369, 0.6562199388462000016, 0.6720119557896999662, 0.6878039727331000108, 0.7035959896765999755, 0.7193880066200000201, 0.7351800235634999847, 0.7509720405069999494, 0.7667640574504001050, 0.7825560743939000696, 0.7983480913373000032, 0.8141401082808000789, 0.8299321252243000435, 0.8457241421676999771, 0.8615161591112000528, 0.8773081760545999863, 0.8931001929981000620, 0.9088922099416000266, 0.9246842268849999602, 0.9404762438285000359, 0.9562682607720000005, 0.9720602777153999341, 0.9878522946589000098, 1.003644311601999961, 1.019436328545999970 ),
 .UNSPECIFIED. ) ;
#36881=CARTESIAN_POINT ( 'NONE',  ( 10.56080513895999928, -2.973119161490000106, -6.929150654994399083 ) ) ;
#36888=CARTESIAN_POINT ( 'NONE',  ( 8.741501215035997419, -4.228777700933000538, -8.375893644236599656 ) ) ;
#36906=ORIENTED_EDGE ( 'NONE', *, *, #61403, .F. ) ;
#36966=CARTESIAN_POINT ( 'NONE',  ( 10.82145113417867677, -3.276884167680957027, -7.991114136793449951 ) ) ;
#36995=CARTESIAN_POINT ( 'NONE',  ( 11.19102897915239936, -3.743141152489600110, -8.470038342183499935 ) ) ;
#37016=CARTESIAN_POINT ( 'NONE',  ( 9.526355082327999213, -4.388021368982800041, -6.724663065681199647 ) ) ;
#37032=CARTESIAN_POINT ( 'NONE',  ( 11.16225954179439839, -3.122605388210700106, -8.229019074832200076 ) ) ;
#37033=ORIENTED_EDGE ( 'NONE', *, *, #27928, .T. ) ;
#37077=CARTESIAN_POINT ( 'NONE',  ( 8.821633776942626071, -3.275060658047592277, -7.989893149673591211 ) ) ;
#37081=CARTESIAN_POINT ( 'NONE',  ( 11.45764291764649911, -5.132124077409000229, -7.360052904210999891 ) ) ;
#37097=CARTESIAN_POINT ( 'NONE',  ( 10.18893802597399834, -4.593629475532499562, -6.524634174392399899 ) ) ;
#37127=CARTESIAN_POINT ( 'NONE',  ( 9.503988259786000370, -4.167373623506299474, -8.768215461831999846 ) ) ;
#37137=B_SPLINE_SURFACE_WITH_KNOTS ( 'NONE', 3, 3, ( 
 ( #22791, #29099, #17201, #6710, #6360, #50409, #1129, #45171, #16853, #1821, #33644, #38886, #38176, #22443, #65080, #38530, #1473, #11959, #8448, #9125, #67161, #29795, #35369, #30464, #62269, #52115, #36040, #30133, #40264, #46544, #40947, #13360, #24868, #24527, #19626, #25556, #57356, #67507, #18940, #3533, #51098, #61584, #67849, #9460, #3200, #46196, #66827, #56000, #30802, #51775, #19274, #14388, #57025, #19971, #35708, #3873, #25207, #41294, #51436, #13700, #40602, #62601, #56345, #8105, #14725, #61928, #2851 ),
 ( #14042, #45852, #4220, #56691, #8790, #66476, #18600, #39927, #61245, #34686, #29448, #35030, #50755, #24179, #45517, #5257, #4907, #13, #5936, #16431, #47916, #68531, #53155, #58061, #20653, #26936, #37760, #31492, #26596, #47228, #36386, #59085, #10845, #47576, #42665, #37417, #48249, #21336, #63972, #16087, #58738, #10499, #41979, #68882, #53501, #36741, #57703, #32187, #20999, #52463, #5591, #355, #63285, #11187, #58394, #9813, #31839, #42334, #21670, #43006, #31162, #64312, #32523, #63636, #62939, #26249, #53839 ),
 ( #46882, #10163, #68189, #15754, #20307, #15414, #41633, #15063, #52814, #4561, #25899, #37081, #54880, #23413, #44749, #33559, #704, #22017, #6982, #66050, #49632, #60471, #65707, #34254, #18171, #59425, #33908, #22709, #27279, #12578, #59773, #43364, #38100, #7325, #64664, #12928, #16768, #28666, #55225, #11523, #38803, #6278, #48601, #49283, #55576, #32867, #39493, #54181, #28309, #27622, #48948, #17477, #1055, #49982, #27972, #22367, #65358, #2094, #1737, #43706, #23056, #39145, #60815, #17829, #65001, #17116, #38450 ),
 ( #60127, #44407, #6634, #1393, #11875, #33214, #54534, #44053, #12234, #66396, #45431, #29361, #51688, #23753, #45089, #19191, #50674, #62520, #3786, #41210, #34945, #8708, #3114, #56259, #46457, #51013, #46110, #25124, #18860, #13621, #30052, #8024, #66742, #50329, #67756, #18519, #30380, #51354, #45771, #24445, #8368, #29712, #62181, #67078, #39841, #40187, #40514, #61503, #19541, #61841, #13959, #35287, #40859, #3446, #14639, #19882, #56601, #2773, #56943, #24783, #61163, #67417, #14303, #35630, #35957, #7676, #9039 ) ),
 .UNSPECIFIED., .F., .F., .F.,
 ( 4, 4 ),
 ( 4, 1, 1, 1, 1, 1, 1, 1, 1, 1, 1, 1, 1, 1, 1, 1, 1, 1, 1, 1, 1, 1, 1, 1, 1, 1, 1, 1, 1, 1, 1, 1, 1, 1, 1, 1, 1, 1, 1, 1, 1, 1, 1, 1, 1, 1, 1, 1, 1, 1, 1, 1, 1, 1, 1, 1, 1, 1, 1, 1, 1, 1, 1, 1, 4 ),
 ( -0.02000000000000000042, 1.020000000000000018 ),
 ( 0.008747244164287000176, 0.02453926110774999961, 0.04033127805120999970, 0.05612329499467000327, 0.07191531193812999989, 0.08770732888158999652, 0.1034993458251000087, 0.1192913627684999978, 0.1350833797120000179, 0.1508753966553999792, 0.1666674135988999994, 0.1824594305423999918, 0.1982514474858000086, 0.2140434644293000011, 0.2298354813727000179, 0.2456274983162000103, 0.2614195152596999749, 0.2772115322030999640, 0.2930035491465999842, 0.3087955660900000288, 0.3245875830334999934, 0.3403795999769999581, 0.3561716169204000026, 0.3719636338639000228, 0.3877556508073999875, 0.4035476677507999765, 0.4193396846942999967, 0.4351317016376999858, 0.4509237185811999504, 0.4667157355247000261, 0.4825077524681000152, 0.4982997694115999798, 0.5140917863550000799, 0.5298838032985000446, 0.5456758202420000092, 0.5614678371854000538, 0.5772598541289000185, 0.5930518710723000630, 0.6088438880158000277, 0.6246359049592999924, 0.6404279219027000369, 0.6562199388462000016, 0.6720119557896999662, 0.6878039727331000108, 0.7035959896765999755, 0.7193880066200000201, 0.7351800235634999847, 0.7509720405069999494, 0.7667640574504001050, 0.7825560743939000696, 0.7983480913373000032, 0.8141401082808000789, 0.8299321252243000435, 0.8457241421676999771, 0.8615161591112000528, 0.8773081760545999863, 0.8931001929981000620, 0.9088922099416000266, 0.9246842268849999602, 0.9404762438285000359, 0.9562682607720000005, 0.9720602777153999341, 0.9878522946589000098, 1.003644311601999961, 1.019436328545999970 ),
 .UNSPECIFIED. ) ;
#37140=CARTESIAN_POINT ( 'NONE',  ( 8.798455008774128672, -3.051544939223430397, -7.736326407956449103 ) ) ;
#37148=CARTESIAN_POINT ( 'NONE',  ( 11.11302897915239818, -3.708003626182200030, -8.602736702002999891 ) ) ;
#37153=CARTESIAN_POINT ( 'NONE',  ( 11.31900581613029821, -3.249313226592100534, -7.982035256002799173 ) ) ;
#37154=CARTESIAN_POINT ( 'NONE',  ( 9.758513540182331525, -3.836375382625526687, -6.250000000000000888 ) ) ;
#37186=ADVANCED_FACE ( 'NONE', ( #6484 ), #43906, .T. ) ;
#37204=CARTESIAN_POINT ( 'NONE',  ( 9.535355082327999554, -4.388021368982800041, -6.724663065681199647 ) ) ;
#37212=CARTESIAN_POINT ( 'NONE',  ( 11.00000000000000000, -5.058572498595999889, -7.825000000000000178 ) ) ;
#37217=CARTESIAN_POINT ( 'NONE',  ( 10.77368717260499942, -4.539928529895099985, -8.381256426168800289 ) ) ;
#37225=CARTESIAN_POINT ( 'NONE',  ( 8.797364180957998769, -4.070567455836420656, -8.475895758763700272 ) ) ;
#37234=CARTESIAN_POINT ( 'NONE',  ( 9.427263540183332680, -4.629523725463626782, -8.592232985442821658 ) ) ;
#37261=CARTESIAN_POINT ( 'NONE',  ( 11.59999999999999964, -4.883784007588900522, -7.825000000000000178 ) ) ;
#37331=CARTESIAN_POINT ( 'NONE',  ( 10.30903300763299946, -3.402282662142699809, -8.126922218169600143 ) ) ;
#37348=CARTESIAN_POINT ( 'NONE',  ( 11.55670819615736278, -4.620649663933218854, -6.880644002891320277 ) ) ;
#37369=CARTESIAN_POINT ( 'NONE',  ( 11.03918313518939875, -4.707599264529200411, -8.394758848575399668 ) ) ;
#37409=VECTOR ( 'NONE', #21712, 1000.000000000000000 ) ;
#37417=CARTESIAN_POINT ( 'NONE',  ( 10.94487616594229884, -4.303437140848100029, -6.543508100188799581 ) ) ;
#37431=CARTESIAN_POINT ( 'NONE',  ( 9.479721904869998994, -3.004358235431599855, -8.058956102599799109 ) ) ;
#37451=CARTESIAN_POINT ( 'NONE',  ( 11.23627509987186102, -4.272452942476324012, -6.249999999999999112 ) ) ;
#37467=CARTESIAN_POINT ( 'NONE',  ( 9.129282595918652987, -2.750056606219162703, -7.730023426265350217 ) ) ;
#37477=CARTESIAN_POINT ( 'NONE',  ( 11.01053724730969918, -4.948425591258600598, -7.174999999999999822 ) ) ;
#37483=CARTESIAN_POINT ( 'NONE',  ( 11.16225954179439839, -3.122605388210700106, -8.229019074832200076 ) ) ;
#37490=CARTESIAN_POINT ( 'NONE',  ( 10.44635971519499940, -3.540377183549800133, -6.735384833238199143 ) ) ;
#37538=CARTESIAN_POINT ( 'NONE',  ( 9.332721904869998752, -3.243980311826100138, -7.924431591189499358 ) ) ;
#37554=CARTESIAN_POINT ( 'NONE',  ( 11.56833327354034857, -4.746587807672299597, -7.011667014989399149 ) ) ;
#37561=CARTESIAN_POINT ( 'NONE',  ( 8.749283493600000128, -3.910012670022149806, -8.350279134800100422 ) ) ;
#37589=CIRCLE ( 'NONE', #53211, 0.7499999936418002555 ) ;
#37631=CARTESIAN_POINT ( 'NONE',  ( 11.14975833414749928, -4.796537143354000499, -7.825000000000000178 ) ) ;
#37645=CARTESIAN_POINT ( 'NONE',  ( 10.87068169682078178, -3.126090202221432079, -7.480731692978241476 ) ) ;
#37675=CARTESIAN_POINT ( 'NONE',  ( 10.87103032197929942, -3.416314376401300201, -6.683751296690399357 ) ) ;
#37679=CARTESIAN_POINT ( 'NONE',  ( 11.84388784977539899, -5.255745690988000263, -7.428242901739219306 ) ) ;
#37711=CARTESIAN_POINT ( 'NONE',  ( 10.54687750876899877, -4.617914354660699772, -8.458891008702400072 ) ) ;
#37716=CARTESIAN_POINT ( 'NONE',  ( 10.89393020684959978, -5.250000000000000000, -7.500000000000000000 ) ) ;
#37760=CARTESIAN_POINT ( 'NONE',  ( 11.16641369783139837, -4.050626550392200542, -8.502191501283999031 ) ) ;
#37772=CARTESIAN_POINT ( 'NONE',  ( 9.843930206850000530, -5.250000000000000000, -7.500000000000000000 ) ) ;
#37776=CARTESIAN_POINT ( 'NONE',  ( 9.074455549952999078, -3.111370763671500228, -6.783011486330899231 ) ) ;
#37796=EDGE_LOOP ( 'NONE', ( #64181, #41161, #7692, #39434 ) ) ;
#37822=CARTESIAN_POINT ( 'NONE',  ( 11.00000000000000000, -4.968589424331200100, -7.174999999999999822 ) ) ;
#37828=CARTESIAN_POINT ( 'NONE',  ( 10.44841638348500013, -5.108333310975999630, -7.230023356477299323 ) ) ;
#37889=CARTESIAN_POINT ( 'NONE',  ( 9.837292290062999101, -3.131390070940299974, -6.995659746333000584 ) ) ;
#37901=CARTESIAN_POINT ( 'NONE',  ( 10.69568717260499824, -4.466067913030199676, -8.260703168378098482 ) ) ;
#37915=ORIENTED_EDGE ( 'NONE', *, *, #23349, .T. ) ;
#37989=VERTEX_POINT ( 'NONE', #3483 ) ;
#38015=CARTESIAN_POINT ( 'NONE',  ( 10.45257053952200010, -4.394359323863099576, -6.577269499510100204 ) ) ;
#38019=CARTESIAN_POINT ( 'NONE',  ( 11.26723293495529887, -5.173938955706000264, -7.452807962566580180 ) ) ;
#38032=EDGE_CURVE ( 'NONE', #47095, #2906, #46490, .T. ) ;
#38050=CARTESIAN_POINT ( 'NONE',  ( 10.46887750876899936, -4.692271380433699512, -8.574279626736998949 ) ) ;
#38064=EDGE_LOOP ( 'NONE', ( #9190, #61062, #2077, #2896 ) ) ;
#38100=CARTESIAN_POINT ( 'NONE',  ( 10.94072200990529886, -5.077092948368999714, -7.124286150322599376 ) ) ;
#38111=CARTESIAN_POINT ( 'NONE',  ( 9.885596873516499627, -5.092232985442824322, -8.129523725463620565 ) ) ;
#38116=CARTESIAN_POINT ( 'NONE',  ( 9.908304848515998131, -3.086535948898899928, -7.917643062525700159 ) ) ;
#38164=CARTESIAN_POINT ( 'NONE',  ( 11.60118044953561878, -2.866798846279000390, -8.090905336380599167 ) ) ;
#38176=CARTESIAN_POINT ( 'NONE',  ( 11.58902763632552002, -4.786505910413500153, -7.137085349939700230 ) ) ;
#38188=CARTESIAN_POINT ( 'NONE',  ( 9.498096873515667227, -4.327184855449103473, -8.717465845835393523 ) ) ;
#38229=CARTESIAN_POINT ( 'NONE',  ( 9.989267173155999657, -4.764472860199700399, -6.848522029265999400 ) ) ;
#38243=CARTESIAN_POINT ( 'NONE',  ( 10.93990547754509812, -2.967013601007999934, -7.532784233952049213 ) ) ;
#38296=CARTESIAN_POINT ( 'NONE',  ( 11.00000000000000000, -2.920245322398999921, -7.825000000000000178 ) ) ;
#38364=CARTESIAN_POINT ( 'NONE',  ( 11.33456651104149948, -3.887457492043800311, -6.364824110469998963 ) ) ;
#38397=CARTESIAN_POINT ( 'NONE',  ( 10.93656785386839836, -5.060279460151999587, -8.213529149347399638 ) ) ;
#38412=AXIS2_PLACEMENT_3D ( 'NONE', #34734, #29150, #2559 ) ;
#38419=CARTESIAN_POINT ( 'NONE',  ( 11.76077869730539938, -4.595338376575799799, -6.326049646822999861 ) ) ;
#38450=CARTESIAN_POINT ( 'NONE',  ( 10.12841772631199966, -3.509411006705700053, -8.509834072393999804 ) ) ;
#38469=CARTESIAN_POINT ( 'NONE',  ( 9.251759580228998914, -5.110528875107000601, -7.234556850645999404 ) ) ;
#38484=CARTESIAN_POINT ( 'NONE',  ( 10.97364560330029981, -3.734560974198899874, -6.675475461903199736 ) ) ;
#38512=CARTESIAN_POINT ( 'NONE',  ( 11.06049777433069892, -4.851452298509800087, -7.174999999999999822 ) ) ;
#38519=CARTESIAN_POINT ( 'NONE',  ( 10.49349279008999858, -4.332388355267299929, -8.734031750754999379 ) ) ;
#38527=CARTESIAN_POINT ( 'NONE',  ( 9.643930206848999376, -2.750000000000000000, -7.500000000000000000 ) ) ;
#38530=CARTESIAN_POINT ( 'NONE',  ( 11.51518179236248862, -4.180996681294200101, -6.652923384986699773 ) ) ;
#38578=CARTESIAN_POINT ( 'NONE',  ( 9.685317406968998455, -3.813190776280700245, -8.486886322867700727 ) ) ;
#38636=CARTESIAN_POINT ( 'NONE',  ( 10.06430484851600049, -2.836617618740000069, -8.031907719862799055 ) ) ;
#38656=B_SPLINE_CURVE_WITH_KNOTS ( 'NONE', 3,
 ( #15757, #49988, #44752, #22021, #11880, #64668, #49636, #17482, #55229, #7329, #65362, #23417, #38806, #11529, #65710, #60130 ),
 .UNSPECIFIED., .F., .F.,
 ( 4, 2, 2, 2, 2, 2, 2, 4 ),
 ( 0.000000000000000000, 0.06249999999999912570, 0.1249999999999982514, 0.2499999999999985012, 0.3749999999999987232, 0.4999999999999990008, 0.7499999999999994449, 1.000000000000000000 ),
 .UNSPECIFIED. ) ;
#38661=DIRECTION ( 'NONE',  ( 0.000000000000000000, 1.000000000000000000, 0.000000000000000000 ) ) ;
#38667=EDGE_CURVE ( 'NONE', #48162, #2906, #19622, .T. ) ;
#38699=DIRECTION ( 'NONE',  ( 0.7071067486699967874, -0.7071068137030968037, 9.022793105466955192E-11 ) ) ;
#38716=CARTESIAN_POINT ( 'NONE',  ( 10.77256919669529900, -3.037654633983899899, -7.784327714719899483 ) ) ;
#38720=CARTESIAN_POINT ( 'NONE',  ( 10.97124174884019965, -4.036194082918090231, -8.815770025351000072 ) ) ;
#38750=CARTESIAN_POINT ( 'NONE',  ( 10.59195391537400077, -2.942766577210000012, -8.218034727798299244 ) ) ;
#38803=CARTESIAN_POINT ( 'NONE',  ( 10.74379975933729980, -2.921317947059999920, -7.128873141726999485 ) ) ;
#38806=CARTESIAN_POINT ( 'NONE',  ( 11.60000000000000142, -3.674136214561154468, -8.622936771936917211 ) ) ;
#38812=B_SPLINE_CURVE_WITH_KNOTS ( 'NONE', 3,
 ( #39542, #53626, #7374, #17876 ),
 .UNSPECIFIED., .F., .F.,
 ( 4, 4 ),
 ( 0.000000000000000000, 1.000000000000000000 ),
 .UNSPECIFIED. ) ;
#38818=CARTESIAN_POINT ( 'NONE',  ( 9.606367640780998585, -3.461752753411900141, -6.493012239633999982 ) ) ;
#38837=CARTESIAN_POINT ( 'NONE',  ( 11.19518313518939934, -4.537300658085600347, -8.179416362154199760 ) ) ;
#38847=CARTESIAN_POINT ( 'NONE',  ( 11.00000000000000000, -3.008232475376599879, -7.174999999999999822 ) ) ;
#38886=CARTESIAN_POINT ( 'NONE',  ( 11.61364291764652812, -4.859654669415900408, -7.393734108507599601 ) ) ;
#38935=CARTESIAN_POINT ( 'NONE',  ( 8.900113844317997902, -3.746347404385800051, -6.528144732449299603 ) ) ;
#38944=B_SPLINE_CURVE_WITH_KNOTS ( 'NONE', 3,
 ( #42163, #31669, #36564, #6027, #27367, #47060, #68363, #58231, #11616, #48692, #38188, #30987, #43796, #20826, #41468, #15586, #30635, #49034 ),
 .UNSPECIFIED., .F., .F.,
 ( 4, 2, 2, 2, 2, 2, 2, 2, 4 ),
 ( 0.000000000000000000, 0.1250000000000000000, 0.2500000000000000000, 0.3750000000000000000, 0.5000000000000000000, 0.6250000000000000000, 0.7500000000000000000, 0.8750000000000000000, 1.000000000000000000 ),
 .UNSPECIFIED. ) ;
#38961=ORIENTED_EDGE ( 'NONE', *, *, #21347, .F. ) ;
#38966=CARTESIAN_POINT ( 'NONE',  ( 11.63611496860034933, -2.828587461987000395, -6.899705789500199415 ) ) ;
#38990=CARTESIAN_POINT ( 'NONE',  ( 9.811013376692999444, -5.140392946802999852, -6.920441276178300072 ) ) ;
#39000=CARTESIAN_POINT ( 'NONE',  ( 11.00008140503725329, -2.915874161187789859, -7.367730262387956586 ) ) ;
#39050=CARTESIAN_POINT ( 'NONE',  ( 8.599999986286999132, -4.750000013710600655, -7.499999999961952213 ) ) ;
#39067=CARTESIAN_POINT ( 'NONE',  ( 11.76077869730539938, -4.595338376575799799, -6.326049646822999861 ) ) ;
#39081=CARTESIAN_POINT ( 'NONE',  ( 8.849999778957998942, -4.000000000000000000, -7.500000000000000000 ) ) ;
#39095=CARTESIAN_POINT ( 'NONE',  ( 10.27610941423800028, -3.155589807313900153, -6.733017893878099791 ) ) ;
#39145=CARTESIAN_POINT ( 'NONE',  ( 10.22687885159599830, -2.867290578374000365, -7.364871923548499844 ) ) ;
#39163=CARTESIAN_POINT ( 'NONE',  ( 10.08359632033899800, -4.802737635155300389, -7.172402329663099430 ) ) ;
#39179=CARTESIAN_POINT ( 'NONE',  ( 10.38287885159599888, -3.139900861731399928, -7.397393329751199786 ) ) ;
#39215=CARTESIAN_POINT ( 'NONE',  ( 10.39503166480599994, -5.274847857784000560, -7.589885038193400213 ) ) ;
#39222=CARTESIAN_POINT ( 'NONE',  ( 9.654346873515669003, -2.749999999999998668, -7.336375382625537789 ) ) ;
#39270=CARTESIAN_POINT ( 'NONE',  ( 10.75851354018298522, -3.836375382625526687, -6.250000000000000888 ) ) ;
#39276=CARTESIAN_POINT ( 'NONE',  ( 9.102747021775998704, -4.754947163618299832, -8.162493079567200382 ) ) ;
#39304=CARTESIAN_POINT ( 'NONE',  ( 11.34523293495530005, -5.315205473512000012, -7.447129085684729866 ) ) ;
#39331=CARTESIAN_POINT ( 'NONE',  ( 10.54555864497999984, -2.992894514506000192, -8.288745882156399958 ) ) ;
#39384=ORIENTED_EDGE ( 'NONE', *, *, #22474, .T. ) ;
#39404=CARTESIAN_POINT ( 'NONE',  ( 10.08521345716899908, -3.075109701058799772, -8.340879262988799780 ) ) ;
#39409=CARTESIAN_POINT ( 'NONE',  ( 11.19434208742519843, -4.478858766422799675, -8.252717006421999457 ) ) ;
#39434=ORIENTED_EDGE ( 'NONE', *, *, #34880, .F. ) ;
#39439=CARTESIAN_POINT ( 'NONE',  ( 10.44426222744799837, -4.986443098259000450, -8.312555471636301263 ) ) ;
#39492=CARTESIAN_POINT ( 'NONE',  ( 11.19518313518939934, -4.537300658085600347, -8.179416362154199760 ) ) ;
#39493=CARTESIAN_POINT ( 'NONE',  ( 10.59610807141099897, -3.947296672195129918, -8.639522915742999132 ) ) ;
#39508=CARTESIAN_POINT ( 'NONE',  ( 9.072442991499999110, -4.063228561016970275, -6.497580701799000380 ) ) ;
#39526=CARTESIAN_POINT ( 'NONE',  ( 10.53057053952199951, -4.340412141385700195, -6.703496287302799672 ) ) ;
#39542=CARTESIAN_POINT ( 'NONE',  ( 10.53521345716899837, -3.075109701058799772, -8.340879262988799780 ) ) ;
#39561=CARTESIAN_POINT ( 'NONE',  ( 10.34580110216399973, -5.090698144635000588, -6.833896451085399448 ) ) ;
#39577=CARTESIAN_POINT ( 'NONE',  ( 11.14975833414749928, -4.796537143354000499, -7.825000000000000178 ) ) ;
#39625=CARTESIAN_POINT ( 'NONE',  ( 8.720797255587999786, -2.859210004667000149, -7.451702546394010085 ) ) ;
#39626=CARTESIAN_POINT ( 'NONE',  ( 9.677263540183330903, -3.370476274536371442, -6.407767014557179230 ) ) ;
#39640=CARTESIAN_POINT ( 'NONE',  ( 10.41476354018330852, -5.217465845835395299, -7.827184855449099921 ) ) ;
#39644=SURFACE_STYLE_FILL_AREA ( #17978 ) ;
#39669=B_SPLINE_CURVE_WITH_KNOTS ( 'NONE', 3,
 ( #37822, #37477, #10563, #38512, #49005, #22427 ),
 .UNSPECIFIED., .F., .F.,
 ( 4, 1, 1, 4 ),
 ( 0.000000000000000000, 0.3333333333333000081, 0.6666666666667000474, 1.000000000000000000 ),
 .UNSPECIFIED. ) ;
#39685=ORIENTED_EDGE ( 'NONE', *, *, #40750, .F. ) ;
#39760=CARTESIAN_POINT ( 'NONE',  ( 11.43856039236529831, -2.967715280237000375, -7.550239075043479353 ) ) ;
#39773=FACE_OUTER_BOUND ( 'NONE', #35632, .T. ) ;
#39789=CARTESIAN_POINT ( 'NONE',  ( 10.05862282008599884, -3.333723918618700210, -8.574682153725998290 ) ) ;
#39793=CARTESIAN_POINT ( 'NONE',  ( 10.16858376188599955, -4.731143729777899765, -7.965979387614599894 ) ) ;
#39809=CARTESIAN_POINT ( 'NONE',  ( 10.47769598648999967, -2.990523684589000197, -8.101059042556599366 ) ) ;
#39826=ORIENTED_EDGE ( 'NONE', *, *, #38667, .T. ) ;
#39828=ORIENTED_EDGE ( 'NONE', *, *, #25310, .T. ) ;
#39840=CARTESIAN_POINT ( 'NONE',  ( 11.66287348028854964, -4.761955701524100526, -7.911973420841600380 ) ) ;
#39841=CARTESIAN_POINT ( 'NONE',  ( 10.56733863405299800, -3.211524470605299886, -8.505794571537999005 ) ) ;
#39859=CARTESIAN_POINT ( 'NONE',  ( 9.880963142879998884, -3.151633609938700342, -7.321163726496699553 ) ) ;
#39879=CARTESIAN_POINT ( 'NONE',  ( 11.58902763632552002, -4.786505910413500153, -7.137085349939700230 ) ) ;
#39914=CARTESIAN_POINT ( 'NONE',  ( 10.66579975933730040, -2.791514215189000225, -7.084213409908699965 ) ) ;
#39927=CARTESIAN_POINT ( 'NONE',  ( 11.63410404293056999, -4.442327784369100030, -8.400720262063998689 ) ) ;
#39975=CARTESIAN_POINT ( 'NONE',  ( 8.796784697134999220, -3.380386586585000241, -6.540930833646799947 ) ) ;
#40003=CARTESIAN_POINT ( 'NONE',  ( 11.27234208742519783, -4.554746427620499638, -8.372004648554700168 ) ) ;
#40031=CARTESIAN_POINT ( 'NONE',  ( 9.912329965421998068, -4.888489908445900589, -8.420309768537698858 ) ) ;
#40035=ORIENTED_EDGE ( 'NONE', *, *, #324, .F. ) ;
#40069=EDGE_CURVE ( 'NONE', #46988, #63961, #27787, .T. ) ;
#40080=CARTESIAN_POINT ( 'NONE',  ( 10.64914416493166449, -4.811858819934198728, -7.823998238890133905 ) ) ;
#40102=CARTESIAN_POINT ( 'NONE',  ( 10.05333291544899943, -3.468906853242414989, -8.658936933361781385 ) ) ;
#40110=CARTESIAN_POINT ( 'NONE',  ( 11.31900581613029821, -3.249313226592100534, -7.982035256002799173 ) ) ;
#40151=ORIENTED_EDGE ( 'NONE', *, *, #6375, .F. ) ;
#40156=CARTESIAN_POINT ( 'NONE',  ( 10.68035971519489813, -3.321859513918399731, -6.371865185335000348 ) ) ;
#40187=CARTESIAN_POINT ( 'NONE',  ( 10.54272335273199879, -3.555125495332600138, -8.698083075453000745 ) ) ;
#40203=CARTESIAN_POINT ( 'NONE',  ( 9.655013376692998861, -4.895413217368500547, -7.044942343771899651 ) ) ;
#40221=CARTESIAN_POINT ( 'NONE',  ( 10.84641504065830020, -3.195537720350400068, -6.900173947321999179 ) ) ;
#40257=CARTESIAN_POINT ( 'NONE',  ( 8.705629240797998492, -4.228941919214900480, -8.376522367004298530 ) ) ;
#40264=CARTESIAN_POINT ( 'NONE',  ( 11.19518313518939934, -4.537300658085600347, -8.179416362154199760 ) ) ;
#40309=CARTESIAN_POINT ( 'NONE',  ( 9.075405316139999456, -4.242421256336299962, -8.615780615741000403 ) ) ;
#40335=CARTESIAN_POINT ( 'NONE',  ( 11.02301463001509774, -3.452642973349600464, -6.623338154204899908 ) ) ;
#40345=CARTESIAN_POINT ( 'NONE',  ( 0.000000000000000000, 0.000000000000000000, 0.000000000000000000 ) ) ;
#40359=CARTESIAN_POINT ( 'NONE',  ( 9.203113844318000503, -3.676949563211899807, -6.262250912840999106 ) ) ;
#40431=CARTESIAN_POINT ( 'NONE',  ( 11.27234208742519783, -4.554746427620499638, -8.372004648554700168 ) ) ;
#40449=CARTESIAN_POINT ( 'NONE',  ( 11.02319144466311052, -2.880026002252477291, -7.824989718906223857 ) ) ;
#40465=CARTESIAN_POINT ( 'NONE',  ( 9.028772138681999238, -4.322628849750500102, -6.695252480703800302 ) ) ;
#40483=CARTESIAN_POINT ( 'NONE',  ( 10.60235971519489873, -3.394698737128500010, -6.493038401303000029 ) ) ;
#40495=DIRECTION ( 'NONE',  ( 0.000000000000000000, 1.000000000000000000, 0.000000000000000000 ) ) ;
#40514=CARTESIAN_POINT ( 'NONE',  ( 10.51810807141099779, -3.940954591493389891, -8.776647962565998995 ) ) ;
#40532=CARTESIAN_POINT ( 'NONE',  ( 8.802265421554999136, -4.188500707411799695, -8.475084258675400051 ) ) ;
#40536=PRODUCT_DEFINITION_SHAPE ( 'NONE', 'NONE',  #43225 ) ;
#40550=CARTESIAN_POINT ( 'NONE',  ( 10.67410807141119911, -3.953638752893899877, -8.502397868920999358 ) ) ;
#40590=VERTEX_POINT ( 'NONE', #22759 ) ;
#40598=CARTESIAN_POINT ( 'NONE',  ( 9.049596101582626062, -4.563377510236459322, -6.830568860986387492 ) ) ;
#40602=CARTESIAN_POINT ( 'NONE',  ( 10.40749413291699987, -3.211956830789300277, -7.140435631538599281 ) ) ;
#40645=CARTESIAN_POINT ( 'NONE',  ( 8.594151519676998419, -3.975306837623020062, -8.641543873690000765 ) ) ;
#40673=CARTESIAN_POINT ( 'NONE',  ( 11.55811496860034815, -2.954409148022000053, -6.964183526617899744 ) ) ;
#40697=CARTESIAN_POINT ( 'NONE',  ( 8.958265421554999719, -4.240073379563900069, -8.741861511046000288 ) ) ;
#40750=EDGE_CURVE ( 'NONE', #28041, #2109, #33065, .T. ) ;
#40776=CARTESIAN_POINT ( 'NONE',  ( 10.56591429142999949, -3.980313504646230349, -6.466681092390999197 ) ) ;
#40812=CARTESIAN_POINT ( 'NONE',  ( 9.839304848515999069, -3.211495113978299898, -7.860510733857099197 ) ) ;
#40826=CARTESIAN_POINT ( 'NONE',  ( 10.59725056272499977, -2.683866746800999792, -7.519505747156228992 ) ) ;
#40845=DIRECTION ( 'NONE',  ( 0.000000000000000000, 0.8514543052404082157, -0.5244287998266055073 ) ) ;
#40856=CARTESIAN_POINT ( 'NONE',  ( 9.393930206848999376, -5.250000000000000000, -7.500000000000000000 ) ) ;
#40858=CARTESIAN_POINT ( 'NONE',  ( 11.76133460557259980, -3.860150918677800025, -8.354833838171700222 ) ) ;
#40859=CARTESIAN_POINT ( 'NONE',  ( 10.37041638348499895, -5.241705141469999774, -7.197535585171899619 ) ) ;
#40880=CARTESIAN_POINT ( 'NONE',  ( 9.273063610504998167, -3.644370728184199937, -8.290718512198798962 ) ) ;
#40898=CARTESIAN_POINT ( 'NONE',  ( 11.48641235500450009, -4.739919807690899489, -6.822158181405299615 ) ) ;
#40942=CARTESIAN_POINT ( 'NONE',  ( 9.834799664234624927, -3.204277625948437347, -7.863810627050381363 ) ) ;
#40947=CARTESIAN_POINT ( 'NONE',  ( 11.14595257254739913, -4.831736303435800295, -7.741895249827200232 ) ) ;
#40967=CARTESIAN_POINT ( 'NONE',  ( 10.84393020684979980, -5.250000000000000000, -7.500000000000000000 ) ) ;
#40973=CARTESIAN_POINT ( 'NONE',  ( 10.40769129028899975, -4.889436474118636689, -8.413289387078531689 ) ) ;
#40994=CARTESIAN_POINT ( 'NONE',  ( 9.632646554151000018, -3.447209681134600245, -8.499078230848398974 ) ) ;
#41010=CARTESIAN_POINT ( 'NONE',  ( 10.31021345716899873, -3.363461959113699606, -8.078719053813800954 ) ) ;
#41022=CARTESIAN_POINT ( 'NONE',  ( 11.14256920625030034, -3.957769094421040190, -6.325872106312999676 ) ) ;
#41023=CARTESIAN_POINT ( 'NONE',  ( 11.60000000000000142, -3.186139913033902538, -6.684405152318921850 ) ) ;
#41024=CARTESIAN_POINT ( 'NONE',  ( 11.08810207955139937, -4.796537143354000499, -7.174999999999999822 ) ) ;
#41071=CYLINDRICAL_SURFACE ( 'NONE', #34175, 1.250000000000000222 ) ;
#41087=FACE_OUTER_BOUND ( 'NONE', #38064, .T. ) ;
#41161=ORIENTED_EDGE ( 'NONE', *, *, #63508, .T. ) ;
#41170=ORIENTED_EDGE ( 'NONE', *, *, #34831, .F. ) ;
#41209=CARTESIAN_POINT ( 'NONE',  ( 10.77672335273219950, -3.698477709264200275, -8.312023951944400579 ) ) ;
#41210=CARTESIAN_POINT ( 'NONE',  ( 11.18272066707849888, -2.906477115133000222, -6.838543969064300398 ) ) ;
#41223=CARTESIAN_POINT ( 'NONE',  ( 11.46253286130405691, -3.661005694687299528, -6.691343801417681370 ) ) ;
#41226=CARTESIAN_POINT ( 'NONE',  ( 8.817138961223998095, -3.281636118526699786, -7.985449642667900250 ) ) ;
#41243=CARTESIAN_POINT ( 'NONE',  ( 11.26487482311540056, -3.069598554678400149, -7.875904247640098887 ) ) ;
#41294=CARTESIAN_POINT ( 'NONE',  ( 10.48133997687999930, -3.815400206859000054, -6.653701289769800020 ) ) ;
#41301=CARTESIAN_POINT ( 'NONE',  ( 10.19601354018254291, -3.000416447002272058, -6.731816600031361730 ) ) ;
#41341=CARTESIAN_POINT ( 'NONE',  ( 8.972076168957999087, -4.649151400100800302, -8.602264418015000302 ) ) ;
#41370=CARTESIAN_POINT ( 'NONE',  ( 10.56591429142999949, -3.980313504646230349, -6.466681092390999197 ) ) ;
#41371=CARTESIAN_POINT ( 'NONE',  ( 11.60000000000000142, -3.579171096429341503, -6.483899970161565385 ) ) ;
#41379=SHAPE_REPRESENTATION_RELATIONSHIP ( 'NONE' , 'NONE' ,  #53976, #23576 ) ;
#41410=VERTEX_POINT ( 'NONE', #20947 ) ;
#41468=CARTESIAN_POINT ( 'NONE',  ( 9.435596873515667227, -5.092232985442824322, -8.129523725463622341 ) ) ;
#41544=B_SPLINE_CURVE_WITH_KNOTS ( 'NONE', 3,
 ( #39404, #67670, #40102, #66306, #18430, #60724, #61417, #13535, #34854, #56169 ),
 .UNSPECIFIED., .F., .F.,
 ( 4, 2, 2, 2, 4 ),
 ( 0.000000000000000000, 0.2500000000000000000, 0.5000000000000000000, 0.7500000000000000000, 1.000000000000000000 ),
 .UNSPECIFIED. ) ;
#41545=CARTESIAN_POINT ( 'NONE',  ( 10.57980110216399972, -4.739241740354600552, -7.048535450274799885 ) ) ;
#41565=CARTESIAN_POINT ( 'NONE',  ( 9.754317406968999293, -3.838745722419000028, -8.351883209406098629 ) ) ;
#41583=CARTESIAN_POINT ( 'NONE',  ( 10.32949413291699869, -3.087070836781100169, -7.083453279150199400 ) ) ;
#41629=CARTESIAN_POINT ( 'NONE',  ( 9.581508192411627434, -4.779998216922380472, -7.103597363128174358 ) ) ;
#41633=CARTESIAN_POINT ( 'NONE',  ( 11.58071932425156980, -4.167269912168199753, -8.628410767520000135 ) ) ;
#41667=CARTESIAN_POINT ( 'NONE',  ( 11.11486084871780022, -2.792989229543000107, -7.174999999999999822 ) ) ;
#41680=CARTESIAN_POINT ( 'NONE',  ( 8.617468108405999416, -2.769196120524999749, -7.848577323721800170 ) ) ;
#41734=B_SPLINE_CURVE_WITH_KNOTS ( 'NONE', 3,
 ( #68947, #21060, #46608, #52876 ),
 .UNSPECIFIED., .F., .F.,
 ( 4, 4 ),
 ( 0.000000000000000000, 1.000000000000000000 ),
 .UNSPECIFIED. ) ;
#41791=CARTESIAN_POINT ( 'NONE',  ( 9.521013540183334456, -3.231816600031356845, -8.499583552997725278 ) ) ;
#41806=CARTESIAN_POINT ( 'NONE',  ( 11.59999999999999964, -2.750000000000000000, -7.500000000000000000 ) ) ;
#41857=CIRCLE ( 'NONE', #15066, 1.249999999999999778 ) ;
#41862=FACE_OUTER_BOUND ( 'NONE', #60193, .T. ) ;
#41878=CARTESIAN_POINT ( 'NONE',  ( 11.53828694957233658, -3.690393262785353734, -8.735060943529678212 ) ) ;
#41889=CARTESIAN_POINT ( 'NONE',  ( 10.50595525820100029, -4.081787880721680750, -6.637672143048099827 ) ) ;
#41908=CARTESIAN_POINT ( 'NONE',  ( 9.323721904869998411, -3.243980311826100138, -7.924431591189499358 ) ) ;
#41919=ORIENTED_EDGE ( 'NONE', *, *, #56935, .T. ) ;
#41927=CARTESIAN_POINT ( 'NONE',  ( 11.43302763632549990, -5.035790660926999784, -7.022058766158599141 ) ) ;
#41973=ADVANCED_FACE ( 'NONE', ( #18725 ), #5207, .T. ) ;
#41979=CARTESIAN_POINT ( 'NONE',  ( 10.77256919669529900, -3.037654633983899899, -7.784327714719899483 ) ) ;
#41997=CARTESIAN_POINT ( 'NONE',  ( 9.809000818239997699, -5.010295986746999830, -8.032011717116800398 ) ) ;
#42030=CARTESIAN_POINT ( 'NONE',  ( 8.693455549952998851, -3.004437130344999929, -6.696732323226999739 ) ) ;
#42050=CARTESIAN_POINT ( 'NONE',  ( 10.17764828895399809, -2.998858038575999974, -8.046814291299300592 ) ) ;
#42057=CARTESIAN_POINT ( 'NONE',  ( 10.94501463001509833, -3.527519786474400121, -6.743262887067199784 ) ) ;
#42098=AXIS2_PLACEMENT_3D ( 'NONE', #44278, #22581, #13494 ) ;
#42110=CARTESIAN_POINT ( 'NONE',  ( 10.19190035061499877, -3.732283713685800031, -8.468075389605498771 ) ) ;
#42124=CARTESIAN_POINT ( 'NONE',  ( 11.35034208742529849, -4.630634088820300143, -8.491292290686200062 ) ) ;
#42163=CARTESIAN_POINT ( 'NONE',  ( 9.643930206848999376, -2.750000000000000000, -7.500000000000000000 ) ) ;
#42179=CARTESIAN_POINT ( 'NONE',  ( 11.39975833414730033, -3.203462856645999945, -7.174999999999999822 ) ) ;
#42246=CARTESIAN_POINT ( 'NONE',  ( 10.33364828895399867, -3.239803852721999888, -7.915211961479200475 ) ) ;
#42260=AXIS2_PLACEMENT_3D ( 'NONE', #14641, #2774, #35958 ) ;
#42266=CARTESIAN_POINT ( 'NONE',  ( 9.019772138681998896, -4.322628849750500102, -6.695252480703800302 ) ) ;
#42284=CARTESIAN_POINT ( 'NONE',  ( 10.84226088462129844, -3.997572771977982775, -6.359261544073000039 ) ) ;
#42334=CARTESIAN_POINT ( 'NONE',  ( 10.40333997687999990, -3.786145554879500441, -6.519583185858300212 ) ) ;
#42341=CARTESIAN_POINT ( 'NONE',  ( 10.34184687351645771, -4.999583552997724389, -6.731816600031354625 ) ) ;
#42351=CARTESIAN_POINT ( 'NONE',  ( 9.760355082327999199, -4.572497688003699601, -6.356045986629998978 ) ) ;
#42378=CARTESIAN_POINT ( 'NONE',  ( 8.490822372493999737, -4.367693913457399546, -8.702849744394999476 ) ) ;
#42398=CARTESIAN_POINT ( 'NONE',  ( 10.42380110216399913, -4.973546009874400653, -6.905442784147899360 ) ) ;
#42419=VERTEX_POINT ( 'NONE', #1616 ) ;
#42441=EDGE_CURVE ( 'NONE', #40590, #26260, #6705, .T. ) ;
#42451=CARTESIAN_POINT ( 'NONE',  ( 9.307392757686999474, -3.414780058706799792, -8.139707405630899117 ) ) ;
#42466=CARTESIAN_POINT ( 'NONE',  ( 11.59603632436369125, -4.842640371965599932, -7.303218851299499548 ) ) ;
#42483=CARTESIAN_POINT ( 'NONE',  ( 9.489763540183334456, -3.672815144550900524, -8.717465845835395299 ) ) ;
#42489=VERTEX_POINT ( 'NONE', #37631 ) ;
#42503=CARTESIAN_POINT ( 'NONE',  ( 10.86190547754509872, -3.108323067758099967, -7.528299448264639260 ) ) ;
#42520=DIRECTION ( 'NONE',  ( 0.000000000000000000, 1.000000000000000000, 0.000000000000000000 ) ) ;
#42570=CARTESIAN_POINT ( 'NONE',  ( 11.44571737393082600, -5.011200127299592744, -8.273761053885760219 ) ) ;
#42580=CARTESIAN_POINT ( 'NONE',  ( 11.38795122972049967, -3.601717549869600354, -6.578956058177199751 ) ) ;
#42595=CIRCLE ( 'NONE', #60469, 0.7499999936418002555 ) ;
#42607=ADVANCED_FACE ( 'NONE', ( #32403 ), #43229, .T. ) ;
#42610=ORIENTED_EDGE ( 'NONE', *, *, #59704, .T. ) ;
#42618=CARTESIAN_POINT ( 'NONE',  ( 10.25564828895399927, -3.119330945648699949, -7.981013126389099099 ) ) ;
#42623=CARTESIAN_POINT ( 'NONE',  ( 11.08482133862618468, -3.057020944820409092, -8.373613860257945518 ) ) ;
#42665=CARTESIAN_POINT ( 'NONE',  ( 10.96949144726329806, -4.580206776679999869, -6.681274802424499448 ) ) ;
#42680=CARTESIAN_POINT ( 'NONE',  ( 10.33890035061499901, -3.732283713685800031, -8.468075389605498771 ) ) ;
#42684=VECTOR ( 'NONE', #59277, 1000.000000000000000 ) ;
#42711=CARTESIAN_POINT ( 'NONE',  ( 8.995772571291157149, -5.001491341851800776, -8.076234199639099387 ) ) ;
#42715=CARTESIAN_POINT ( 'NONE',  ( 9.200038493598999167, -3.074215132699300135, -6.617216466537199970 ) ) ;
#42728=CARTESIAN_POINT ( 'NONE',  ( 8.761230081853241813, -3.478588282862478120, -8.281074114623761417 ) ) ;
#42735=CARTESIAN_POINT ( 'NONE',  ( 10.79303032197930001, -3.336467919271199900, -6.572090902022299730 ) ) ;
#42741=CARTESIAN_POINT ( 'NONE',  ( 11.56833327354034857, -4.746587807672299597, -7.011667014989399149 ) ) ;
#42786=CARTESIAN_POINT ( 'NONE',  ( 10.89393020684959978, -5.250000000000000000, -7.500000000000000000 ) ) ;
#42794=CARTESIAN_POINT ( 'NONE',  ( 9.459367640780998343, -3.591293244209800228, -6.735364967924099666 ) ) ;
#42808=CARTESIAN_POINT ( 'NONE',  ( 10.64902344389989963, -4.883530143601199747, -6.963800219468099684 ) ) ;
#42895=CARTESIAN_POINT ( 'NONE',  ( 11.01837338474678063, -4.264324089837040255, -6.666799917282374643 ) ) ;
#42925=CARTESIAN_POINT ( 'NONE',  ( 10.69872335273220010, -3.650693637952500126, -8.440710326446700051 ) ) ;
#42929=CARTESIAN_POINT ( 'NONE',  ( 10.84657802013509986, -5.315911219205999849, -7.469366283838649423 ) ) ;
#42959=CARTESIAN_POINT ( 'NONE',  ( 10.69456919669529960, -2.906008650422999828, -7.823222900359999343 ) ) ;
#42965=CARTESIAN_POINT ( 'NONE',  ( 11.02755399909320566, -3.866653594937912608, -8.778526265510098625 ) ) ;
#42975=CARTESIAN_POINT ( 'NONE',  ( 11.36486084871759950, -5.207010770456999893, -7.825000000000000178 ) ) ;
#42996=VECTOR ( 'NONE', #32615, 1000.000000000000000 ) ;
#43006=CARTESIAN_POINT ( 'NONE',  ( 10.35410941423799791, -3.257202320419700037, -6.825313060354999628 ) ) ;
#43023=CARTESIAN_POINT ( 'NONE',  ( 10.06027973160899869, -3.909869487835140323, -6.499640669006000238 ) ) ;
#43073=CARTESIAN_POINT ( 'NONE',  ( 10.86687616594229944, -4.344946439135400240, -6.412662853391999818 ) ) ;
#43080=CARTESIAN_POINT ( 'NONE',  ( 11.19434208742519843, -4.478858766422799675, -8.252717006421999457 ) ) ;
#43134=CARTESIAN_POINT ( 'NONE',  ( 8.824126402770998467, -3.060189502158800146, -7.145601175474399547 ) ) ;
#43149=CARTESIAN_POINT ( 'NONE',  ( 11.19434208742519843, -4.478858766422799675, -8.252717006421999457 ) ) ;
#43164=CARTESIAN_POINT ( 'NONE',  ( 10.33351354018233259, -5.249999999999999112, -7.336375382625531572 ) ) ;
#43225=PRODUCT_DEFINITION ( 'UNKNOWN', '', #22913, #44184 ) ;
#43229=CYLINDRICAL_SURFACE ( 'NONE', #28687, 1.250000000000000222 ) ;
#43269=CARTESIAN_POINT ( 'NONE',  ( 11.48225819896749833, -5.120994791668000090, -7.711331004020999913 ) ) ;
#43273=CARTESIAN_POINT ( 'NONE',  ( 10.88813259637009878, -5.155817667926999803, -8.129798612793599943 ) ) ;
#43301=VERTEX_POINT ( 'NONE', #53622 ) ;
#43306=CARTESIAN_POINT ( 'NONE',  ( 10.12841772631199966, -3.509411006705700053, -8.509834072393999804 ) ) ;
#43323=ORIENTED_EDGE ( 'NONE', *, *, #55318, .F. ) ;
#43328=B_SPLINE_CURVE_WITH_KNOTS ( 'NONE', 3,
 ( #24799, #7690, #46469, #55933, #23765, #45100, #29032, #18872, #51028 ),
 .UNSPECIFIED., .F., .F.,
 ( 4, 1, 1, 1, 1, 1, 4 ),
 ( 0.000000000000000000, 0.1176715969261405564, 0.3173201826739889819, 0.5169687684225861002, 0.7166173541704345951, 0.9162659399182834230, 1.000000000000000000 ),
 .UNSPECIFIED. ) ;
#43364=CARTESIAN_POINT ( 'NONE',  ( 10.96533729122639933, -5.140346530769000388, -7.470001566214039990 ) ) ;
#43379=CARTESIAN_POINT ( 'NONE',  ( 9.707684229509998985, -4.804883439508000897, -6.690125258578699885 ) ) ;
#43432=CARTESIAN_POINT ( 'NONE',  ( 10.66995391537419913, -3.056324258617099776, -8.140910455049299443 ) ) ;
#43455=B_SPLINE_SURFACE_WITH_KNOTS ( 'NONE', 3, 3, ( 
 ( #22437, #43778, #27007, #48325 ),
 ( #64384, #11257, #23134, #56337 ),
 ( #50747, #55302, #44822, #44485 ),
 ( #7397, #65776, #40257, #13353 ) ),
 .UNSPECIFIED., .F., .F., .F.,
 ( 4, 4 ),
 ( 4, 4 ),
 ( -0.01349945606786999951, 0.08053609420915000539 ),
 ( -0.0005287450254680999126, 0.02696599629895000266 ),
 .UNSPECIFIED. ) ;
#43491=CARTESIAN_POINT ( 'NONE',  ( 10.11390035061499937, -3.695660922043800145, -8.600505223349999895 ) ) ;
#43503=CARTESIAN_POINT ( 'NONE',  ( 10.94501463001509833, -3.527519786474400121, -6.743262887067199784 ) ) ;
#43518=CARTESIAN_POINT ( 'NONE',  ( 11.71922412107039868, -3.930460928605089777, -6.185573549454999487 ) ) ;
#43613=CARTESIAN_POINT ( 'NONE',  ( 9.289752973821547855, -4.327172861449232855, -6.282573595533348154 ) ) ;
#43614=DIRECTION ( 'NONE',  ( 0.000000000000000000, 1.000000000000000000, 0.000000000000000000 ) ) ;
#43623=CARTESIAN_POINT ( 'NONE',  ( 11.53148876160955005, -4.790673964186999534, -8.322268080792200706 ) ) ;
#43627=CARTESIAN_POINT ( 'NONE',  ( 10.52799293566599914, -3.193321847920899792, -8.489570425681801424 ) ) ;
#43656=CARTESIAN_POINT ( 'NONE',  ( 11.01041369783139956, -4.064477673403060543, -8.776385133971000840 ) ) ;
#43706=CARTESIAN_POINT ( 'NONE',  ( 10.27610941423800028, -3.155589807313900153, -6.733017893878099791 ) ) ;
#43714=EDGE_CURVE ( 'NONE', #8437, #24854, #30009, .T. ) ;
#43722=CARTESIAN_POINT ( 'NONE',  ( 9.631696787963999640, -3.803923679411099990, -6.375149554610999303 ) ) ;
#43739=CARTESIAN_POINT ( 'NONE',  ( 10.92441504065829960, -3.305585767322499979, -6.982228367137699898 ) ) ;
#43764=CARTESIAN_POINT ( 'NONE',  ( 11.59213512191444018, -4.803449168604846164, -7.174950736703190834 ) ) ;
#43772=ORIENTED_EDGE ( 'NONE', *, *, #47854, .F. ) ;
#43774=CARTESIAN_POINT ( 'NONE',  ( 10.07503300763299947, -3.118110956362800223, -8.424978748982498544 ) ) ;
#43778=CARTESIAN_POINT ( 'NONE',  ( 8.741072744221000335, -4.062652182992059657, -8.366433385397499478 ) ) ;
#43782=CARTESIAN_POINT ( 'NONE',  ( 11.59999999999999964, -4.304783012932057673, -6.544326332797709256 ) ) ;
#43796=CARTESIAN_POINT ( 'NONE',  ( 9.466846873515667227, -4.768183399968645375, -8.499583552997723501 ) ) ;
#43833=CARTESIAN_POINT ( 'NONE',  ( 9.887950584426999256, -3.601336184534900120, -6.578094656394299911 ) ) ;
#43838=DIRECTION ( 'NONE',  ( 0.7071067617951957152, 0.000000000000000000, -0.7071068005778986532 ) ) ;
#43882=EDGE_CURVE ( 'NONE', #63961, #46988, #28892, .T. ) ;
#43890=CARTESIAN_POINT ( 'NONE',  ( 10.14029229006299992, -2.893743561734000380, -6.857675253263499471 ) ) ;
#43906=CYLINDRICAL_SURFACE ( 'NONE', #52962, 1.250000000000000222 ) ;
#43927=CARTESIAN_POINT ( 'NONE',  ( 10.84393020684979980, -5.250000000000000000, -7.500000000000000000 ) ) ;
#43966=CARTESIAN_POINT ( 'NONE',  ( 10.23103300763299828, -3.307558760216100069, -8.226274395107198600 ) ) ;
#43968=ADVANCED_FACE ( 'NONE', ( #23623 ), #24227, .T. ) ;
#43972=CARTESIAN_POINT ( 'NONE',  ( 11.59456039236534330, -2.685288321999000249, -7.563984187103470092 ) ) ;
#44000=CARTESIAN_POINT ( 'NONE',  ( 10.71503032197929883, -3.256621462143499901, -6.460430507351999196 ) ) ;
#44024=CARTESIAN_POINT ( 'NONE',  ( 11.38678751119029897, -5.166297436425000278, -8.110172976325500827 ) ) ;
#44053=CARTESIAN_POINT ( 'NONE',  ( 11.47810404293059960, -4.563346034752700398, -8.647151967355000579 ) ) ;
#44072=CARTESIAN_POINT ( 'NONE',  ( 9.049126402770998112, -2.931626221533000010, -7.097120470443400109 ) ) ;
#44082=DIRECTION ( 'NONE',  ( -0.5000000000000150990, -0.08222066253632250021, 0.8621135439442261239 ) ) ;
#44091=CARTESIAN_POINT ( 'NONE',  ( 11.81056516821459823, -3.390321848206700128, -8.115298063151199059 ) ) ;
#44100=CARTESIAN_POINT ( 'NONE',  ( 11.11486084871780022, -2.792989229543000107, -7.174999999999999822 ) ) ;
#44103=CARTESIAN_POINT ( 'NONE',  ( 9.022188178962251115, -4.591134893453497234, -8.523911321890818016 ) ) ;
#44128=CARTESIAN_POINT ( 'NONE',  ( 11.10887482311539998, -2.815046254222000055, -7.978749413531599721 ) ) ;
#44135=CARTESIAN_POINT ( 'NONE',  ( 9.664763540182335078, -2.782534154164604256, -7.172815144550905408 ) ) ;
#44181=CARTESIAN_POINT ( 'NONE',  ( 10.88351354018293904, -5.249999999999998224, -7.336375382625530683 ) ) ;
#44184=PRODUCT_DEFINITION_CONTEXT ( 'detailed design', #49409, 'design' ) ;
#44188=CARTESIAN_POINT ( 'NONE',  ( 9.178734463322998138, -3.895375416816699854, -8.498947444525299488 ) ) ;
#44205=DIRECTION ( 'NONE',  ( -1.000000000000000000, 0.000000000000000000, 0.000000000000000000 ) ) ;
#44220=CARTESIAN_POINT ( 'NONE',  ( 10.52799293566599914, -3.193321847920899792, -8.489570425681801424 ) ) ;
#44246=CARTESIAN_POINT ( 'NONE',  ( 9.836342523874998633, -5.264483068122999931, -7.306436165809000016 ) ) ;
#44278=CARTESIAN_POINT ( 'NONE',  ( 8.849999778957998942, -4.000000000000000000, -7.500000000000000000 ) ) ;
#44324=CARTESIAN_POINT ( 'NONE',  ( 10.72191429142990060, -3.974927396630719922, -6.183971186511000084 ) ) ;
#44354=CARTESIAN_POINT ( 'NONE',  ( 10.86272200990529946, -5.206705454565000224, -7.079074440652799893 ) ) ;
#44369=ORIENTED_EDGE ( 'NONE', *, *, #63221, .F. ) ;
#44392=AXIS2_PLACEMENT_3D ( 'NONE', #13074, #44205, #54675 ) ;
#44407=CARTESIAN_POINT ( 'NONE',  ( 11.61759063708296047, -2.782734359457999851, -7.842242470354300110 ) ) ;
#44424=CARTESIAN_POINT ( 'NONE',  ( 9.604355082327998616, -4.449513475323099598, -6.601790705997299114 ) ) ;
#44433=ORIENTED_EDGE ( 'NONE', *, *, #16746, .T. ) ;
#44442=CARTESIAN_POINT ( 'NONE',  ( 10.87518447801629939, -3.134012688501500055, -7.480906371072489236 ) ) ;
#44485=CARTESIAN_POINT ( 'NONE',  ( 8.698396402458998367, -4.369105567410300317, -8.298253663472900499 ) ) ;
#44537=EDGE_CURVE ( 'NONE', #14453, #7391, #2448, .T. ) ;
#44540=CARTESIAN_POINT ( 'NONE',  ( 9.533342523874999586, -4.992846242613000030, -7.348017636355000270 ) ) ;
#44542=CARTESIAN_POINT ( 'NONE',  ( 9.833513540183334456, -5.249999999999999112, -7.336375382625531572 ) ) ;
#44558=CARTESIAN_POINT ( 'NONE',  ( 10.40434687351665310, -5.250000000000000888, -7.663624617374465764 ) ) ;
#44562=FILL_AREA_STYLE_COLOUR ( '', #54066 ) ;
#44570=CARTESIAN_POINT ( 'NONE',  ( 11.17901463001529905, -3.302889347096799710, -6.383488688482000128 ) ) ;
#44589=CARTESIAN_POINT ( 'NONE',  ( 8.599999952505998024, -4.000000000000000000, -7.500000000000000000 ) ) ;
#44593=CARTESIAN_POINT ( 'NONE',  ( 10.08963399569799790, -2.728594541839999721, -7.641111829547599932 ) ) ;
#44662=CARTESIAN_POINT ( 'NONE',  ( 8.956149159797568871, -5.077028306801780744, -7.209669135134798346 ) ) ;
#44669=CARTESIAN_POINT ( 'NONE',  ( 11.10612378248509913, -4.482960757953799558, -6.586279795136899651 ) ) ;
#44695=ORIENTED_EDGE ( 'NONE', *, *, #23795, .F. ) ;
#44699=CARTESIAN_POINT ( 'NONE',  ( 11.13349010443639919, -2.725546193138000284, -7.595309363461700158 ) ) ;
#44704=CARTESIAN_POINT ( 'NONE',  ( 10.26990035061499817, -3.768906505327899836, -8.335645555860798694 ) ) ;
#44736=VERTEX_POINT ( 'NONE', #6684 ) ;
#44749=CARTESIAN_POINT ( 'NONE',  ( 11.38379707368349969, -4.566644629509899467, -6.509947486183500054 ) ) ;
#44752=CARTESIAN_POINT ( 'NONE',  ( 11.59999999999999964, -4.862088370180456032, -7.912526219123482640 ) ) ;
#44763=EDGE_CURVE ( 'NONE', #41410, #55747, #27460, .T. ) ;
#44766=CARTESIAN_POINT ( 'NONE',  ( 9.579025935145997650, -4.145841638824199649, -6.506233167833100239 ) ) ;
#44783=CARTESIAN_POINT ( 'NONE',  ( 10.60441638348510018, -4.841589649988700117, -7.294998899090099798 ) ) ;
#44807=CARTESIAN_POINT ( 'NONE',  ( 11.59610237318921477, -4.810409949404850671, -7.174950768514437804 ) ) ;
#44817=CARTESIAN_POINT ( 'NONE',  ( 10.51810807141099779, -3.940954591493389891, -8.776647962565998995 ) ) ;
#44822=CARTESIAN_POINT ( 'NONE',  ( 8.712681907068999365, -4.225805508133200661, -8.364514367444298770 ) ) ;
#44876=CARTESIAN_POINT ( 'NONE',  ( 9.835279731608999043, -3.897539901865500145, -6.362794488108000301 ) ) ;
#44891=CARTESIAN_POINT ( 'NONE',  ( 10.59184687351642751, -3.000416447002275167, -8.268183399968643599 ) ) ;
#44903=CARTESIAN_POINT ( 'NONE',  ( 10.84657802013509986, -5.315911219205999849, -7.469366283838649423 ) ) ;
#44975=CARTESIAN_POINT ( 'NONE',  ( 10.62452888361057113, -4.871957554394390044, -7.561478660064198110 ) ) ;
#45005=CARTESIAN_POINT ( 'NONE',  ( 10.51925056272499859, -2.825232917634000085, -7.517410630436119234 ) ) ;
#45036=CARTESIAN_POINT ( 'NONE',  ( 10.05041772631199848, -3.450375740502100275, -8.631352948887998977 ) ) ;
#45038=VECTOR ( 'NONE', #44082, 1000.000000000000114 ) ;
#45055=CARTESIAN_POINT ( 'NONE',  ( 11.75203632436369894, -5.109717061557999429, -7.240848640331599917 ) ) ;
#45089=CARTESIAN_POINT ( 'NONE',  ( 11.30579707368350029, -4.634832087857400751, -6.390809033205999690 ) ) ;
#45091=ORIENTED_EDGE ( 'NONE', *, *, #17843, .F. ) ;
#45100=CARTESIAN_POINT ( 'NONE',  ( 11.42394752546313441, -4.702246198360438889, -8.603859202887296220 ) ) ;
#45104=CARTESIAN_POINT ( 'NONE',  ( 9.931621437244999129, -3.424116261072899903, -6.851875117168399143 ) ) ;
#45122=CARTESIAN_POINT ( 'NONE',  ( 11.73671932425159881, -4.127012898954600217, -8.356835045446798560 ) ) ;
#45158=CARTESIAN_POINT ( 'NONE',  ( 10.86272200990529946, -5.206705454565000224, -7.079074440652799893 ) ) ;
#45171=CARTESIAN_POINT ( 'NONE',  ( 11.71210404293059959, -4.381818659177399766, -8.277504409418298792 ) ) ;
#45219=CARTESIAN_POINT ( 'NONE',  ( 9.252709346416999381, -2.968569381205999669, -7.010219103474399915 ) ) ;
#45247=CARTESIAN_POINT ( 'NONE',  ( 11.43856039236529831, -2.967715280237000375, -7.550239075043479353 ) ) ;
#45282=CIRCLE ( 'NONE', #15125, 1.249999999999999778 ) ;
#45316=EDGE_CURVE ( 'NONE', #47095, #28041, #11409, .T. ) ;
#45321=CARTESIAN_POINT ( 'NONE',  ( 10.72299000889467635, -4.227343628179307977, -8.344040565988990465 ) ) ;
#45350=CARTESIAN_POINT ( 'NONE',  ( 11.36056039236529891, -3.108928759355700233, -7.543366519014379712 ) ) ;
#45380=CARTESIAN_POINT ( 'NONE',  ( 10.14887885159599890, -2.730985436695000157, -7.348611220446799486 ) ) ;
#45400=CARTESIAN_POINT ( 'NONE',  ( 11.67403632436368888, -4.976178716761900489, -7.272033745815799755 ) ) ;
#45431=CARTESIAN_POINT ( 'NONE',  ( 11.40425819896749893, -5.255890247626999745, -7.736761623643599428 ) ) ;
#45447=CARTESIAN_POINT ( 'NONE',  ( 8.945797255587999430, -2.996487526130999779, -7.457514444071220439 ) ) ;
#45465=CARTESIAN_POINT ( 'NONE',  ( 10.94487616594229884, -4.303437140848100029, -6.543508100188799581 ) ) ;
#45517=CARTESIAN_POINT ( 'NONE',  ( 11.46179707368349909, -4.498457171163099844, -6.629085939160999530 ) ) ;
#45560=VECTOR ( 'NONE', #4964, 1000.000000000000000 ) ;
#45565=CARTESIAN_POINT ( 'NONE',  ( 9.430013376692999216, -5.017903082085999777, -6.982691809975100306 ) ) ;
#45591=CARTESIAN_POINT ( 'NONE',  ( 10.85168717260509830, -4.613789146762799831, -8.501809683958001074 ) ) ;
#45616=CARTESIAN_POINT ( 'NONE',  ( 9.355088727410999283, -5.274736981944999847, -7.606911245136100064 ) ) ;
#45642=ORIENTED_EDGE ( 'NONE', *, *, #26125, .T. ) ;
#45684=CARTESIAN_POINT ( 'NONE',  ( 8.824071121570657539, -3.025928824985223198, -7.248446557932072487 ) ) ;
#45692=CARTESIAN_POINT ( 'NONE',  ( 11.64633327354034797, -4.864904118400500188, -6.934277916748599502 ) ) ;
#45723=ORIENTED_EDGE ( 'NONE', *, *, #40069, .F. ) ;
#45726=CARTESIAN_POINT ( 'NONE',  ( 9.104759580228998672, -4.843256805554699618, -7.298441312785299395 ) ) ;
#45740=CARTESIAN_POINT ( 'NONE',  ( 11.10101463001529964, -3.377766160221900016, -6.503413421344399481 ) ) ;
#45751=DIRECTION ( 'NONE',  ( -1.000000000000000000, 0.000000000000000000, 0.000000000000000000 ) ) ;
#45771=CARTESIAN_POINT ( 'NONE',  ( 10.71503032197929883, -3.256621462143499901, -6.460430507351999196 ) ) ;
#45787=CARTESIAN_POINT ( 'NONE',  ( 9.528367640780999182, -3.526522998810799781, -6.614188603779100006 ) ) ;
#45803=CARTESIAN_POINT ( 'NONE',  ( 10.60026222744819790, -4.774534945026900346, -8.138001937130599828 ) ) ;
#45831=CARTESIAN_POINT ( 'NONE',  ( 8.751496707488000126, -3.918323994020610268, -8.356402621895700378 ) ) ;
#45848=CARTESIAN_POINT ( 'NONE',  ( 9.454862456499625978, -3.587552194319129750, -6.728365969834097626 ) ) ;
#45852=CARTESIAN_POINT ( 'NONE',  ( 11.77359063708300013, -3.044227915785300276, -7.768721787835699999 ) ) ;
#45868=CARTESIAN_POINT ( 'NONE',  ( 11.33810207955129812, -3.203462856645999945, -7.825000000000000178 ) ) ;
#45895=DIRECTION ( 'NONE',  ( 0.000000000000000000, 0.8514547570628037132, -0.5244280662542021298 ) ) ;
#45898=CARTESIAN_POINT ( 'NONE',  ( 8.948759580228999866, -5.110528875107000601, -7.234556850645999404 ) ) ;
#45925=CARTESIAN_POINT ( 'NONE',  ( 11.18923293495519822, -5.032672437899000428, -7.458486839450950256 ) ) ;
#45931=CYLINDRICAL_SURFACE ( 'NONE', #12763, 1.250000000000000222 ) ;
#45935=( NAMED_UNIT ( * ) SI_UNIT ( $, .STERADIAN. ) SOLID_ANGLE_UNIT ( ) );
#45936=EDGE_LOOP ( 'NONE', ( #63445, #57461, #3423, #6128 ) ) ;
#45947=DIRECTION ( 'NONE',  ( 1.000000000000000000, 0.000000000000000000, 0.000000000000000000 ) ) ;
#45949=CARTESIAN_POINT ( 'NONE',  ( 9.101797255588000013, -2.721932483203000075, -7.445890648716809501 ) ) ;
#46020=CARTESIAN_POINT ( 'NONE',  ( 8.876902336861418163, -3.730411824524082043, -6.500155937682547069 ) ) ;
#46028=CARTESIAN_POINT ( 'NONE',  ( 10.73213259636989925, -4.907524392912299582, -7.994504989494399361 ) ) ;
#46029=ORIENTED_EDGE ( 'NONE', *, *, #61787, .F. ) ;
#46051=VECTOR ( 'NONE', #25399, 1000.000000000000114 ) ;
#46065=CARTESIAN_POINT ( 'NONE',  ( 10.25944474310099785, -3.106516218291800246, -7.933599538786499039 ) ) ;
#46078=CARTESIAN_POINT ( 'NONE',  ( 11.22056920625029974, -3.952687217764870198, -6.184582852561999466 ) ) ;
#46109=CARTESIAN_POINT ( 'NONE',  ( 11.41672066707849886, -3.258843737379200078, -7.051685395375099752 ) ) ;
#46110=CARTESIAN_POINT ( 'NONE',  ( 11.01041369783139956, -4.064477673403060543, -8.776385133971000840 ) ) ;
#46127=CARTESIAN_POINT ( 'NONE',  ( 8.791809814040998816, -3.469640109842400122, -8.185876144228299012 ) ) ;
#46147=CARTESIAN_POINT ( 'NONE',  ( 10.47718582084299932, -4.656536239972400182, -6.741111985563299491 ) ) ;
#46196=CARTESIAN_POINT ( 'NONE',  ( 10.77672335273219950, -3.698477709264200275, -8.312023951944400579 ) ) ;
#46245=CARTESIAN_POINT ( 'NONE',  ( 9.151392757686998891, -3.229293331742300044, -8.342464052342599246 ) ) ;
#46274=CARTESIAN_POINT ( 'NONE',  ( 10.64902344389989963, -4.883530143601199747, -6.963800219468099684 ) ) ;
#46276=CARTESIAN_POINT ( 'NONE',  ( 8.807788144226000426, -3.909067355573210278, -8.453461841935100196 ) ) ;
#46309=CARTESIAN_POINT ( 'NONE',  ( 11.41486084871699802, -5.207010770456999893, -7.825000000000000178 ) ) ;
#46323=LINE ( 'NONE', #35826, #16288 ) ;
#46378=CARTESIAN_POINT ( 'NONE',  ( 11.14975833414749928, -4.796537143354000499, -7.825000000000000178 ) ) ;
#46456=CARTESIAN_POINT ( 'NONE',  ( 10.85056919669530018, -3.169300617545700138, -7.745432529082900253 ) ) ;
#46457=CARTESIAN_POINT ( 'NONE',  ( 11.05964426047339799, -3.312306505177499805, -8.577215873335999774 ) ) ;
#46469=CARTESIAN_POINT ( 'NONE',  ( 11.54292372906209074, -2.967457464456211280, -8.269164421058194492 ) ) ;
#46472=CARTESIAN_POINT ( 'NONE',  ( 9.045101285863999863, -4.558267473659599389, -6.836640842107200022 ) ) ;
#46490=LINE ( 'NONE', #35991, #4994 ) ;
#46492=CARTESIAN_POINT ( 'NONE',  ( 11.65871932425156920, -4.147141405561299621, -8.492622906483498824 ) ) ;
#46531=CARTESIAN_POINT ( 'NONE',  ( 9.120327454391752298, -2.808826379911543825, -7.088789390544037339 ) ) ;
#46538=CARTESIAN_POINT ( 'NONE',  ( 10.08809113605762597, -4.810085401003767913, -7.169403702379763210 ) ) ;
#46544=CARTESIAN_POINT ( 'NONE',  ( 11.17056785386839834, -4.718624889240500053, -7.983608166707499620 ) ) ;
#46562=CARTESIAN_POINT ( 'NONE',  ( 10.69809687351600225, -3.672815144550895639, -6.282534154164608253 ) ) ;
#46575=CARTESIAN_POINT ( 'NONE',  ( 9.048601287889788125, -3.999999532294070459, -8.698595322193611423 ) ) ;
#46593=CARTESIAN_POINT ( 'NONE',  ( 9.402671671056999969, -5.261543809652999393, -7.711876388024100137 ) ) ;
#46608=CARTESIAN_POINT ( 'NONE',  ( 11.23052404082913291, -5.045680872279848295, -7.175009054135016662 ) ) ;
#46620=CARTESIAN_POINT ( 'NONE',  ( 10.93990547754509812, -2.967013601007999934, -7.532784233952049213 ) ) ;
#46622=CARTESIAN_POINT ( 'NONE',  ( 8.978248830702483474, -3.044910121894152333, -8.117373328463406423 ) ) ;
#46741=CARTESIAN_POINT ( 'NONE',  ( 8.710288521113000115, -4.352953559891299840, -8.284550957747498501 ) ) ;
#46774=VERTEX_POINT ( 'NONE', #22075 ) ;
#46797=CARTESIAN_POINT ( 'NONE',  ( 11.70794988689359961, -3.544213289744700290, -8.393984925606600811 ) ) ;
#46800=CARTESIAN_POINT ( 'NONE',  ( 11.12299956498149811, -2.792989229543000107, -7.825000000000000178 ) ) ;
#46834=CARTESIAN_POINT ( 'NONE',  ( 10.28441772631199846, -3.627481539113199815, -8.266796319406900295 ) ) ;
#46869=ORIENTED_EDGE ( 'NONE', *, *, #48099, .T. ) ;
#46877=CARTESIAN_POINT ( 'NONE',  ( 9.125583543129625497, -4.871885936991885657, -7.573124426811684629 ) ) ;
#46882=CARTESIAN_POINT ( 'NONE',  ( 11.70379573085659786, -2.893744357957000357, -7.691418046581699919 ) ) ;
#46890=CARTESIAN_POINT ( 'NONE',  ( 10.31059687351633158, -4.629523725463621453, -6.407767014557176566 ) ) ;
#46903=CARTESIAN_POINT ( 'NONE',  ( 10.76059687351620475, -4.629523725463621453, -6.407767014557177454 ) ) ;
#46932=B_SPLINE_CURVE_WITH_KNOTS ( 'NONE', 3,
 ( #51967, #36588, #25406, #46741 ),
 .UNSPECIFIED., .F., .F.,
 ( 4, 4 ),
 ( 0.1836163425310833319, 1.000000000000000000 ),
 .UNSPECIFIED. ) ;
#46933=CARTESIAN_POINT ( 'NONE',  ( 9.579975701332999805, -3.061513547538400104, -8.369268408503399925 ) ) ;
#46960=CARTESIAN_POINT ( 'NONE',  ( 10.82035090130999855, -3.241273085157000189, -7.969278253227299658 ) ) ;
#46970=ORIENTED_EDGE ( 'NONE', *, *, #60528, .T. ) ;
#46988=VERTEX_POINT ( 'NONE', #53396 ) ;
#47041=CARTESIAN_POINT ( 'NONE',  ( 9.458513540183334456, -4.163624617374470205, -8.749999999999998224 ) ) ;
#47057=CARTESIAN_POINT ( 'NONE',  ( 8.849999778957998942, -4.000000000000000000, -8.499999833805500060 ) ) ;
#47060=CARTESIAN_POINT ( 'NONE',  ( 9.571013540182331525, -3.231816600031356845, -8.499583552997725278 ) ) ;
#47095=VERTEX_POINT ( 'NONE', #51925 ) ;
#47115=DIRECTION ( 'NONE',  ( -1.000000000000000000, 0.000000000000000000, 0.000000000000000000 ) ) ;
#47141=CARTESIAN_POINT ( 'NONE',  ( 10.75210807141120029, -3.959980833595939664, -8.365272822098500427 ) ) ;
#47159=CARTESIAN_POINT ( 'NONE',  ( 8.867797255587998251, -3.133765047594600173, -7.463326341748410364 ) ) ;
#47176=CARTESIAN_POINT ( 'NONE',  ( 10.71918447801630059, -2.859536135895000442, -7.474854604063350116 ) ) ;
#47224=CARTESIAN_POINT ( 'NONE',  ( 9.505520750864626223, -4.127043264527912925, -6.634325535862901191 ) ) ;
#47228=CARTESIAN_POINT ( 'NONE',  ( 11.09256785386839894, -4.832509746210599921, -8.060248494254899754 ) ) ;
#47239=B_SPLINE_CURVE_WITH_KNOTS ( 'NONE', 3,
 ( #10235, #48675, #31570, #52889, #779, #26324, #15824, #68962, #16166, #37154, #10577, #50405, #7754, #11600, #49356, #44135, #39222, #38527 ),
 .UNSPECIFIED., .F., .F.,
 ( 4, 2, 2, 2, 2, 2, 2, 2, 4 ),
 ( 0.000000000000000000, 0.1250000000000000000, 0.2500000000000000000, 0.3750000000000000000, 0.5000000000000000000, 0.6250000000000000000, 0.7500000000000000000, 0.8750000000000000000, 1.000000000000000000 ),
 .UNSPECIFIED. ) ;
#47244=CARTESIAN_POINT ( 'NONE',  ( 9.859659112603999631, -4.496147888241900148, -8.528383061402999843 ) ) ;
#47278=CARTESIAN_POINT ( 'NONE',  ( 9.022734463322999332, -3.866750753272200303, -8.772253522581999974 ) ) ;
#47282=CARTESIAN_POINT ( 'NONE',  ( 9.143927823787141307, -2.750011555256801188, -7.499999844943244121 ) ) ;
#47290=DIRECTION ( 'NONE',  ( -0.4999999999999719669, 0.6407827956774649891, -0.5825782426110679424 ) ) ;
#47298=CARTESIAN_POINT ( 'NONE',  ( 11.35502763632549872, -5.160433036184000066, -6.964545474268299508 ) ) ;
#47304=CARTESIAN_POINT ( 'NONE',  ( 11.23589666366019912, -4.039600775206940497, -8.391246537305399045 ) ) ;
#47354=ADVANCED_FACE ( 'NONE', ( #53909 ), #43455, .F. ) ;
#47357=CARTESIAN_POINT ( 'NONE',  ( 9.737988259786000356, -4.113440707072600233, -8.359557531806398600 ) ) ;
#47368=VERTEX_POINT ( 'NONE', #66125 ) ;
#47371=CARTESIAN_POINT ( 'NONE',  ( 11.05946005378019947, -2.963614890480000152, -6.946587256304699309 ) ) ;
#47407=CARTESIAN_POINT ( 'NONE',  ( 10.77879632507499785, -3.576455950783300253, -8.285174533868300273 ) ) ;
#47455=CARTESIAN_POINT ( 'NONE',  ( 10.96914282210478042, -3.732132604854249802, -6.667932297870764913 ) ) ;
#47485=CARTESIAN_POINT ( 'NONE',  ( 10.94903032197929882, -3.496160833528699996, -6.795411691360399686 ) ) ;
#47523=CARTESIAN_POINT ( 'NONE',  ( 11.38379707368349969, -4.566644629509899467, -6.509947486183500054 ) ) ;
#47524=VERTEX_POINT ( 'NONE', #24171 ) ;
#47576=CARTESIAN_POINT ( 'NONE',  ( 10.99410672858429905, -4.801902424331299990, -6.896755974168000236 ) ) ;
#47592=CARTESIAN_POINT ( 'NONE',  ( 10.44222949779799947, -3.366547096154099972, -8.449985803660998940 ) ) ;
#47606=CARTESIAN_POINT ( 'NONE',  ( 9.065735834902588053, -3.588654020114534049, -8.662764376609992212 ) ) ;
#47621=CARTESIAN_POINT ( 'NONE',  ( 8.499265421555000088, -4.240073379563900069, -8.741861511046000288 ) ) ;
#47644=CARTESIAN_POINT ( 'NONE',  ( 10.57149279008999798, -4.296686446741600385, -8.601484120896000007 ) ) ;
#47701=CARTESIAN_POINT ( 'NONE',  ( 9.813975701332999790, -3.363922674822000136, -8.089163458558500608 ) ) ;
#47716=CARTESIAN_POINT ( 'NONE',  ( 10.73724174883999893, -4.024531238983009906, -8.391788556008700439 ) ) ;
#47724=CARTESIAN_POINT ( 'NONE',  ( 8.734997988989999129, -4.062652182992059657, -8.366433385397400002 ) ) ;
#47766=ORIENTED_EDGE ( 'NONE', *, *, #48099, .F. ) ;
#47834=CARTESIAN_POINT ( 'NONE',  ( 11.58487348028854846, -4.882707455860599843, -7.977261354519500358 ) ) ;
#47854=EDGE_CURVE ( 'NONE', #48162, #46774, #38812, .T. ) ;
#47869=CARTESIAN_POINT ( 'NONE',  ( 10.30072469555899950, -3.429147315060100176, -6.512367818249299667 ) ) ;
#47905=ORIENTED_EDGE ( 'NONE', *, *, #26760, .T. ) ;
#47916=CARTESIAN_POINT ( 'NONE',  ( 11.31410538575739899, -3.024036709177600368, -7.266662245194900116 ) ) ;
#47928=CARTESIAN_POINT ( 'NONE',  ( 10.07309687351575178, -2.782534154164605589, -7.827184855449103473 ) ) ;
#47931=CARTESIAN_POINT ( 'NONE',  ( 10.11295058442699890, -3.546800160410199965, -6.451980747609000311 ) ) ;
#47950=CARTESIAN_POINT ( 'NONE',  ( 11.25361999289386716, -4.544092497359195626, -6.342116603374311268 ) ) ;
#47962=CARTESIAN_POINT ( 'NONE',  ( 8.718784697134999817, -3.305825103746500293, -6.425520776924999566 ) ) ;
#47982=CARTESIAN_POINT ( 'NONE',  ( 11.23610538575739959, -2.890527834009000152, -7.234742334405199315 ) ) ;
#47987=CARTESIAN_POINT ( 'NONE',  ( 10.61257802013489737, -4.891884252872400474, -7.479237407015119743 ) ) ;
#47989=CARTESIAN_POINT ( 'NONE',  ( 11.59999999999999964, -3.983295036746754558, -6.452290402036156891 ) ) ;
#48027=CARTESIAN_POINT ( 'NONE',  ( 10.55518582084299872, -4.566724035220099509, -6.844925608615599621 ) ) ;
#48037=CARTESIAN_POINT ( 'NONE',  ( 8.876797255587998592, -3.133765047594600173, -7.463326341748410364 ) ) ;
#48054=CARTESIAN_POINT ( 'NONE',  ( 10.44125056272499918, -2.966599088466999934, -7.515315513715298934 ) ) ;
#48069=CARTESIAN_POINT ( 'NONE',  ( 9.448096873516666605, -4.327184855449103473, -8.717465845835395299 ) ) ;
#48071=ORIENTED_EDGE ( 'NONE', *, *, #24503, .T. ) ;
#48079=ORIENTED_EDGE ( 'NONE', *, *, #43882, .T. ) ;
#48097=DIRECTION ( 'NONE',  ( 0.000000000000000000, 1.000000000000000000, 0.000000000000000000 ) ) ;
#48099=EDGE_CURVE ( 'NONE', #14453, #13264, #36198, .T. ) ;
#48110=DIRECTION ( 'NONE',  ( -1.000000000000000000, 0.000000000000000000, 0.000000000000000000 ) ) ;
#48162=VERTEX_POINT ( 'NONE', #36075 ) ;
#48168=CARTESIAN_POINT ( 'NONE',  ( 11.62994988689359843, -3.481863023525599843, -8.516279404258998653 ) ) ;
#48202=CARTESIAN_POINT ( 'NONE',  ( 11.28533594839949750, -3.249987070165300196, -6.640482273977399430 ) ) ;
#48238=CARTESIAN_POINT ( 'NONE',  ( 9.293111399473126255, -5.011294126480321687, -6.748153640515438312 ) ) ;
#48249=CARTESIAN_POINT ( 'NONE',  ( 10.92026088462129962, -3.997864853650589634, -6.496532863517000322 ) ) ;
#48265=CARTESIAN_POINT ( 'NONE',  ( 10.11093802597399893, -4.522194782554399772, -6.642005297568199573 ) ) ;
#48267=B_SPLINE_CURVE_WITH_KNOTS ( 'NONE', 3,
 ( #63907, #16019, #37348, #32118, #53433, #5530, #41223, #19897, #14655, #35971 ),
 .UNSPECIFIED., .F., .F.,
 ( 4, 2, 2, 2, 4 ),
 ( 0.000000000000000000, 0.2500000000000006661, 0.5000000000000013323, 0.7500000000000006661, 1.000000000000000000 ),
 .UNSPECIFIED. ) ;
#48286=ORIENTED_EDGE ( 'NONE', *, *, #32793, .F. ) ;
#48294=CARTESIAN_POINT ( 'NONE',  ( 9.035395982797805203, -4.311073552809154386, -8.654212551762981320 ) ) ;
#48299=CARTESIAN_POINT ( 'NONE',  ( 11.33830977893730108, -4.976598135215292373, -6.673569913327194847 ) ) ;
#48320=CARTESIAN_POINT ( 'NONE',  ( 10.52226222744799955, -4.880489021643899861, -8.225278704382400718 ) ) ;
#48325=CARTESIAN_POINT ( 'NONE',  ( 8.712501735000000025, -4.358851904410700584, -8.276078370613198842 ) ) ;
#48327=CARTESIAN_POINT ( 'NONE',  ( 10.90346005378009941, -3.213042707518099839, -7.079777642108599167 ) ) ;
#48379=CARTESIAN_POINT ( 'NONE',  ( 9.735975701333000387, -3.263119632394099856, -8.182531775206799196 ) ) ;
#48388=CARTESIAN_POINT ( 'NONE',  ( 10.99999970531878013, -5.098631745860898512, -7.597293174631950308 ) ) ;
#48394=CARTESIAN_POINT ( 'NONE',  ( 10.89835090130999973, -3.121033016283800254, -8.043647632228999811 ) ) ;
#48410=CARTESIAN_POINT ( 'NONE',  ( 10.27101354018233437, -4.768183399968641822, -6.500416447002272058 ) ) ;
#48507=ORIENTED_EDGE ( 'NONE', *, *, #11583, .T. ) ;
#48513=CARTESIAN_POINT ( 'NONE',  ( 11.70379573085659786, -2.893744357957000357, -7.691418046581699919 ) ) ;
#48517=CARTESIAN_POINT ( 'NONE',  ( 11.47500581613029880, -3.011381429075500105, -8.134817373646898275 ) ) ;
#48532=EDGE_CURVE ( 'NONE', #8437, #26260, #46323, .T. ) ;
#48551=CARTESIAN_POINT ( 'NONE',  ( 10.91610672858429965, -4.911600290708499905, -6.814233985789400094 ) ) ;
#48581=ADVANCED_FACE ( 'NONE', ( #61706 ), #41071, .T. ) ;
#48601=CARTESIAN_POINT ( 'NONE',  ( 10.69456919669529960, -2.906008650422999828, -7.823222900359999343 ) ) ;
#48614=CARTESIAN_POINT ( 'NONE',  ( 9.927263540182998725, -4.629523725463626782, -8.592232985442821658 ) ) ;
#48619=CARTESIAN_POINT ( 'NONE',  ( 8.947809814040999399, -3.301541394817099739, -8.403266072559899769 ) ) ;
#48647=EDGE_LOOP ( 'NONE', ( #63236, #4782, #39384, #1752, #3973, #64824, #29335 ) ) ;
#48649=CARTESIAN_POINT ( 'NONE',  ( 11.54684497800060150, -4.976842342332563618, -7.824998645711865208 ) ) ;
#48661=CARTESIAN_POINT ( 'NONE',  ( 8.748821772879614045, -3.697635112905263366, -8.374063393888503626 ) ) ;
#48667=CARTESIAN_POINT ( 'NONE',  ( 11.62579573085663043, -2.760622544769000264, -7.714452430741599365 ) ) ;
#48675=CARTESIAN_POINT ( 'NONE',  ( 9.883513540182333301, -5.249999999999998224, -7.336375382625530683 ) ) ;
#48692=CARTESIAN_POINT ( 'NONE',  ( 9.508513540182335078, -4.163624617374471093, -8.749999999999998224 ) ) ;
#48730=CARTESIAN_POINT ( 'NONE',  ( 9.406696787962999906, -3.827518619249500098, -6.510508982544899403 ) ) ;
#48743=CARTESIAN_POINT ( 'NONE',  ( 10.37199293566600034, -3.366612813978900220, -8.276990458557699881 ) ) ;
#48749=CARTESIAN_POINT ( 'NONE',  ( 8.762289945692000259, -4.238022715896200054, -8.411288920148800585 ) ) ;
#48758=CARTESIAN_POINT ( 'NONE',  ( 10.29184687351566829, -4.999583552997724389, -6.731816600031356401 ) ) ;
#48788=CARTESIAN_POINT ( 'NONE',  ( 8.599999952505998024, -3.250000006358199744, -7.500000000000000000 ) ) ;
#48813=DIRECTION ( 'NONE',  ( 0.7071067388045961799, 0.7071068235684964121, -1.176037761303994353E-10 ) ) ;
#48821=CARTESIAN_POINT ( 'NONE',  ( 10.97755399909358154, -3.866653594937912608, -8.778526265510096849 ) ) ;
#48831=CARTESIAN_POINT ( 'NONE',  ( 11.08126742035591228, -4.768619073576778611, -7.106626190113856545 ) ) ;
#48853=CYLINDRICAL_SURFACE ( 'NONE', #63805, 1.250000000000000222 ) ;
#48861=CARTESIAN_POINT ( 'NONE',  ( 10.99410672858429905, -4.801902424331299990, -6.896755974168000236 ) ) ;
#48888=CARTESIAN_POINT ( 'NONE',  ( 11.40221299665285670, -3.091095606691090847, -7.824988380119695996 ) ) ;
#48897=CARTESIAN_POINT ( 'NONE',  ( 11.37964291764649971, -5.268358781405000357, -7.343212302062899433 ) ) ;
#48902=CARTESIAN_POINT ( 'NONE',  ( 10.91301932002725650, -5.250000000000000888, -7.799851088612626882 ) ) ;
#48948=CARTESIAN_POINT ( 'NONE',  ( 10.49764694612699856, -5.059486515935999407, -7.922821994243300914 ) ) ;
#48958=CARTESIAN_POINT ( 'NONE',  ( 10.02101354018262569, -3.231816600031356845, -8.499583552997725278 ) ) ;
#48961=CARTESIAN_POINT ( 'NONE',  ( 9.530380199233999150, -2.867101906753999785, -7.357604921762999517 ) ) ;
#48983=LINE ( 'NONE', #54574, #37409 ) ;
#49004=CARTESIAN_POINT ( 'NONE',  ( 11.00000000000000000, -5.058572498595999889, -7.825000000000000178 ) ) ;
#49005=CARTESIAN_POINT ( 'NONE',  ( 11.07907162307749793, -4.814611760850799449, -7.174999999999999822 ) ) ;
#49012=CARTESIAN_POINT ( 'NONE',  ( 10.54272335273199879, -3.555125495332600138, -8.698083075453000745 ) ) ;
#49034=CARTESIAN_POINT ( 'NONE',  ( 9.393930206848999376, -5.250000000000000000, -7.500000000000000000 ) ) ;
#49069=CARTESIAN_POINT ( 'NONE',  ( 9.001430433046998303, -4.854750075120300323, -6.972511033848699746 ) ) ;
#49084=CARTESIAN_POINT ( 'NONE',  ( 11.02301463001509774, -3.452642973349600464, -6.623338154204899908 ) ) ;
#49097=FACE_OUTER_BOUND ( 'NONE', #22666, .T. ) ;
#49099=CARTESIAN_POINT ( 'NONE',  ( 10.23976354018233259, -4.327184855449098144, -6.282534154164605589 ) ) ;
#49169=CARTESIAN_POINT ( 'NONE',  ( 10.31021345716899873, -3.363461959113699606, -8.078719053813800954 ) ) ;
#49200=CARTESIAN_POINT ( 'NONE',  ( 11.28533594839949750, -3.249987070165300196, -6.640482273977399430 ) ) ;
#49204=CARTESIAN_POINT ( 'NONE',  ( 11.72433327354039889, -4.983220429128399687, -6.856888818507299810 ) ) ;
#49231=CARTESIAN_POINT ( 'NONE',  ( 11.55194988689359903, -3.419512757306400363, -8.638573882912000457 ) ) ;
#49253=CARTESIAN_POINT ( 'NONE',  ( 11.59456039236534330, -2.685288321999000249, -7.563984187103470092 ) ) ;
#49260=VERTEX_POINT ( 'NONE', #27671 ) ;
#49270=CARTESIAN_POINT ( 'NONE',  ( 9.343930206849998754, -5.250000000000000000, -7.500000000000000000 ) ) ;
#49283=CARTESIAN_POINT ( 'NONE',  ( 10.66995391537419913, -3.056324258617099776, -8.140910455049299443 ) ) ;
#49297=CARTESIAN_POINT ( 'NONE',  ( 9.733013376692998264, -5.017903082085999777, -6.982691809975100306 ) ) ;
#49314=CARTESIAN_POINT ( 'NONE',  ( 11.83518044953559922, -3.231951024059400268, -7.900497508315099893 ) ) ;
#49348=CARTESIAN_POINT ( 'NONE',  ( 10.76426088462129904, -3.997280690308189666, -6.221990224628999755 ) ) ;
#49356=CARTESIAN_POINT ( 'NONE',  ( 9.685596873515667227, -2.907767014557174790, -6.870476274536379435 ) ) ;
#49409=APPLICATION_CONTEXT ( 'automotive_design' ) ;
#49410=CARTESIAN_POINT ( 'NONE',  ( 9.508013376692998619, -4.895413217368500547, -7.044942343771899651 ) ) ;
#49438=CARTESIAN_POINT ( 'NONE',  ( 10.59725056272499977, -2.683866746800999792, -7.519505747156228992 ) ) ;
#49466=FACE_OUTER_BOUND ( 'NONE', #61004, .T. ) ;
#49512=CARTESIAN_POINT ( 'NONE',  ( 10.69837472757367713, -4.473492782822720670, -8.234774922628410820 ) ) ;
#49541=CARTESIAN_POINT ( 'NONE',  ( 10.21462282008599942, -3.476853648246800432, -8.343818446627699004 ) ) ;
#49545=CARTESIAN_POINT ( 'NONE',  ( 11.38678751119029897, -5.166297436425000278, -8.110172976325500827 ) ) ;
#49563=DIRECTION ( 'NONE',  ( 1.000000000000000000, 0.000000000000000000, 0.000000000000000000 ) ) ;
#49579=CARTESIAN_POINT ( 'NONE',  ( 10.13662282008599824, -3.405288783432600219, -8.459250300176799797 ) ) ;
#49617=ORIENTED_EDGE ( 'NONE', *, *, #56184, .F. ) ;
#49632=CARTESIAN_POINT ( 'NONE',  ( 11.23610538575739959, -2.890527834009000152, -7.234742334405199315 ) ) ;
#49634=EDGE_LOOP ( 'NONE', ( #52929, #53239, #3516, #39828 ) ) ;
#49636=CARTESIAN_POINT ( 'NONE',  ( 11.60000000000000320, -4.689830048140306573, -8.238968815098687060 ) ) ;
#49649=CARTESIAN_POINT ( 'NONE',  ( 9.378405316141000370, -4.242421256336299962, -8.615780615741000403 ) ) ;
#49666=CARTESIAN_POINT ( 'NONE',  ( 11.66287348028854964, -4.761955701524100526, -7.911973420841600380 ) ) ;
#49756=CARTESIAN_POINT ( 'NONE',  ( 10.82101354018296391, -4.768183399968640934, -6.500416447002272946 ) ) ;
#49761=ORIENTED_EDGE ( 'NONE', *, *, #58869, .T. ) ;
#49763=CARTESIAN_POINT ( 'NONE',  ( 9.761304848515999666, -3.086535948898899928, -7.917643062525700159 ) ) ;
#49780=CARTESIAN_POINT ( 'NONE',  ( 10.50851354018319128, -4.163624617374471093, -8.749999999999998224 ) ) ;
#49818=CARTESIAN_POINT ( 'NONE',  ( 10.44424205625099944, -4.458751122174599679, -8.694123841252999085 ) ) ;
#49897=CARTESIAN_POINT ( 'NONE',  ( 11.60988784977536348, -4.851105903694400645, -7.451365240271489832 ) ) ;
#49929=CARTESIAN_POINT ( 'NONE',  ( 10.56733863405299800, -3.211524470605299886, -8.505794571537999005 ) ) ;
#49955=ORIENTED_EDGE ( 'NONE', *, *, #23599, .T. ) ;
#49982=CARTESIAN_POINT ( 'NONE',  ( 10.42380110216399913, -4.973546009874400653, -6.905442784147899360 ) ) ;
#49988=CARTESIAN_POINT ( 'NONE',  ( 11.59999999999999787, -4.874497702741446226, -7.869208573981368637 ) ) ;
#50000=CARTESIAN_POINT ( 'NONE',  ( 9.629684229509999582, -4.708027397558999461, -6.787581931282099745 ) ) ;
#50018=CARTESIAN_POINT ( 'NONE',  ( 11.51518179236248862, -4.180996681294200101, -6.652923384986699773 ) ) ;
#50022=CIRCLE ( 'NONE', #35497, 1.250000000000000888 ) ;
#50055=CARTESIAN_POINT ( 'NONE',  ( 10.81349144726329925, -4.738947899111299655, -6.457276458983999490 ) ) ;
#50081=EDGE_LOOP ( 'NONE', ( #66975, #4924, #55545 ) ) ;
#50115=CARTESIAN_POINT ( 'NONE',  ( 8.999417874593998334, -5.050800927762999493, -7.946712276748498560 ) ) ;
#50116=CARTESIAN_POINT ( 'NONE',  ( 9.843930206850000530, -5.250000000000000000, -7.500000000000000000 ) ) ;
#50141=CARTESIAN_POINT ( 'NONE',  ( 9.893930206848997599, -5.250000000000000000, -7.500000000000000000 ) ) ;
#50144=CARTESIAN_POINT ( 'NONE',  ( 11.42834208742529967, -4.706521750018099581, -8.610579932818998472 ) ) ;
#50169=CARTESIAN_POINT ( 'NONE',  ( 10.26693802597399952, -4.665064168510499876, -6.407263051216999017 ) ) ;
#50208=CARTESIAN_POINT ( 'NONE',  ( 11.59999999999999964, -4.000000000000000000, -7.500000000000000000 ) ) ;
#50236=CARTESIAN_POINT ( 'NONE',  ( 8.962753061708914615, -5.112753122729035482, -7.353476507976679954 ) ) ;
#50243=CARTESIAN_POINT ( 'NONE',  ( 11.02812378248509795, -4.416893162838900544, -6.711274001288999536 ) ) ;
#50276=CARTESIAN_POINT ( 'NONE',  ( 11.15810538575740019, -2.757018958839999812, -7.202822423614300362 ) ) ;
#50297=CARTESIAN_POINT ( 'NONE',  ( 11.17901463001529905, -3.302889347096799710, -6.383488688482000128 ) ) ;
#50329=CARTESIAN_POINT ( 'NONE',  ( 10.83810672858429847, -5.021298157087000114, -6.731711997412900494 ) ) ;
#50343=ORIENTED_EDGE ( 'NONE', *, *, #61893, .F. ) ;
#50345=CARTESIAN_POINT ( 'NONE',  ( 10.00760887879199856, -4.196341783741199372, -6.655513263298900029 ) ) ;
#50363=CARTESIAN_POINT ( 'NONE',  ( 10.80133863405319872, -3.465595476214000215, -8.181696703306599261 ) ) ;
#50364=ORIENTED_EDGE ( 'NONE', *, *, #27928, .F. ) ;
#50388=CARTESIAN_POINT ( 'NONE',  ( 11.00000000000000000, -5.058572498595999889, -7.825000000000000178 ) ) ;
#50394=EDGE_LOOP ( 'NONE', ( #60503, #47905, #56575, #28560 ) ) ;
#50396=CARTESIAN_POINT ( 'NONE',  ( 10.73964560330029983, -3.608363763633400279, -6.283473206644000442 ) ) ;
#50405=CARTESIAN_POINT ( 'NONE',  ( 9.727263540182331525, -3.370476274536371442, -6.407767014557179230 ) ) ;
#50409=CARTESIAN_POINT ( 'NONE',  ( 11.76133460557259980, -3.860150918677800025, -8.354833838171700222 ) ) ;
#50452=CARTESIAN_POINT ( 'NONE',  ( 8.568822372493999140, -4.328199826929600036, -8.573651380901999630 ) ) ;
#50476=CARTESIAN_POINT ( 'NONE',  ( 11.58810207955109917, -4.796537143354000499, -7.174999999999999822 ) ) ;
#50480=CARTESIAN_POINT ( 'NONE',  ( 10.76857802013509868, -5.174568897094999897, -7.472656658230009796 ) ) ;
#50568=CARTESIAN_POINT ( 'NONE',  ( 9.343930206849998754, -5.250000000000000000, -7.500000000000000000 ) ) ;
#50590=CARTESIAN_POINT ( 'NONE',  ( 11.06456920625009843, -3.962850971080120299, -6.467161360063999886 ) ) ;
#50599=ORIENTED_EDGE ( 'NONE', *, *, #66861, .F. ) ;
#50639=CARTESIAN_POINT ( 'NONE',  ( 10.76857802013509868, -5.174568897094999897, -7.472656658230009796 ) ) ;
#50673=CARTESIAN_POINT ( 'NONE',  ( 11.04749144726329924, -4.500836215462999945, -6.793273974143599681 ) ) ;
#50674=CARTESIAN_POINT ( 'NONE',  ( 11.25656651104150008, -3.873914634362100262, -6.228222165170999247 ) ) ;
#50690=CARTESIAN_POINT ( 'NONE',  ( 9.325734463322998380, -3.895375416816699854, -8.498947444525299488 ) ) ;
#50707=CARTESIAN_POINT ( 'NONE',  ( 11.63410404293056999, -4.442327784369100030, -8.400720262063998689 ) ) ;
#50747=CARTESIAN_POINT ( 'NONE',  ( 8.741252916288999586, -3.907441415015589836, -8.374574604871998673 ) ) ;
#50750=CARTESIAN_POINT ( 'NONE',  ( 10.17726354018233081, -3.370476274536371442, -6.407767014557179230 ) ) ;
#50755=CARTESIAN_POINT ( 'NONE',  ( 11.51102763632551884, -4.911148285670300595, -7.079572058049399708 ) ) ;
#50805=CARTESIAN_POINT ( 'NONE',  ( 9.733963142879998642, -2.882742046518000034, -7.264481182560499128 ) ) ;
#50822=CARTESIAN_POINT ( 'NONE',  ( 11.00000000000000000, -4.000000000000000000, -7.500000000000000000 ) ) ;
#50829=CARTESIAN_POINT ( 'NONE',  ( 11.01790547754519878, -2.825704134258000266, -7.537269019642879542 ) ) ;
#50831=CARTESIAN_POINT ( 'NONE',  ( 9.051300837857860770, -2.809882456706737308, -7.723566111296684689 ) ) ;
#50854=CARTESIAN_POINT ( 'NONE',  ( 9.051138961223999857, -2.940105638081000006, -8.216246114996598848 ) ) ;
#50859=VERTEX_POINT ( 'NONE', #12859 ) ;
#50931=CARTESIAN_POINT ( 'NONE',  ( 11.52166954483529793, -3.437903757373499847, -6.632714178206799538 ) ) ;
#50982=CARTESIAN_POINT ( 'NONE',  ( 11.39700581613019992, -3.130347327833300053, -8.058426314824099990 ) ) ;
#50993=CYLINDRICAL_SURFACE ( 'NONE', #17659, 1.250000000000000222 ) ;
#51013=CARTESIAN_POINT ( 'NONE',  ( 11.03502897915239878, -3.672866099873000056, -8.735435061820998826 ) ) ;
#51028=CARTESIAN_POINT ( 'NONE',  ( 11.36486084871759950, -5.207010770456999893, -7.825000000000000178 ) ) ;
#51031=CARTESIAN_POINT ( 'NONE',  ( 9.351063610504999346, -3.588011994494999968, -8.416028484082099581 ) ) ;
#51048=CARTESIAN_POINT ( 'NONE',  ( 11.24025954179439957, -3.228187097503200320, -8.141292208271599051 ) ) ;
#51093=CARTESIAN_POINT ( 'NONE',  ( 9.201570984676626708, -4.444002162597382011, -8.253919324947762703 ) ) ;
#51098=CARTESIAN_POINT ( 'NONE',  ( 10.89979975933730039, -3.180925410802600162, -7.218192605361100078 ) ) ;
#51120=CARTESIAN_POINT ( 'NONE',  ( 10.89393020684959978, -5.250000000000000000, -7.500000000000000000 ) ) ;
#51148=CARTESIAN_POINT ( 'NONE',  ( 9.303367640780999537, -3.461752753411900141, -6.493012239633999982 ) ) ;
#51176=CARTESIAN_POINT ( 'NONE',  ( 10.89324174884020024, -4.032306468273969990, -8.674442868902998427 ) ) ;
#51182=FACE_OUTER_BOUND ( 'NONE', #49634, .T. ) ;
#51191=CARTESIAN_POINT ( 'NONE',  ( 8.731616107288068918, -3.999997736744774546, -8.381579007094499545 ) ) ;
#51201=CARTESIAN_POINT ( 'NONE',  ( 9.684367640780997988, -3.396982508013000501, -6.371835875489000323 ) ) ;
#51205=VERTEX_POINT ( 'NONE', #46309 ) ;
#51234=CYLINDRICAL_SURFACE ( 'NONE', #8873, 1.250000000000000222 ) ;
#51274=CARTESIAN_POINT ( 'NONE',  ( 10.85679632507500081, -3.509334349252600127, -8.409605917786398877 ) ) ;
#51304=CARTESIAN_POINT ( 'NONE',  ( 10.09964828895399869, -2.878385131502000149, -8.112615456209400833 ) ) ;
#51307=CARTESIAN_POINT ( 'NONE',  ( 8.724822372493999723, -4.249211653873900651, -8.315254653915399530 ) ) ;
#51323=CARTESIAN_POINT ( 'NONE',  ( 10.85168717260509830, -4.613789146762799831, -8.501809683958001074 ) ) ;
#51345=B_SPLINE_SURFACE_WITH_KNOTS ( 'NONE', 3, 3, ( 
 ( #11496, #27943, #60096, #38419, #59744, #12895, #34224, #49253, #1362, #55543, #677, #22680, #44024, #21988, #16742, #67386, #46078, #50297, #19508, #24065, #8674, #66362, #13927, #9010, #24753, #56226, #15553, #61131, #23719, #40156, #2739, #40826, #62151, #14269, #35597 ),
 ( #56911, #45055, #3079, #7641, #2395, #29679, #24412, #35254, #4698, #26044, #56570, #42124, #30021, #29326, #30351, #63432, #68676, #45740, #47371, #52605, #13248, #18483, #28989, #51323, #67050, #50639, #20794, #19159, #61472, #40483, #36881, #3418, #39809, #34573, #13591 ),
 ( #55889, #45400, #7993, #66709, #61810, #18830, #34911, #8335, #50982, #69028, #32666, #15886, #27418, #17269, #22163, #500, #53977, #49084, #65148, #38243, #48394, #155, #10641, #37217, #63775, #33008, #42808, #58534, #21141, #58197, #16230, #48054, #16576, #48743, #53298 ),
 ( #31985, #42466, #37554, #21816, #5401, #21473, #6081, #59223, #26737, #58885, #27774, #43149, #64115, #10989, #64454, #32329, #846, #43503, #31634, #64801, #53640, #11325, #47716, #37901, #59570, #16912, #5736, #10299, #27077, #5052, #11668, #54323, #6422, #1195, #22504 ) ),
 .UNSPECIFIED., .F., .F., .F.,
 ( 4, 4 ),
 ( 4, 1, 1, 1, 1, 1, 1, 1, 1, 1, 1, 1, 1, 1, 1, 1, 1, 1, 1, 1, 1, 1, 1, 1, 1, 1, 1, 1, 1, 1, 1, 1, 4 ),
 ( -0.02000000000000000042, 1.020000000000000018 ),
 ( 0.1633025096610999927, 0.1899619885200000136, 0.2166214673788000034, 0.2432809462376999965, 0.2699404250964999585, 0.2965999039553000038, 0.3232593828141999692, 0.3499188616730000145, 0.3765783405318000043, 0.4032378193906999697, 0.4298972982494999595, 0.4565567771083000048, 0.4832162559671999702, 0.5098757348260000155, 0.5365352136848999809, 0.5631946925437000262, 0.5898541714025000715, 0.6165136502614000369, 0.6431731291201999712, 0.6698326079790000165, 0.6964920868378999819, 0.7231515656967000272, 0.7498110445554999615, 0.7764705234143999268, 0.8031300022731999722, 0.8297894811320000175, 0.8564489599908999828, 0.8831084388497000282, 0.9097679177085999935, 0.9364273965674000388, 0.9630868754261999731, 0.9897463542851000495, 1.016405833144000015 ),
 .UNSPECIFIED. ) ;
#51354=CARTESIAN_POINT ( 'NONE',  ( 10.73964560330029983, -3.608363763633400279, -6.283473206644000442 ) ) ;
#51370=CARTESIAN_POINT ( 'NONE',  ( 9.452380199233999747, -3.003429752324399793, -7.374740103075099640 ) ) ;
#51389=CARTESIAN_POINT ( 'NONE',  ( 10.52641638348499953, -4.974961480482700260, -7.262511127784999410 ) ) ;
#51423=CARTESIAN_POINT ( 'NONE',  ( 11.41486084871699802, -5.207010770456999893, -7.825000000000000178 ) ) ;
#51432=CARTESIAN_POINT ( 'NONE',  ( 9.733483075504627990, -4.114479073428862321, -8.367425391989351979 ) ) ;
#51436=CARTESIAN_POINT ( 'NONE',  ( 10.45672469555900008, -3.566534988568399900, -6.750062220519700062 ) ) ;
#51481=CARTESIAN_POINT ( 'NONE',  ( 9.379355082327998971, -4.511005581663400044, -6.478918346312998899 ) ) ;
#51507=CARTESIAN_POINT ( 'NONE',  ( 10.47769598648999967, -2.990523684589000197, -8.101059042556599366 ) ) ;
#51516=B_SPLINE_CURVE_WITH_KNOTS ( 'NONE', 3,
 ( #31213, #52517, #62659, #31547 ),
 .UNSPECIFIED., .F., .F.,
 ( 4, 4 ),
 ( 0.000000000000000000, 0.8163836489557126930 ),
 .UNSPECIFIED. ) ;
#51567=DIRECTION ( 'NONE',  ( -1.000000000000000000, 0.000000000000000000, 0.000000000000000000 ) ) ;
#51687=CARTESIAN_POINT ( 'NONE',  ( 11.68748876160954886, -4.600381688599499697, -8.124372018288600117 ) ) ;
#51688=CARTESIAN_POINT ( 'NONE',  ( 11.35502763632549872, -5.160433036184000066, -6.964545474268299508 ) ) ;
#51707=CARTESIAN_POINT ( 'NONE',  ( 8.969113844317998741, -3.781046324972699768, -6.661091642253600398 ) ) ;
#51726=CARTESIAN_POINT ( 'NONE',  ( 11.19102897915239936, -3.743141152489600110, -8.470038342183499935 ) ) ;
#51762=LINE ( 'NONE', #51423, #20466 ) ;
#51771=CARTESIAN_POINT ( 'NONE',  ( 10.31021345716899873, -3.363461959113699606, -8.078719053813800954 ) ) ;
#51775=CARTESIAN_POINT ( 'NONE',  ( 10.67826222744820086, -4.668580868411999596, -8.050725169876500331 ) ) ;
#51794=CARTESIAN_POINT ( 'NONE',  ( 10.72934687351609817, -4.163624617374463099, -6.249999999999998224 ) ) ;
#51821=CARTESIAN_POINT ( 'NONE',  ( 9.352013376692999813, -5.140392946802999852, -6.920441276178300072 ) ) ;
#51849=CARTESIAN_POINT ( 'NONE',  ( 11.06456920625009843, -3.962850971080120299, -6.467161360063999886 ) ) ;
#51850=CARTESIAN_POINT ( 'NONE',  ( 11.60000000000000320, -2.860800829850470794, -7.074412716661199418 ) ) ;
#51925=CARTESIAN_POINT ( 'NONE',  ( 10.64393020684969926, -2.750000000000000000, -7.500000000000000000 ) ) ;
#51941=DIRECTION ( 'NONE',  ( 0.7071067617951957152, 0.000000000000000000, -0.7071068005778986532 ) ) ;
#51967=CARTESIAN_POINT ( 'NONE',  ( 8.731616107288068918, -3.999997736744774546, -8.381579007094499545 ) ) ;
#51999=CARTESIAN_POINT ( 'NONE',  ( 11.59999999999999964, -4.000000000000000000, -7.500000000000000000 ) ) ;
#52003=ORIENTED_EDGE ( 'NONE', *, *, #6066, .F. ) ;
#52026=CARTESIAN_POINT ( 'NONE',  ( 11.36333594839950045, -3.340240242524600056, -6.743912759487099784 ) ) ;
#52062=CARTESIAN_POINT ( 'NONE',  ( 10.42795525820099911, -4.094749303624469761, -6.501013802764199490 ) ) ;
#52111=CARTESIAN_POINT ( 'NONE',  ( 9.632166486775625813, -4.862862160676565182, -7.644917771834661480 ) ) ;
#52115=CARTESIAN_POINT ( 'NONE',  ( 11.26902897915239876, -3.778278678798900447, -8.337339982364900592 ) ) ;
#52167=CARTESIAN_POINT ( 'NONE',  ( 9.833267173155999075, -4.973628086880700572, -6.670281532133299329 ) ) ;
#52191=ADVANCED_FACE ( 'NONE', ( #21436 ), #57814, .F. ) ;
#52197=CARTESIAN_POINT ( 'NONE',  ( 11.60000000000000142, -3.133991299512490336, -6.727195615969564280 ) ) ;
#52198=CARTESIAN_POINT ( 'NONE',  ( 8.856495485442710702, -3.650546589001255171, -8.453238005838597857 ) ) ;
#52245=ADVANCED_FACE ( 'NONE', ( #14829 ), #9571, .T. ) ;
#52302=CARTESIAN_POINT ( 'NONE',  ( 11.18114303127866727, -4.620698129841968260, -8.119425260350672247 ) ) ;
#52375=CARTESIAN_POINT ( 'NONE',  ( 11.24025954179439957, -3.228187097503200320, -8.141292208271599051 ) ) ;
#52397=CARTESIAN_POINT ( 'NONE',  ( 9.703659112603999048, -4.376739491155700712, -8.280881105104999307 ) ) ;
#52414=CARTESIAN_POINT ( 'NONE',  ( 10.76841504065829902, -3.085489673376300424, -6.818119527508899935 ) ) ;
#52459=CARTESIAN_POINT ( 'NONE',  ( 9.986774547327625484, -3.921486932049647489, -6.628582782427464792 ) ) ;
#52463=CARTESIAN_POINT ( 'NONE',  ( 10.60026222744819790, -4.774534945026900346, -8.138001937130599828 ) ) ;
#52480=CARTESIAN_POINT ( 'NONE',  ( 10.21426717315699939, -4.869050473540199597, -6.759401780699699103 ) ) ;
#52483=CARTESIAN_POINT ( 'NONE',  ( 10.60434687351569494, -2.749999999999998224, -7.336375382625535124 ) ) ;
#52511=CARTESIAN_POINT ( 'NONE',  ( 8.820101285864000218, -4.823683599683300294, -6.521261160937499746 ) ) ;
#52517=CARTESIAN_POINT ( 'NONE',  ( 8.736820887142258130, -4.253281749927233513, -8.358484985884542695 ) ) ;
#52539=CARTESIAN_POINT ( 'NONE',  ( 10.28014141025500017, -3.582647672488299850, -8.243346240911998635 ) ) ;
#52580=EDGE_CURVE ( 'NONE', #2109, #48162, #65089, .T. ) ;
#52590=CARTESIAN_POINT ( 'NONE',  ( 9.965950584426998660, -3.655872208659600275, -6.704208565179699875 ) ) ;
#52605=CARTESIAN_POINT ( 'NONE',  ( 11.01790547754519878, -2.825704134258000266, -7.537269019642879542 ) ) ;
#52641=CARTESIAN_POINT ( 'NONE',  ( 10.73724174883999893, -4.024531238983009906, -8.391788556008700439 ) ) ;
#52691=ORIENTED_EDGE ( 'NONE', *, *, #57177, .F. ) ;
#52710=CARTESIAN_POINT ( 'NONE',  ( 9.185590450029501142, -2.907727159402500039, -6.870462550877413754 ) ) ;
#52721=CARTESIAN_POINT ( 'NONE',  ( 11.09256785386839894, -4.832509746210599921, -8.060248494254899754 ) ) ;
#52742=CARTESIAN_POINT ( 'NONE',  ( 9.171747021775997766, -4.651672637235799712, -8.071865996877098937 ) ) ;
#52757=B_SPLINE_CURVE_WITH_KNOTS ( 'NONE', 3,
 ( #25298, #24955, #14130, #51191 ),
 .UNSPECIFIED., .F., .F.,
 ( 4, 4 ),
 ( 0.000000000000000000, 0.1836163425310833319 ),
 .UNSPECIFIED. ) ;
#52761=CARTESIAN_POINT ( 'NONE',  ( 11.69559063708295987, -2.913481137622000006, -7.805482129094999166 ) ) ;
#52814=CARTESIAN_POINT ( 'NONE',  ( 11.53148876160955005, -4.790673964186999534, -8.322268080792200706 ) ) ;
#52829=CARTESIAN_POINT ( 'NONE',  ( 9.304430433046999127, -5.088604610742000212, -6.828193190755800224 ) ) ;
#52845=CARTESIAN_POINT ( 'NONE',  ( 9.091433907306445406, -3.054280487670652189, -8.331756427597948544 ) ) ;
#52848=CARTESIAN_POINT ( 'NONE',  ( 11.30565467195989093, -5.136173005413446013, -6.911917091190548312 ) ) ;
#52861=CARTESIAN_POINT ( 'NONE',  ( 8.541480666858999982, -3.573487373903700082, -8.706015266875999359 ) ) ;
#52876=CARTESIAN_POINT ( 'NONE',  ( 11.32299956498189886, -5.207010770456999893, -7.174999999999999822 ) ) ;
#52883=CARTESIAN_POINT ( 'NONE',  ( 10.69456919669529960, -2.906008650422999828, -7.823222900359999343 ) ) ;
#52888=CARTESIAN_POINT ( 'NONE',  ( 10.44125056272499918, -2.966599088466999934, -7.515315513715298934 ) ) ;
#52889=CARTESIAN_POINT ( 'NONE',  ( 9.852263540182327972, -5.092232985442820770, -6.870476274536370553 ) ) ;
#52912=CARTESIAN_POINT ( 'NONE',  ( 11.00000000000000000, -4.968589424331200100, -7.174999999999999822 ) ) ;
#52929=ORIENTED_EDGE ( 'NONE', *, *, #29463, .F. ) ;
#52941=CARTESIAN_POINT ( 'NONE',  ( 9.991279731608999626, -3.922199073804859992, -6.636486849903699969 ) ) ;
#52962=AXIS2_PLACEMENT_3D ( 'NONE', #64859, #48110, #42520 ) ;
#52993=CARTESIAN_POINT ( 'NONE',  ( 10.32169598648999909, -3.233475335853099875, -7.956401575444799867 ) ) ;
#53007=CARTESIAN_POINT ( 'NONE',  ( 11.51961669203094196, -2.969723712172476215, -7.175016092226064401 ) ) ;
#53071=CARTESIAN_POINT ( 'NONE',  ( 11.75718044953559804, -3.110233631466100324, -7.963966784336999005 ) ) ;
#53085=EDGE_LOOP ( 'NONE', ( #40151, #26146, #56544, #26479, #50343 ) ) ;
#53105=CARTESIAN_POINT ( 'NONE',  ( 10.62072335273219892, -3.602909566644000083, -8.569396700949999612 ) ) ;
#53155=CARTESIAN_POINT ( 'NONE',  ( 11.26487482311540056, -3.069598554678400149, -7.875904247640098887 ) ) ;
#53170=CARTESIAN_POINT ( 'NONE',  ( 9.507063610504999929, -3.475294527116599586, -8.666648427848999248 ) ) ;
#53202=CARTESIAN_POINT ( 'NONE',  ( 9.985242056249999720, -4.458751122174599679, -8.694123841252999085 ) ) ;
#53211=AXIS2_PLACEMENT_3D ( 'NONE', #25342, #51567, #25002 ) ;
#53224=CARTESIAN_POINT ( 'NONE',  ( 10.22687885159599830, -2.867290578374000365, -7.364871923548499844 ) ) ;
#53230=CARTESIAN_POINT ( 'NONE',  ( 10.32169598648999909, -3.233475335853099875, -7.956401575444799867 ) ) ;
#53232=CARTESIAN_POINT ( 'NONE',  ( 11.59999999999999787, -4.794859953698266786, -7.075514291626550545 ) ) ;
#53239=ORIENTED_EDGE ( 'NONE', *, *, #64786, .T. ) ;
#53274=CARTESIAN_POINT ( 'NONE',  ( 10.35826357027499789, -3.149486845331399998, -7.664090691848299386 ) ) ;
#53285=CARTESIAN_POINT ( 'NONE',  ( 9.915292290062998504, -3.250213325543700016, -7.064651992867799990 ) ) ;
#53298=CARTESIAN_POINT ( 'NONE',  ( 10.35814141025499957, -3.516507310755200066, -8.361148840840000318 ) ) ;
#53367=B_SPLINE_CURVE_WITH_KNOTS ( 'NONE', 3,
 ( #750, #10893, #48299, #65407, #32239, #1791, #5640, #60179, #22760, #403 ),
 .UNSPECIFIED., .F., .F.,
 ( 4, 2, 2, 2, 4 ),
 ( 0.000000000000000000, 0.2499999999999997780, 0.4999999999999995559, 0.7499999999999997780, 1.000000000000000000 ),
 .UNSPECIFIED. ) ;
#53396=CARTESIAN_POINT ( 'NONE',  ( 11.59999999999999964, -2.820501972398000046, -7.174999999999999822 ) ) ;
#53417=CARTESIAN_POINT ( 'NONE',  ( 11.16641369783139837, -4.050626550392200542, -8.502191501283999031 ) ) ;
#53420=ORIENTED_EDGE ( 'NONE', *, *, #12706, .T. ) ;
#53433=CARTESIAN_POINT ( 'NONE',  ( 11.50962052873067698, -4.169679534937900556, -6.639752069194234885 ) ) ;
#53452=CARTESIAN_POINT ( 'NONE',  ( 10.23103300763299828, -3.307558760216100069, -8.226274395107198600 ) ) ;
#53489=CARTESIAN_POINT ( 'NONE',  ( 9.303275160948496492, -5.099670516381894281, -6.884602962369688051 ) ) ;
#53501=CARTESIAN_POINT ( 'NONE',  ( 10.72333863405319931, -3.380905141010200232, -8.289729326049599223 ) ) ;
#53519=CARTESIAN_POINT ( 'NONE',  ( 10.16159632033899918, -4.929952350555500296, -7.120485934352199564 ) ) ;
#53567=CARTESIAN_POINT ( 'NONE',  ( 11.57656516821460890, -3.100463633631699967, -8.407828142327998577 ) ) ;
#53622=CARTESIAN_POINT ( 'NONE',  ( 11.00000000000000000, -3.008232475376599879, -7.174999999999999822 ) ) ;
#53626=CARTESIAN_POINT ( 'NONE',  ( 10.46029575260939026, -3.171266584307757874, -8.253465265694870823 ) ) ;
#53627=CARTESIAN_POINT ( 'NONE',  ( 9.231405316140000039, -4.184077495686000958, -8.347244604637999998 ) ) ;
#53638=ORIENTED_EDGE ( 'NONE', *, *, #10640, .F. ) ;
#53640=CARTESIAN_POINT ( 'NONE',  ( 10.82035090130999855, -3.241273085157000189, -7.969278253227299658 ) ) ;
#53734=CLOSED_SHELL ( 'NONE', ( #37186, #41973, #43968, #5143, #54039, #47354, #9054, #2710, #8405, #32604, #52245, #48581, #12665, #435, #61701, #2440, #26222, #16026, #31655, #42607, #7091, #22976, #60106, #9173, #32136, #1423, #26041, #9135, #14367, #52191, #59658 ) ) ;
#53756=CARTESIAN_POINT ( 'NONE',  ( 10.30487885159599770, -3.003595720052600448, -7.381132626649399064 ) ) ;
#53760=CARTESIAN_POINT ( 'NONE',  ( 11.51656039236534923, -2.826501801118000312, -7.557111631074219460 ) ) ;
#53790=CARTESIAN_POINT ( 'NONE',  ( 11.60533460557258323, -3.815825449682300086, -8.625775273268001087 ) ) ;
#53839=CARTESIAN_POINT ( 'NONE',  ( 10.20641772631199906, -3.568446272909699957, -8.388315195900499788 ) ) ;
#53843=B_SPLINE_CURVE_WITH_KNOTS ( 'NONE', 3,
 ( #35699, #4547, #46531, #67838, #19959, #68178, #31151, #62930, #57691, #9802, #68520, #20642, #15405, #48238, #53489, #11512, #22355, #49270 ),
 .UNSPECIFIED., .F., .F.,
 ( 4, 2, 2, 2, 2, 2, 2, 2, 4 ),
 ( 0.000000000000000000, 0.1250000000000000000, 0.2500000000000000000, 0.3750000000000000000, 0.5000000000000000000, 0.6250000000000000000, 0.7500000000000000000, 0.8750000000000000000, 1.000000000000000000 ),
 .UNSPECIFIED. ) ;
#53855=CARTESIAN_POINT ( 'NONE',  ( 9.958963142879998287, -3.017187828228399926, -7.292822454528599785 ) ) ;
#53905=CARTESIAN_POINT ( 'NONE',  ( 10.91610672858429965, -4.911600290708499905, -6.814233985789400094 ) ) ;
#53909=FACE_OUTER_BOUND ( 'NONE', #50394, .T. ) ;
#53962=CARTESIAN_POINT ( 'NONE',  ( 8.925442991499998868, -4.063228561016970275, -6.497580701799000380 ) ) ;
#53976=SHAPE_REPRESENTATION ( 'Terminal Screw 1', ( #9676 ), #756 ) ;
#53977=CARTESIAN_POINT ( 'NONE',  ( 11.06456920625009843, -3.962850971080120299, -6.467161360063999886 ) ) ;
#54024=VERTEX_POINT ( 'NONE', #17701 ) ;
#54039=ADVANCED_FACE ( 'NONE', ( #1960 ), #26677, .T. ) ;
#54066=COLOUR_RGB ( '', 0.72549020, 0.75294118, 0.79215686) ;
#54097=CARTESIAN_POINT ( 'NONE',  ( 10.55103166480599874, -5.000984463463999496, -7.570575893572789816 ) ) ;
#54102=CARTESIAN_POINT ( 'NONE',  ( 11.14256920625030034, -3.957769094421040190, -6.325872106312999676 ) ) ;
#54132=CARTESIAN_POINT ( 'NONE',  ( 11.60118044953561878, -2.866798846279000390, -8.090905336380599167 ) ) ;
#54181=CARTESIAN_POINT ( 'NONE',  ( 10.57149279008999798, -4.296686446741600385, -8.601484120896000007 ) ) ;
#54194=CARTESIAN_POINT ( 'NONE',  ( 10.31357120343299982, -4.048688523195909994, -8.503230697164999796 ) ) ;
#54234=CARTESIAN_POINT ( 'NONE',  ( 11.58810207955109917, -4.796537143354000499, -7.174999999999999822 ) ) ;
#54246=CARTESIAN_POINT ( 'NONE',  ( 10.34995525820099971, -4.107710726525199973, -6.364355462479999836 ) ) ;
#54310=CARTESIAN_POINT ( 'NONE',  ( 9.330709346416998784, -3.092687088662700035, -7.069157126958599768 ) ) ;
#54323=CARTESIAN_POINT ( 'NONE',  ( 10.36325056272499978, -3.107965259299500183, -7.513220396995270001 ) ) ;
#54337=CARTESIAN_POINT ( 'NONE',  ( 11.76077869730539938, -4.595338376575799799, -6.326049646822999861 ) ) ;
#54345=ORIENTED_EDGE ( 'NONE', *, *, #34544, .F. ) ;
#54348=VERTEX_POINT ( 'NONE', #42975 ) ;
#54366=CARTESIAN_POINT ( 'NONE',  ( 10.24160887879199855, -4.289688213680199702, -6.254020414961999563 ) ) ;
#54417=CARTESIAN_POINT ( 'NONE',  ( 10.50145247700547557, -4.082536117276985621, -6.629783135293719099 ) ) ;
#54418=VERTEX_POINT ( 'NONE', #57905 ) ;
#54424=EDGE_LOOP ( 'NONE', ( #40035, #53638, #56480 ) ) ;
#54445=CARTESIAN_POINT ( 'NONE',  ( 10.74795391537419853, -3.169881940022800215, -8.063786182297898009 ) ) ;
#54449=CARTESIAN_POINT ( 'NONE',  ( 11.80233327354039830, -5.101536739857000846, -6.779499720266399798 ) ) ;
#54480=CARTESIAN_POINT ( 'NONE',  ( 11.52733460557258915, -3.793662715184400014, -8.761245990815998752 ) ) ;
#54496=B_SPLINE_CURVE_WITH_KNOTS ( 'NONE', 3,
 ( #15973, #48831, #58624, #4786, #42895, #939, #47455, #64201, #21222, #68760, #37645, #20880, #36966, #58280, #31722, #13167, #45321, #49512, #7556, #40080, #44975, #1978, #34141, #12462, #7216, #54417, #66627, #55808, #34496, #66279, #22595, #1626, #54761, #7909, #49169 ),
 .UNSPECIFIED., .F., .F.,
 ( 4, 1, 1, 1, 1, 1, 1, 1, 1, 1, 1, 1, 1, 1, 1, 1, 1, 1, 1, 1, 1, 1, 1, 1, 1, 1, 1, 1, 1, 1, 1, 1, 4 ),
 ( 0.000000000000000000, 0.02634724210002164710, 0.05799096732718461711, 0.08963469255434758365, 0.1212784177813103353, 0.1529221430084733158, 0.1845658682354360536, 0.2162095934625990201, 0.2478533186897620144, 0.2794970439167247522, 0.3111407691438877188, 0.3427844943710506853, 0.3744282195980134231, 0.4060719448251764452, 0.4377156700521391830, 0.4693593952793021495, 0.5010031205064651161, 0.5326468457334281315, 0.5642905709605910980, 0.5959342961875535583, 0.6275780214147167468, 0.6592217466418797134, 0.6908654718688422847, 0.7225091970960054732, 0.7541529223229680445, 0.7857966475501312331, 0.8174403727772941997, 0.8490840980042566599, 0.8807278232314198485, 0.9123715484585828150, 0.9440152736855453863, 0.9756589989127085749, 1.000000000000000000 ),
 .UNSPECIFIED. ) ;
#54534=CARTESIAN_POINT ( 'NONE',  ( 11.50271932425157040, -4.187398418774900044, -8.764198628556998827 ) ) ;
#54550=CARTESIAN_POINT ( 'NONE',  ( 9.150442991499998513, -4.071878040089889517, -6.360452723514999462 ) ) ;
#54568=CARTESIAN_POINT ( 'NONE',  ( 11.17056785386839834, -4.718624889240500053, -7.983608166707499620 ) ) ;
#54574=CARTESIAN_POINT ( 'NONE',  ( 11.00000000000000000, -3.008232475376599879, -7.174999999999999822 ) ) ;
#54599=EDGE_LOOP ( 'NONE', ( #9004, #54345, #56807, #6939 ) ) ;
#54601=CARTESIAN_POINT ( 'NONE',  ( 10.59195391537400077, -2.942766577210000012, -8.218034727798299244 ) ) ;
#54604=LINE ( 'NONE', #33289, #26025 ) ;
#54629=ORIENTED_EDGE ( 'NONE', *, *, #10000, .T. ) ;
#54652=ORIENTED_EDGE ( 'NONE', *, *, #1845, .T. ) ;
#54662=CARTESIAN_POINT ( 'NONE',  ( 9.710646554150999421, -3.513729974241599940, -8.378853663802400931 ) ) ;
#54675=DIRECTION ( 'NONE',  ( 0.000000000000000000, 1.000000000000000000, 0.000000000000000000 ) ) ;
#54684=VERTEX_POINT ( 'NONE', #62376 ) ;
#54746=CARTESIAN_POINT ( 'NONE',  ( 8.849999778957998942, -4.000000000000000000, -7.500000000000000000 ) ) ;
#54761=CARTESIAN_POINT ( 'NONE',  ( 10.33103907547007694, -3.225837863097586133, -7.899515915943056577 ) ) ;
#54791=CARTESIAN_POINT ( 'NONE',  ( 11.55610404293055993, -4.502836909561000134, -8.523936114709998790 ) ) ;
#54795=CARTESIAN_POINT ( 'NONE',  ( 11.43345123989529810, -3.459769760840400110, -8.543317325199000223 ) ) ;
#54827=CARTESIAN_POINT ( 'NONE',  ( 11.23195122972050086, -3.492749840905900349, -6.326963915009999440 ) ) ;
#54880=CARTESIAN_POINT ( 'NONE',  ( 11.43302763632549990, -5.035790660926999784, -7.022058766158599141 ) ) ;
#54896=CARTESIAN_POINT ( 'NONE',  ( 9.277088727410998104, -5.137817193984000497, -7.595427884080399927 ) ) ;
#54912=CARTESIAN_POINT ( 'NONE',  ( 11.68748876160954886, -4.600381688599499697, -8.124372018288600117 ) ) ;
#54925=CARTESIAN_POINT ( 'NONE',  ( 9.015584277044482064, -4.716917290452846245, -8.431467892494236338 ) ) ;
#54950=CARTESIAN_POINT ( 'NONE',  ( 11.15810538575740019, -2.757018958839999812, -7.202822423614300362 ) ) ;
#55011=CARTESIAN_POINT ( 'NONE',  ( 9.381367640780998940, -3.526522998810799781, -6.614188603779100006 ) ) ;
#55057=B_SPLINE_CURVE_WITH_KNOTS ( 'NONE', 3,
 ( #31342, #53007, #19468, #42179 ),
 .UNSPECIFIED., .F., .F.,
 ( 4, 4 ),
 ( 0.000000000000000000, 1.000000000000000000 ),
 .UNSPECIFIED. ) ;
#55142=CARTESIAN_POINT ( 'NONE',  ( 11.71922412107039868, -3.930460928605089777, -6.185573549454999487 ) ) ;
#55172=CARTESIAN_POINT ( 'NONE',  ( 10.76426088462129904, -3.997280690308189666, -6.221990224628999755 ) ) ;
#55214=ORIENTED_EDGE ( 'NONE', *, *, #35028, .T. ) ;
#55225=CARTESIAN_POINT ( 'NONE',  ( 10.79303032197930001, -3.336467919271199900, -6.572090902022299730 ) ) ;
#55229=CARTESIAN_POINT ( 'NONE',  ( 11.60000000000000142, -4.471166781226291853, -8.438845841270557813 ) ) ;
#55244=CARTESIAN_POINT ( 'NONE',  ( 9.781659112603998452, -4.436443689698799986, -8.404632083253700259 ) ) ;
#55263=CARTESIAN_POINT ( 'NONE',  ( 10.43210941423799909, -3.358814833524500276, -6.917608226833099394 ) ) ;
#55275=CARTESIAN_POINT ( 'NONE',  ( 10.08521345716899908, -3.075109701058799772, -8.340879262988799780 ) ) ;
#55298=CARTESIAN_POINT ( 'NONE',  ( 11.01041369783139956, -4.064477673403060543, -8.776385133971000840 ) ) ;
#55302=CARTESIAN_POINT ( 'NONE',  ( 8.726967411678998587, -4.064442376558529801, -8.391190439313799487 ) ) ;
#55318=EDGE_CURVE ( 'NONE', #36490, #65063, #27489, .T. ) ;
#55356=CARTESIAN_POINT ( 'NONE',  ( 8.923430433046998900, -4.971677342931100085, -6.900352112302299723 ) ) ;
#55385=CARTESIAN_POINT ( 'NONE',  ( 11.55300581613033906, -2.892415530317000272, -8.211208432468300344 ) ) ;
#55491=CARTESIAN_POINT ( 'NONE',  ( 11.35545123989519922, -3.524778630617700248, -8.417769225118700405 ) ) ;
#55521=CARTESIAN_POINT ( 'NONE',  ( 10.37041638348499895, -5.241705141469999774, -7.197535585171899619 ) ) ;
#55543=CARTESIAN_POINT ( 'NONE',  ( 11.51145123989532948, -3.394760891061399999, -8.668865425277999748 ) ) ;
#55545=ORIENTED_EDGE ( 'NONE', *, *, #6066, .T. ) ;
#55576=CARTESIAN_POINT ( 'NONE',  ( 10.64533863405319991, -3.296214805808900028, -8.397761948794601139 ) ) ;
#55592=CARTESIAN_POINT ( 'NONE',  ( 10.10892546752099896, -4.864937374655599278, -7.440072690703440017 ) ) ;
#55611=CARTESIAN_POINT ( 'NONE',  ( 11.63825819896753977, -4.851203879749700576, -7.660469764776300039 ) ) ;
#55637=CARTESIAN_POINT ( 'NONE',  ( 11.10328610135029948, -4.878060775730400422, -7.825000000000000178 ) ) ;
#55646=CARTESIAN_POINT ( 'NONE',  ( 11.20733594839949809, -3.159733897807000425, -6.537051788466999191 ) ) ;
#55663=EDGE_CURVE ( 'NONE', #49260, #8310, #50022, .T. ) ;
#55706=CARTESIAN_POINT ( 'NONE',  ( 9.278038493598998571, -3.173653894988100355, -6.712036445818600150 ) ) ;
#55726=ORIENTED_EDGE ( 'NONE', *, *, #38667, .F. ) ;
#55734=CARTESIAN_POINT ( 'NONE',  ( 11.47500581613029880, -3.011381429075500105, -8.134817373646898275 ) ) ;
#55747=VERTEX_POINT ( 'NONE', #63678 ) ;
#55792=ORIENTED_EDGE ( 'NONE', *, *, #43882, .F. ) ;
#55808=CARTESIAN_POINT ( 'NONE',  ( 10.45222191436347714, -3.562569433230172944, -6.743201413565676816 ) ) ;
#55836=CARTESIAN_POINT ( 'NONE',  ( 11.31389666366019853, -4.045876550911099656, -8.532487796751999198 ) ) ;
#55842=EDGE_CURVE ( 'NONE', #13264, #35196, #31415, .T. ) ;
#55866=CARTESIAN_POINT ( 'NONE',  ( 10.07503300763299947, -3.118110956362800223, -8.424978748982498544 ) ) ;
#55870=CARTESIAN_POINT ( 'NONE',  ( 10.09259632033899834, -4.802737635155300389, -7.172402329663099430 ) ) ;
#55889=CARTESIAN_POINT ( 'NONE',  ( 11.68788784977535933, -4.985985832792199979, -7.443657794094239222 ) ) ;
#55919=CARTESIAN_POINT ( 'NONE',  ( 11.81056516821459823, -3.390321848206700128, -8.115298063151199059 ) ) ;
#55933=CARTESIAN_POINT ( 'NONE',  ( 11.50705667793316778, -3.398423525757989339, -8.661791977777625107 ) ) ;
#55936=CARTESIAN_POINT ( 'NONE',  ( 10.31155864497999808, -3.317414799430800088, -8.034587760591801242 ) ) ;
#55951=CARTESIAN_POINT ( 'NONE',  ( 10.30487885159599770, -3.003595720052600448, -7.381132626649399064 ) ) ;
#55987=CARTESIAN_POINT ( 'NONE',  ( 11.18272066707849888, -2.906477115133000222, -6.838543969064300398 ) ) ;
#55996=CARTESIAN_POINT ( 'NONE',  ( 10.14601354018232904, -3.000416447002271170, -6.731816600031360842 ) ) ;
#56000=CARTESIAN_POINT ( 'NONE',  ( 10.72749279009019929, -4.225282629687599822, -8.336388861178200216 ) ) ;
#56013=CARTESIAN_POINT ( 'NONE',  ( 11.12299956498149811, -2.792989229543000107, -7.825000000000000178 ) ) ;
#56036=CARTESIAN_POINT ( 'NONE',  ( 10.84184687351628540, -4.999583552997724389, -6.731816600031354625 ) ) ;
#56042=CARTESIAN_POINT ( 'NONE',  ( 9.480671671056999372, -5.126041103316000047, -7.689118697196099639 ) ) ;
#56068=CARTESIAN_POINT ( 'NONE',  ( 11.60477869730532774, -4.467447516829900600, -6.578238193496799724 ) ) ;
#56093=CARTESIAN_POINT ( 'NONE',  ( 9.253772138682000659, -4.476015718025199597, -6.312652778810999621 ) ) ;
#56122=DIRECTION ( 'NONE',  ( 0.000000000000000000, 0.000000000000000000, -1.000000000000000000 ) ) ;
#56127=DIRECTION ( 'NONE',  ( 0.000000000000000000, 1.000000000000000000, 0.000000000000000000 ) ) ;
#56134=DIRECTION ( 'NONE',  ( 0.000000000000000000, 1.000000000000000000, 0.000000000000000000 ) ) ;
#56153=CARTESIAN_POINT ( 'NONE',  ( 9.364763540183330903, -5.217465845835395299, -7.827184855449096368 ) ) ;
#56169=CARTESIAN_POINT ( 'NONE',  ( 9.893930206848997599, -5.250000000000000000, -7.500000000000000000 ) ) ;
#56174=CARTESIAN_POINT ( 'NONE',  ( 10.85168717260509830, -4.613789146762799831, -8.501809683958001074 ) ) ;
#56184=EDGE_CURVE ( 'NONE', #8310, #47368, #20270, .T. ) ;
#56207=CARTESIAN_POINT ( 'NONE',  ( 10.12426357027499790, -2.745128867668000350, -7.742104041724699570 ) ) ;
#56209=VECTOR ( 'NONE', #34883, 1000.000000000000000 ) ;
#56226=CARTESIAN_POINT ( 'NONE',  ( 10.84657802013509986, -5.315911219205999849, -7.469366283838649423 ) ) ;
#56259=CARTESIAN_POINT ( 'NONE',  ( 11.08425954179440076, -3.017023678917100327, -8.316745941391600283 ) ) ;
#56278=CARTESIAN_POINT ( 'NONE',  ( 9.199088727410998700, -5.000897406023000258, -7.583944523024719331 ) ) ;
#56297=CARTESIAN_POINT ( 'NONE',  ( 10.79718447801629999, -2.996774412198000448, -7.477880487566260115 ) ) ;
#56337=CARTESIAN_POINT ( 'NONE',  ( 8.705449068729999240, -4.363978735910500006, -8.287166017043100297 ) ) ;
#56340=CARTESIAN_POINT ( 'NONE',  ( 10.11342028323962694, -4.872854478606138073, -7.439524153027672781 ) ) ;
#56345=CARTESIAN_POINT ( 'NONE',  ( 10.35826357027499789, -3.149486845331399998, -7.664090691848299386 ) ) ;
#56371=CARTESIAN_POINT ( 'NONE',  ( 10.53521345716899837, -3.075109701058799772, -8.340879262988799780 ) ) ;
#56391=CARTESIAN_POINT ( 'NONE',  ( 10.03791290906799993, -4.722468360609500593, -8.384179803770500428 ) ) ;
#56417=CARTESIAN_POINT ( 'NONE',  ( 11.30878751119029957, -5.041025164610000608, -8.044634158732998586 ) ) ;
#56442=CARTESIAN_POINT ( 'NONE',  ( 9.785684229509998389, -4.901739481456999670, -6.592668585875199661 ) ) ;
#56480=ORIENTED_EDGE ( 'NONE', *, *, #61779, .T. ) ;
#56517=CARTESIAN_POINT ( 'NONE',  ( 10.56080513895999928, -2.973119161490000106, -6.929150654994399083 ) ) ;
#56544=ORIENTED_EDGE ( 'NONE', *, *, #11991, .T. ) ;
#56554=CARTESIAN_POINT ( 'NONE',  ( 8.902126402770997871, -3.188752782784400441, -7.194081880505399873 ) ) ;
#56570=CARTESIAN_POINT ( 'NONE',  ( 11.39189666366029918, -4.052152326617509459, -8.673729056199000809 ) ) ;
#56575=ORIENTED_EDGE ( 'NONE', *, *, #22474, .F. ) ;
#56601=CARTESIAN_POINT ( 'NONE',  ( 10.27195525820100031, -4.120672149427799802, -6.227697122196000024 ) ) ;
#56619=CARTESIAN_POINT ( 'NONE',  ( 8.869809814040998219, -3.385590752329799891, -8.294571108394100278 ) ) ;
#56638=CARTESIAN_POINT ( 'NONE',  ( 11.53564291764652872, -4.995889373412399692, -7.376893506359599506 ) ) ;
#56654=CARTESIAN_POINT ( 'NONE',  ( 9.393930206848999376, -5.250000000000000000, -7.500000000000000000 ) ) ;
#56678=DIRECTION ( 'NONE',  ( -1.000000000000000000, 0.000000000000000000, 1.665334536957000056E-14 ) ) ;
#56686=CARTESIAN_POINT ( 'NONE',  ( 8.973608660036624940, -3.779042157900793786, -6.653412791890684019 ) ) ;
#56691=CARTESIAN_POINT ( 'NONE',  ( 11.73256516821459883, -3.293702443348299980, -8.212808089543500500 ) ) ;
#56709=CARTESIAN_POINT ( 'NONE',  ( 10.77101354018289925, -4.768183399968641822, -6.500416447002272058 ) ) ;
#56740=CARTESIAN_POINT ( 'NONE',  ( 10.08655864497999843, -2.992894514506000192, -8.288745882156399958 ) ) ;
#56767=CARTESIAN_POINT ( 'NONE',  ( 11.64122412107036908, -3.937930136014310190, -6.326756392227999015 ) ) ;
#56770=CARTESIAN_POINT ( 'NONE',  ( 9.002599499754321499, -2.949662297526366661, -7.998361244042363261 ) ) ;
#56807=ORIENTED_EDGE ( 'NONE', *, *, #44763, .F. ) ;
#56833=B_SPLINE_CURVE_WITH_KNOTS ( 'NONE', 3,
 ( #56013, #8807, #3217, #45868 ),
 .UNSPECIFIED., .F., .F.,
 ( 4, 4 ),
 ( 0.000000000000000000, 1.000000000000000000 ),
 .UNSPECIFIED. ) ;
#56865=CARTESIAN_POINT ( 'NONE',  ( 11.14767835872009982, -4.874341053673500568, -6.948943352864199952 ) ) ;
#56899=ORIENTED_EDGE ( 'NONE', *, *, #35371, .F. ) ;
#56911=CARTESIAN_POINT ( 'NONE',  ( 11.76588784977539781, -5.120865761890000201, -7.435950347916509884 ) ) ;
#56935=EDGE_CURVE ( 'NONE', #36490, #10153, #37589, .T. ) ;
#56942=CARTESIAN_POINT ( 'NONE',  ( 11.85159063708299954, -3.174974693948799942, -7.731961446576300467 ) ) ;
#56943=CARTESIAN_POINT ( 'NONE',  ( 10.22272469555899832, -3.360453478306600239, -6.393520617113999549 ) ) ;
#56958=CARTESIAN_POINT ( 'NONE',  ( 9.070430433046999141, -4.737822807309499673, -7.044669955395099770 ) ) ;
#56976=CARTESIAN_POINT ( 'NONE',  ( 10.72333863405319931, -3.380905141010200232, -8.289729326049599223 ) ) ;
#57021=CARTESIAN_POINT ( 'NONE',  ( 8.922950365671626471, -3.319061674888539315, -6.950586433956124743 ) ) ;
#57025=CARTESIAN_POINT ( 'NONE',  ( 10.60441638348510018, -4.841589649988700117, -7.294998899090099798 ) ) ;
#57031=CARTESIAN_POINT ( 'NONE',  ( 10.28976354018291239, -4.327184855449096368, -6.282534154164603812 ) ) ;
#57070=CARTESIAN_POINT ( 'NONE',  ( 9.782608878791998919, -4.289688213680199702, -6.254020414961999563 ) ) ;
#57096=CARTESIAN_POINT ( 'NONE',  ( 11.39700581613019992, -3.130347327833300053, -8.058426314824099990 ) ) ;
#57097=CARTESIAN_POINT ( 'NONE',  ( 11.59999999999999964, -3.409519984105200852, -6.540686298265701915 ) ) ;
#57177=EDGE_CURVE ( 'NONE', #26585, #64554, #6253, .T. ) ;
#57196=ORIENTED_EDGE ( 'NONE', *, *, #24272, .T. ) ;
#57260=CARTESIAN_POINT ( 'NONE',  ( 11.47657389914466464, -4.648774973711785385, -8.595592487855949315 ) ) ;
#57270=CARTESIAN_POINT ( 'NONE',  ( 11.51102763632551884, -4.911148285670300595, -7.079572058049399708 ) ) ;
#57309=CARTESIAN_POINT ( 'NONE',  ( 10.40333997687999990, -3.786145554879500441, -6.519583185858300212 ) ) ;
#57322=DIRECTION ( 'NONE',  ( -1.000000000000000000, 0.000000000000000000, -1.233561263588000078E-14 ) ) ;
#57352=CARTESIAN_POINT ( 'NONE',  ( 9.606837339593626623, -4.864872534707646246, -7.367607524272325570 ) ) ;
#57356=CARTESIAN_POINT ( 'NONE',  ( 10.99826088462129903, -3.998156935320088756, -6.633804182961699603 ) ) ;
#57364=CARTESIAN_POINT ( 'NONE',  ( 10.15434687351570631, -2.749999999999998668, -7.336375382625537789 ) ) ;
#57377=CARTESIAN_POINT ( 'NONE',  ( 10.64601354018249779, -3.000416447002271170, -6.731816600031360842 ) ) ;
#57407=CARTESIAN_POINT ( 'NONE',  ( 9.048063610504998522, -3.475294527116599586, -8.666648427848999248 ) ) ;
#57434=CARTESIAN_POINT ( 'NONE',  ( 10.86190547754509872, -3.108323067758099967, -7.528299448264639260 ) ) ;
#57461=ORIENTED_EDGE ( 'NONE', *, *, #4469, .T. ) ;
#57538=CARTESIAN_POINT ( 'NONE',  ( 10.69568717260499824, -4.466067913030199676, -8.260703168378098482 ) ) ;
#57617=CARTESIAN_POINT ( 'NONE',  ( 11.77359063708300013, -3.044227915785300276, -7.768721787835699999 ) ) ;
#57653=CARTESIAN_POINT ( 'NONE',  ( 11.18687482311539938, -2.942322404451000128, -7.927326830586499007 ) ) ;
#57691=CARTESIAN_POINT ( 'NONE',  ( 9.211801307670125283, -3.888124047000113048, -6.244821713992729784 ) ) ;
#57698=CARTESIAN_POINT ( 'NONE',  ( 10.30371347217102773, -3.410708369063949696, -8.130653431319531776 ) ) ;
#57703=CARTESIAN_POINT ( 'NONE',  ( 10.67410807141119911, -3.953638752893899877, -8.502397868920999358 ) ) ;
#57715=AXIS2_PLACEMENT_3D ( 'NONE', #28924, #28567, #6878 ) ;
#57720=CARTESIAN_POINT ( 'NONE',  ( 9.000480666858997836, -3.573487373903700082, -8.706015266875999359 ) ) ;
#57751=CARTESIAN_POINT ( 'NONE',  ( 9.478659112603999404, -4.555852086785099786, -8.652134039551000910 ) ) ;
#57774=DIRECTION ( 'NONE',  ( 1.000000000000000000, 0.000000000000000000, -0.000000000000000000 ) ) ;
#57780=CARTESIAN_POINT ( 'NONE',  ( 10.40480513895999870, -3.220259576336399920, -7.066537524675499782 ) ) ;
#57814=PLANE ( 'NONE',  #63379 ) ;
#57836=CARTESIAN_POINT ( 'NONE',  ( 10.04193802597399987, -4.450760089576400347, -6.759376420744099612 ) ) ;
#57905=CARTESIAN_POINT ( 'NONE',  ( 11.39975833414730033, -3.203462856645999945, -7.174999999999999822 ) ) ;
#57972=CARTESIAN_POINT ( 'NONE',  ( 11.56025819896753859, -4.986099335708799707, -7.685900384398899554 ) ) ;
#58011=CARTESIAN_POINT ( 'NONE',  ( 11.33456651104149948, -3.887457492043800311, -6.364824110469998963 ) ) ;
#58013=CARTESIAN_POINT ( 'NONE',  ( 10.14393020684899938, -2.750000000000000000, -7.500000000000000000 ) ) ;
#58055=CARTESIAN_POINT ( 'NONE',  ( 8.872292071306626227, -3.125836066416603387, -7.462990653670714458 ) ) ;
#58061=CARTESIAN_POINT ( 'NONE',  ( 11.24025954179439957, -3.228187097503200320, -8.141292208271599051 ) ) ;
#58076=CARTESIAN_POINT ( 'NONE',  ( 9.532392757686999119, -3.136549968260000210, -8.443842375698499936 ) ) ;
#58106=CARTESIAN_POINT ( 'NONE',  ( 8.794772138681999252, -4.476015718025199597, -6.312652778810999621 ) ) ;
#58128=CARTESIAN_POINT ( 'NONE',  ( 10.84226088462129844, -3.997572771977982775, -6.359261544073000039 ) ) ;
#58133=CARTESIAN_POINT ( 'NONE',  ( 11.36056039236529891, -3.108928759355700233, -7.543366519014379712 ) ) ;
#58183=CARTESIAN_POINT ( 'NONE',  ( 10.11591290906799934, -4.635529777446699917, -8.277781595084700683 ) ) ;
#58197=CARTESIAN_POINT ( 'NONE',  ( 10.52435971519499880, -3.467537960339900138, -6.614211617270199461 ) ) ;
#58204=CARTESIAN_POINT ( 'NONE',  ( 8.811649685568998080, -3.898643963693099845, -8.457700632733599733 ) ) ;
#58231=CARTESIAN_POINT ( 'NONE',  ( 9.539763540182331525, -3.672815144550900524, -8.717465845835397076 ) ) ;
#58233=CARTESIAN_POINT ( 'NONE',  ( 10.57102344389999971, -4.762665848028800220, -7.037150754511299233 ) ) ;
#58280=CARTESIAN_POINT ( 'NONE',  ( 10.79683585285767577, -3.460706475588385178, -8.187933206668011721 ) ) ;
#58289=LINE ( 'NONE', #5150, #1477 ) ;
#58309=CARTESIAN_POINT ( 'NONE',  ( 10.53057053952199951, -4.340412141385700195, -6.703496287302799672 ) ) ;
#58344=CARTESIAN_POINT ( 'NONE',  ( 10.21462282008599942, -3.476853648246800432, -8.343818446627699004 ) ) ;
#58388=CARTESIAN_POINT ( 'NONE',  ( 8.751496707488000126, -3.918323994020610268, -8.356402621895700378 ) ) ;
#58394=CARTESIAN_POINT ( 'NONE',  ( 10.47718582084299932, -4.656536239972400182, -6.741111985563299491 ) ) ;
#58410=CARTESIAN_POINT ( 'NONE',  ( 10.16360887879199915, -4.258572737033900601, -6.387851364408000165 ) ) ;
#58445=CARTESIAN_POINT ( 'NONE',  ( 9.453329965421998438, -4.888489908445900589, -8.420309768537698858 ) ) ;
#58465=CARTESIAN_POINT ( 'NONE',  ( 11.61759063708296047, -2.782734359457999851, -7.842242470354300110 ) ) ;
#58472=CARTESIAN_POINT ( 'NONE',  ( 11.59603632436369125, -4.842640371965599932, -7.303218851299499548 ) ) ;
#58474=CARTESIAN_POINT ( 'NONE',  ( 11.60000000000000142, -4.094072174251358831, -6.471240206706526443 ) ) ;
#58522=CARTESIAN_POINT ( 'NONE',  ( 9.687329965421998423, -4.602191201513400109, -8.123757726465999696 ) ) ;
#58529=CARTESIAN_POINT ( 'NONE',  ( 11.00000000000000000, -4.968589424331200100, -7.174999999999999822 ) ) ;
#58534=CARTESIAN_POINT ( 'NONE',  ( 10.60746886766490071, -4.498335456194499926, -6.594573315824700188 ) ) ;
#58542=CARTESIAN_POINT ( 'NONE',  ( 8.770072224255999416, -3.906223101245800411, -8.386086300777899183 ) ) ;
#58620=ORIENTED_EDGE ( 'NONE', *, *, #7257, .T. ) ;
#58624=CARTESIAN_POINT ( 'NONE',  ( 11.06623059009866061, -4.687762524153129995, -6.964041498692941090 ) ) ;
#58655=CARTESIAN_POINT ( 'NONE',  ( 11.33872066707849768, -3.141388196630700236, -6.980638253271099103 ) ) ;
#58689=CARTESIAN_POINT ( 'NONE',  ( 10.98995257254739855, -5.095356924909000718, -7.818564472783199548 ) ) ;
#58738=CARTESIAN_POINT ( 'NONE',  ( 10.82179975933729921, -3.051121678931899783, -7.173532873542499466 ) ) ;
#58744=EDGE_CURVE ( 'NONE', #30625, #11095, #16158, .T. ) ;
#58750=CARTESIAN_POINT ( 'NONE',  ( 10.01059687351599692, -3.370476274536376771, -8.592232985442825210 ) ) ;
#58753=CARTESIAN_POINT ( 'NONE',  ( 9.302417874593999159, -5.050800927762999493, -7.946712276748498560 ) ) ;
#58782=CARTESIAN_POINT ( 'NONE',  ( 8.969356963619999235, -5.119357025014000584, -7.499999999914821025 ) ) ;
#58788=CARTESIAN_POINT ( 'NONE',  ( 11.48513281071060277, -5.084573083995119980, -7.824999134348144203 ) ) ;
#58794=( GEOMETRIC_REPRESENTATION_CONTEXT ( 3 ) GLOBAL_UNCERTAINTY_ASSIGNED_CONTEXT ( ( #4513 ) ) GLOBAL_UNIT_ASSIGNED_CONTEXT ( ( #12748, #3282, #45935 ) ) REPRESENTATION_CONTEXT ( 'NONE', 'WORKASPACE' ) );
#58810=CARTESIAN_POINT ( 'NONE',  ( 10.89149144726329865, -4.659577337894599935, -6.569275630703699242 ) ) ;
#58817=CARTESIAN_POINT ( 'NONE',  ( 11.59999999999999609, -4.755880058522732767, -6.982116912833851607 ) ) ;
#58850=CARTESIAN_POINT ( 'NONE',  ( 9.343930206849998754, -5.250000000000000000, -7.500000000000000000 ) ) ;
#58869=EDGE_CURVE ( 'NONE', #59745, #46774, #54496, .T. ) ;
#58871=CARTESIAN_POINT ( 'NONE',  ( 9.206076168957999073, -4.439974903344300117, -8.247081005603298820 ) ) ;
#58885=CARTESIAN_POINT ( 'NONE',  ( 11.27745123989519982, -3.589787500396900199, -8.292221125039500151 ) ) ;
#58894=CARTESIAN_POINT ( 'NONE',  ( 8.720712484379999907, -4.219532685969900498, -8.340498368324299250 ) ) ;
#58969=ORIENTED_EDGE ( 'NONE', *, *, #22389, .T. ) ;
#58985=EDGE_LOOP ( 'NONE', ( #30851, #31539, #335, #5741, #16183, #36906, #48286, #12660, #9897, #35357, #55792 ) ) ;
#59005=CARTESIAN_POINT ( 'NONE',  ( 10.82179975933729921, -3.051121678931899783, -7.173532873542499466 ) ) ;
#59009=CARTESIAN_POINT ( 'NONE',  ( 10.76346886766499900, -4.634677072395899877, -6.346853961441000003 ) ) ;
#59039=CARTESIAN_POINT ( 'NONE',  ( 11.08841369783139896, -4.057552111898620417, -8.639288317626999003 ) ) ;
#59085=CARTESIAN_POINT ( 'NONE',  ( 11.04333729122639873, -5.003122373830000136, -7.473611442402849470 ) ) ;
#59101=CARTESIAN_POINT ( 'NONE',  ( 10.03495058442699950, -3.601336184534900120, -6.578094656394299911 ) ) ;
#59150=CARTESIAN_POINT ( 'NONE',  ( 11.08841369783139896, -4.057552111898620417, -8.639288317626999003 ) ) ;
#59159=CARTESIAN_POINT ( 'NONE',  ( 11.59999999999999964, -4.569820763625128457, -6.730205196242793342 ) ) ;
#59209=CARTESIAN_POINT ( 'NONE',  ( 9.052088727410998459, -5.000897406023000258, -7.583944523024719331 ) ) ;
#59223=CARTESIAN_POINT ( 'NONE',  ( 11.36056039236529891, -3.108928759355700233, -7.543366519014379712 ) ) ;
#59238=CARTESIAN_POINT ( 'NONE',  ( 10.09393020684899867, -2.750000000000000000, -7.500000000000000000 ) ) ;
#59277=DIRECTION ( 'NONE',  ( -1.000000000000000000, 0.000000000000000000, 0.000000000000000000 ) ) ;
#59292=B_SPLINE_CURVE_WITH_KNOTS ( 'NONE', 3,
 ( #23493, #3538, #24875, #39577 ),
 .UNSPECIFIED., .F., .F.,
 ( 4, 4 ),
 ( 0.000000000000000000, 1.000000000000000000 ),
 .UNSPECIFIED. ) ;
#59314=B_SPLINE_CURVE_WITH_KNOTS ( 'NONE', 3,
 ( #42786, #44181, #34725, #13056, #56036, #49756, #18295, #59896, #7104, #39270, #1516, #23185, #7799, #66516, #60940, #24216, #12003, #17952 ),
 .UNSPECIFIED., .F., .F.,
 ( 4, 2, 2, 2, 2, 2, 2, 2, 4 ),
 ( 0.000000000000000000, 0.1250000000000000000, 0.2500000000000000000, 0.3750000000000000000, 0.5000000000000000000, 0.6250000000000000000, 0.7500000000000000000, 0.8750000000000000000, 1.000000000000000000 ),
 .UNSPECIFIED. ) ;
#59340=CARTESIAN_POINT ( 'NONE',  ( 10.20641772631199906, -3.568446272909699957, -8.388315195900499788 ) ) ;
#59346=CARTESIAN_POINT ( 'NONE',  ( 11.22567835872029995, -4.993948309075300074, -6.873560442659099046 ) ) ;
#59375=CARTESIAN_POINT ( 'NONE',  ( 10.64118447801629941, -2.722297859592000435, -7.471828720557429193 ) ) ;
#59425=CARTESIAN_POINT ( 'NONE',  ( 11.11302897915239818, -3.708003626182200030, -8.602736702002999891 ) ) ;
#59437=CARTESIAN_POINT ( 'NONE',  ( 9.979346873516126593, -3.836375382625532904, -8.749999999999998224 ) ) ;
#59441=CARTESIAN_POINT ( 'NONE',  ( 9.882975701332998852, -3.263119632394200220, -8.182531775206799196 ) ) ;
#59483=B_SPLINE_SURFACE_WITH_KNOTS ( 'NONE', 3, 3, ( 
 ( #34559, #2044, #60765, #23364, #44704, #12880, #66345, #18467, #39793, #61116, #13233, #55870, #67370, #57836, #64102, #52941, #52590, #63415, #53285, #26375, #31280, #40812, #47701, #9944, #16216, #47357, #68661, #58522, #62136, #19495, #14255, #69012, #32314, #37204, #5037, #21458, #42794, #31620, #67034, #19144, #21125, #37538, #42451, #10627, #63761, #53627, #58871, #24396, #31971, #10976, #45726, #5385, #4684, #40465, #35240, #26724, #61796, #13913, #56554, #48037, #142, #8658, #36866, #3404, #30005, #20778, #51307 ),
 ( #24738, #46065, #15871, #15539, #42110, #36513, #26026, #58183, #10285, #6758, #34043, #64438, #38229, #17612, #6410, #16899, #43833, #5721, #37889, #11312, #59556, #49763, #48379, #54662, #38578, #21801, #33346, #32995, #28098, #27063, #44540, #49410, #27403, #12010, #11656, #48730, #55011, #65833, #54310, #1521, #16562, #22841, #27758, #32650, #44188, #33692, #833, #39276, #17254, #59209, #59902, #49069, #7112, #65485, #53962, #38935, #1180, #22149, #43134, #22491, #60257, #28450, #12361, #60598, #1873, #12709, #23192 ),
 ( #65133, #17959, #486, #6067, #43491, #64788, #24226, #56391, #34730, #29498, #7453, #19673, #8837, #35414, #19319, #44876, #23883, #7804, #66870, #50805, #23536, #29841, #29145, #40994, #30176, #62319, #13407, #8494, #2897, #56042, #24911, #45565, #24574, #51481, #66524, #61291, #51148, #55706, #45219, #28804, #3578, #66180, #46245, #3246, #18983, #40309, #67551, #14433, #50115, #61629, #45898, #55356, #18301, #18644, #67208, #8149, #39975, #13744, #2222, #39625, #60946, #35077, #13060, #34389, #40645, #61978, #50452 ),
 ( #2552, #14088, #56740, #36092, #9170, #35754, #53202, #62985, #68235, #3919, #68932, #25945, #52167, #10548, #57070, #63332, #25605, #25255, #15114, #14774, #63683, #15798, #46933, #60, #21383, #37127, #57751, #58445, #30509, #46593, #62654, #51821, #4611, #36786, #36434, #9863, #67899, #42715, #31891, #5303, #21046, #20017, #4269, #57407, #47278, #31207, #41341, #10208, #9511, #64019, #26645, #30853, #52511, #58106, #68579, #20701, #47962, #42030, #4962, #20357, #41680, #15461, #31541, #52861, #26295, #47621, #42378 ) ),
 .UNSPECIFIED., .F., .F., .F.,
 ( 4, 4 ),
 ( 4, 1, 1, 1, 1, 1, 1, 1, 1, 1, 1, 1, 1, 1, 1, 1, 1, 1, 1, 1, 1, 1, 1, 1, 1, 1, 1, 1, 1, 1, 1, 1, 1, 1, 1, 1, 1, 1, 1, 1, 1, 1, 1, 1, 1, 1, 1, 1, 1, 1, 1, 1, 1, 1, 1, 1, 1, 1, 1, 1, 1, 1, 1, 1, 4 ),
 ( -0.02000000000000000042, 1.020000000000000018 ),
 ( -0.02000000000000000042, -0.003749999999999999861, 0.01250000000000000069, 0.02875000000000000125, 0.04499999999999999833, 0.06124999999999999889, 0.07749999999999999944, 0.09375000000000000000, 0.1100000000000000006, 0.1262500000000000011, 0.1424999999999999878, 0.1587500000000000022, 0.1749999999999999889, 0.1912500000000000033, 0.2074999999999999900, 0.2237500000000000044, 0.2399999999999999911, 0.2562499999999999778, 0.2725000000000000200, 0.2887500000000000067, 0.3049999999999999933, 0.3212499999999999800, 0.3375000000000000222, 0.3537500000000000089, 0.3699999999999999956, 0.3862499999999999822, 0.4025000000000000244, 0.4187500000000000111, 0.4349999999999999978, 0.4512499999999999845, 0.4675000000000000266, 0.4837500000000000133, 0.5000000000000000000, 0.5162499999999999867, 0.5324999999999999734, 0.5487499999999999600, 0.5649999999999999467, 0.5812500000000000444, 0.5975000000000000311, 0.6137500000000000178, 0.6300000000000000044, 0.6462499999999999911, 0.6624999999999999778, 0.6787499999999999645, 0.6949999999999999512, 0.7112500000000000488, 0.7275000000000000355, 0.7437500000000000222, 0.7600000000000000089, 0.7762499999999999956, 0.7924999999999999822, 0.8087499999999999689, 0.8249999999999999556, 0.8412500000000000533, 0.8575000000000000400, 0.8737500000000000266, 0.8900000000000000133, 0.9062500000000000000, 0.9224999999999999867, 0.9387499999999999734, 0.9549999999999999600, 0.9712499999999999467, 0.9875000000000000444, 1.003749999999999920, 1.020000000000000018 ),
 .UNSPECIFIED. ) ;
#59494=CARTESIAN_POINT ( 'NONE',  ( 11.55194988689359903, -3.419512757306400363, -8.638573882912000457 ) ) ;
#59556=CARTESIAN_POINT ( 'NONE',  ( 9.786633995697998856, -3.001718438313799808, -7.610798122400000310 ) ) ;
#59570=CARTESIAN_POINT ( 'NONE',  ( 10.65413259636999932, -4.783377755405500587, -7.926858177843299380 ) ) ;
#59577=CARTESIAN_POINT ( 'NONE',  ( 8.768793171737998549, -4.404188085824999987, -8.374125585548998885 ) ) ;
#59584=CARTESIAN_POINT ( 'NONE',  ( 11.83003632436370012, -5.243255406354000669, -7.209663534847899236 ) ) ;
#59658=ADVANCED_FACE ( 'NONE', ( #33377 ), #2251, .F. ) ;
#59661=CARTESIAN_POINT ( 'NONE',  ( 8.795853127542962113, -3.970210778477947233, -8.445853177989366856 ) ) ;
#59680=CARTESIAN_POINT ( 'NONE',  ( 9.393930206848999376, -5.250000000000000000, -7.500000000000000000 ) ) ;
#59689=CARTESIAN_POINT ( 'NONE',  ( 11.38379707368349969, -4.566644629509899467, -6.509947486183500054 ) ) ;
#59693=CARTESIAN_POINT ( 'NONE',  ( 11.30367835872029936, -5.113555564477999305, -6.798177532456199934 ) ) ;
#59704=EDGE_CURVE ( 'NONE', #44736, #55747, #61064, .T. ) ;
#59722=CARTESIAN_POINT ( 'NONE',  ( 10.15303300763299887, -3.212834858289399964, -8.325626572044798834 ) ) ;
#59744=CARTESIAN_POINT ( 'NONE',  ( 11.71922412107039868, -3.930460928605089777, -6.185573549454999487 ) ) ;
#59745=VERTEX_POINT ( 'NONE', #41024 ) ;
#59773=CARTESIAN_POINT ( 'NONE',  ( 10.98995257254739855, -5.095356924909000718, -7.818564472783199548 ) ) ;
#59785=CARTESIAN_POINT ( 'NONE',  ( 9.989763540182750035, -3.672815144550900524, -8.717465845835395299 ) ) ;
#59789=CARTESIAN_POINT ( 'NONE',  ( 9.175772138681999479, -4.424886761933599644, -6.440186012775000357 ) ) ;
#59807=CARTESIAN_POINT ( 'NONE',  ( 10.94903032197929882, -3.496160833528699996, -6.795411691360399686 ) ) ;
#59840=CARTESIAN_POINT ( 'NONE',  ( 10.29657053952199952, -4.502253688815499366, -6.324815923923999605 ) ) ;
#59896=CARTESIAN_POINT ( 'NONE',  ( 10.78976354018297634, -4.327184855449096368, -6.282534154164603812 ) ) ;
#59902=CARTESIAN_POINT ( 'NONE',  ( 9.026759580228999269, -4.976892840331100132, -7.266499081715599218 ) ) ;
#59930=CARTESIAN_POINT ( 'NONE',  ( 11.38678751119029897, -5.166297436425000278, -8.110172976325500827 ) ) ;
#59958=CARTESIAN_POINT ( 'NONE',  ( 9.988317406969001055, -3.762080884004200154, -8.756892549790999070 ) ) ;
#60035=CARTESIAN_POINT ( 'NONE',  ( 10.57564694612699974, -4.931992688388300294, -7.871941502982999772 ) ) ;
#60040=CARTESIAN_POINT ( 'NONE',  ( 11.05435090131019926, -2.880552878538999995, -8.192386390235398608 ) ) ;
#60077=CARTESIAN_POINT ( 'NONE',  ( 11.50271932425157040, -4.187398418774900044, -8.764198628556998827 ) ) ;
#60096=CARTESIAN_POINT ( 'NONE',  ( 11.80233327354039830, -5.101536739857000846, -6.779499720266399798 ) ) ;
#60106=ADVANCED_FACE ( 'NONE', ( #23490 ), #37137, .F. ) ;
#60127=CARTESIAN_POINT ( 'NONE',  ( 11.62579573085663043, -2.760622544769000264, -7.714452430741599365 ) ) ;
#60130=CARTESIAN_POINT ( 'NONE',  ( 11.59999999999999964, -2.935681553670999921, -8.155535082817699788 ) ) ;
#60144=CARTESIAN_POINT ( 'NONE',  ( 10.40644474310099810, -3.106516218291800246, -7.933599538786499039 ) ) ;
#60163=CARTESIAN_POINT ( 'NONE',  ( 11.31825954179440075, -3.333768806796900019, -8.053565341712399572 ) ) ;
#60179=CARTESIAN_POINT ( 'NONE',  ( 11.19955063476129631, -3.023401864784706294, -6.673569913327194847 ) ) ;
#60193=EDGE_LOOP ( 'NONE', ( #28842, #22963, #54652, #27841, #19287 ) ) ;
#60220=VERTEX_POINT ( 'NONE', #21848 ) ;
#60257=CARTESIAN_POINT ( 'NONE',  ( 8.773468108405998223, -3.033597967472499768, -7.773695785133000413 ) ) ;
#60272=CARTESIAN_POINT ( 'NONE',  ( 10.57101354018312023, -3.231816600031356845, -8.499583552997725278 ) ) ;
#60283=CARTESIAN_POINT ( 'NONE',  ( 11.75203632436369894, -5.109717061557999429, -7.240848640331599917 ) ) ;
#60291=ORIENTED_EDGE ( 'NONE', *, *, #26125, .F. ) ;
#60388=CARTESIAN_POINT ( 'NONE',  ( 11.51145123989532948, -3.394760891061399999, -8.668865425277999748 ) ) ;
#60420=CARTESIAN_POINT ( 'NONE',  ( 11.20733594839949809, -3.159733897807000425, -6.537051788466999191 ) ) ;
#60469=AXIS2_PLACEMENT_3D ( 'NONE', #44589, #65187, #7161 ) ;
#60471=CARTESIAN_POINT ( 'NONE',  ( 11.21149010443640037, -2.862435565199000109, -7.585072163144589652 ) ) ;
#60486=CARTESIAN_POINT ( 'NONE',  ( 9.173759580228997734, -4.976892840331100132, -7.266499081715599218 ) ) ;
#60502=CARTESIAN_POINT ( 'NONE',  ( 11.14595257254739913, -4.831736303435800295, -7.741895249827200232 ) ) ;
#60503=ORIENTED_EDGE ( 'NONE', *, *, #2910, .F. ) ;
#60528=EDGE_CURVE ( 'NONE', #50859, #32857, #52757, .T. ) ;
#60541=CARTESIAN_POINT ( 'NONE',  ( 11.25656651104150008, -3.873914634362100262, -6.228222165170999247 ) ) ;
#60598=CARTESIAN_POINT ( 'NONE',  ( 8.697480666858998788, -3.665111009453500213, -8.446938520915798776 ) ) ;
#60616=CARTESIAN_POINT ( 'NONE',  ( 10.46684687351657672, -4.768183399968645375, -8.499583552997723501 ) ) ;
#60627=CARTESIAN_POINT ( 'NONE',  ( 11.80233327354039830, -5.101536739857000846, -6.779499720266399798 ) ) ;
#60651=AXIS2_PLACEMENT_3D ( 'NONE', #11056, #27482, #38661 ) ;
#60652=CARTESIAN_POINT ( 'NONE',  ( 10.29226717315700057, -4.973628086880700572, -6.670281532133299329 ) ) ;
#60683=CARTESIAN_POINT ( 'NONE',  ( 11.59999999999999964, -4.817420948848700313, -7.174999999999999822 ) ) ;
#60720=EDGE_CURVE ( 'NONE', #24854, #40590, #15502, .T. ) ;
#60722=CARTESIAN_POINT ( 'NONE',  ( 8.942941355974880935, -4.954666522228586167, -6.948775311896397966 ) ) ;
#60724=CARTESIAN_POINT ( 'NONE',  ( 9.973631561148998514, -4.684311564990208510, -8.575598637068459595 ) ) ;
#60730=CARTESIAN_POINT ( 'NONE',  ( 11.15278751119019773, -4.790480620979200133, -7.913556523549700294 ) ) ;
#60759=CARTESIAN_POINT ( 'NONE',  ( 10.41964694612699915, -5.186980343482999523, -7.973702485506099613 ) ) ;
#60765=CARTESIAN_POINT ( 'NONE',  ( 10.32055864497999842, -3.317414799430800088, -8.034587760591801242 ) ) ;
#60781=FACE_OUTER_BOUND ( 'NONE', #13935, .T. ) ;
#60814=CARTESIAN_POINT ( 'NONE',  ( 11.14595257254739913, -4.831736303435800295, -7.741895249827200232 ) ) ;
#60815=CARTESIAN_POINT ( 'NONE',  ( 10.20226357027499908, -2.879914860223000250, -7.716099591766099053 ) ) ;
#60832=CARTESIAN_POINT ( 'NONE',  ( 9.123101285863999266, -4.646739515667500875, -6.731514281717299930 ) ) ;
#60850=CARTESIAN_POINT ( 'NONE',  ( 10.48133997687999930, -3.815400206859000054, -6.653701289769800020 ) ) ;
#60885=CARTESIAN_POINT ( 'NONE',  ( 11.08425954179440076, -3.017023678917100327, -8.316745941391600283 ) ) ;
#60940=CARTESIAN_POINT ( 'NONE',  ( 10.68559687351635112, -2.907767014557174790, -6.870476274536379435 ) ) ;
#60946=CARTESIAN_POINT ( 'NONE',  ( 8.695468108405998819, -2.901397043998999781, -7.811136554427399403 ) ) ;
#60947=CARTESIAN_POINT ( 'NONE',  ( 9.698096873516668381, -3.672815144550895639, -6.282534154164608253 ) ) ;
#60997=CARTESIAN_POINT ( 'NONE',  ( 10.39358376188600097, -5.078750111091999919, -8.187519150726398465 ) ) ;
#61004=EDGE_LOOP ( 'NONE', ( #30756, #19802, #13929, #23988, #45091, #42610, #62953, #50364, #43772, #31465 ) ) ;
#61031=DIRECTION ( 'NONE',  ( 0.000000000000000000, 0.000000000000000000, -1.000000000000000000 ) ) ;
#61062=ORIENTED_EDGE ( 'NONE', *, *, #65013, .T. ) ;
#61064=B_SPLINE_CURVE_WITH_KNOTS ( 'NONE', 3,
 ( #25288, #30540, #50831, #56770, #46622, #14803, #3609, #52198, #61660, #46276 ),
 .UNSPECIFIED., .F., .F.,
 ( 4, 2, 2, 2, 4 ),
 ( 0.000000000000000000, 0.2500000000000000000, 0.5000000000000000000, 0.7500000000000000000, 1.000000000000000000 ),
 .UNSPECIFIED. ) ;
#61079=CARTESIAN_POINT ( 'NONE',  ( 10.76857802013509868, -5.174568897094999897, -7.472656658230009796 ) ) ;
#61116=CARTESIAN_POINT ( 'NONE',  ( 10.14325461470300027, -4.840245908677600184, -7.713763321667399531 ) ) ;
#61131=CARTESIAN_POINT ( 'NONE',  ( 10.76346886766499900, -4.634677072395899877, -6.346853961441000003 ) ) ;
#61162=CARTESIAN_POINT ( 'NONE',  ( 11.46595122972049907, -3.656201404350900130, -6.704952129760900270 ) ) ;
#61163=CARTESIAN_POINT ( 'NONE',  ( 10.17349413291699811, -2.837298848764000514, -6.969488574374499201 ) ) ;
#61180=CARTESIAN_POINT ( 'NONE',  ( 9.855633995697999694, -3.138280386550500012, -7.595641268826199166 ) ) ;
#61189=ORIENTED_EDGE ( 'NONE', *, *, #24272, .F. ) ;
#61196=CARTESIAN_POINT ( 'NONE',  ( 11.02287616594229824, -4.261927842557799551, -6.674353346984900348 ) ) ;
#61232=CARTESIAN_POINT ( 'NONE',  ( 10.32118582084299874, -4.836160649475099937, -6.533484739457099622 ) ) ;
#61245=CARTESIAN_POINT ( 'NONE',  ( 11.60948876160955479, -4.695527826393099957, -8.223320049540498999 ) ) ;
#61291=CARTESIAN_POINT ( 'NONE',  ( 9.328696787962998727, -3.803923679411099990, -6.375149554610999303 ) ) ;
#61295=FACE_OUTER_BOUND ( 'NONE', #33953, .T. ) ;
#61318=CARTESIAN_POINT ( 'NONE',  ( 11.10612378248509913, -4.482960757953799558, -6.586279795136899651 ) ) ;
#61343=CARTESIAN_POINT ( 'NONE',  ( 10.01163399569799850, -2.865156490077000129, -7.625954975973699312 ) ) ;
#61403=EDGE_CURVE ( 'NONE', #43301, #64554, #48983, .T. ) ;
#61417=CARTESIAN_POINT ( 'NONE',  ( 9.957691290288998687, -4.889436474118637577, -8.413289387078533466 ) ) ;
#61422=CARTESIAN_POINT ( 'NONE',  ( 10.64902344389989963, -4.883530143601199747, -6.963800219468099684 ) ) ;
#61472=CARTESIAN_POINT ( 'NONE',  ( 10.64391429142989765, -3.977620450637519678, -6.325326139450999641 ) ) ;
#61503=CARTESIAN_POINT ( 'NONE',  ( 10.49349279008999858, -4.332388355267299929, -8.734031750754999379 ) ) ;
#61521=CARTESIAN_POINT ( 'NONE',  ( 9.300405316139999101, -4.213249376011100722, -8.481512610189300361 ) ) ;
#61537=CARTESIAN_POINT ( 'NONE',  ( 11.78179573085659904, -3.026866171144600326, -7.668383662421899061 ) ) ;
#61580=CARTESIAN_POINT ( 'NONE',  ( 9.784141369869628235, -3.576408136849907216, -8.265573120213877800 ) ) ;
#61584=CARTESIAN_POINT ( 'NONE',  ( 10.87518447801629939, -3.134012688501500055, -7.480906371072489236 ) ) ;
#61629=CARTESIAN_POINT ( 'NONE',  ( 8.974088727410999056, -5.137817193984000497, -7.595427884080399927 ) ) ;
#61658=CARTESIAN_POINT ( 'NONE',  ( 10.89835090130999973, -3.121033016283800254, -8.043647632228999811 ) ) ;
#61660=CARTESIAN_POINT ( 'NONE',  ( 8.832144816391009456, -3.783447583457012264, -8.465905425056138967 ) ) ;
#61681=CARTESIAN_POINT ( 'NONE',  ( 10.06229229006299875, -3.012566816337000297, -6.926667499798199401 ) ) ;
#61701=ADVANCED_FACE ( 'NONE', ( #33861 ), #59483, .F. ) ;
#61706=FACE_OUTER_BOUND ( 'NONE', #45936, .T. ) ;
#61747=PRODUCT ( 'Terminal Screw 1', 'Terminal Screw 1', '', ( #11324 ) ) ;
#61750=CARTESIAN_POINT ( 'NONE',  ( 8.863694533038728451, -3.488685518255360662, -6.614578276768173559 ) ) ;
#61757=CARTESIAN_POINT ( 'NONE',  ( 10.44999293566599974, -3.279967330949900450, -8.383280442119700027 ) ) ;
#61773=B_SPLINE_CURVE_WITH_KNOTS ( 'NONE', 3,
 ( #17677, #39000, #7180, #38296 ),
 .UNSPECIFIED., .F., .F.,
 ( 4, 4 ),
 ( 0.000000000000000000, 1.000000000000000000 ),
 .UNSPECIFIED. ) ;
#61775=CARTESIAN_POINT ( 'NONE',  ( 11.07299956498199833, -2.792989229543000107, -7.825000000000000178 ) ) ;
#61779=EDGE_CURVE ( 'NONE', #67987, #51205, #4939, .T. ) ;
#61787=EDGE_CURVE ( 'NONE', #30625, #54024, #53367, .T. ) ;
#61796=CARTESIAN_POINT ( 'NONE',  ( 8.952784697134999803, -3.529509552262100058, -6.771750947090999340 ) ) ;
#61810=CARTESIAN_POINT ( 'NONE',  ( 11.56322412107030928, -3.945399343424460525, -6.467939235001000320 ) ) ;
#61840=CARTESIAN_POINT ( 'NONE',  ( 11.78594988689359901, -3.606563555963900214, -8.271690446953899212 ) ) ;
#61841=CARTESIAN_POINT ( 'NONE',  ( 10.44426222744799837, -4.986443098259000450, -8.312555471636301263 ) ) ;
#61857=CARTESIAN_POINT ( 'NONE',  ( 8.996455549952997899, -3.218304396998100003, -6.869290649434700136 ) ) ;
#61868=VECTOR ( 'NONE', #43838, 1000.000000000000227 ) ;
#61879=CARTESIAN_POINT ( 'NONE',  ( 11.21564426047340035, -3.460037133261700149, -8.345807871442598724 ) ) ;
#61893=EDGE_CURVE ( 'NONE', #62696, #3420, #2477, .T. ) ;
#61923=CARTESIAN_POINT ( 'NONE',  ( 8.998937807218627682, -4.055078665241000024, -6.626788336335921237 ) ) ;
#61928=CARTESIAN_POINT ( 'NONE',  ( 10.29262282008599882, -3.548418513060800361, -8.228386593078399258 ) ) ;
#61978=CARTESIAN_POINT ( 'NONE',  ( 8.577265421554999492, -4.214287043487900064, -8.608472884860999486 ) ) ;
#62005=CARTESIAN_POINT ( 'NONE',  ( 10.60235971519489873, -3.394698737128500010, -6.493038401303000029 ) ) ;
#62026=CARTESIAN_POINT ( 'NONE',  ( 10.48444474310099928, -2.984290294633999974, -7.992914665944799602 ) ) ;
#62059=B_SPLINE_CURVE_WITH_KNOTS ( 'NONE', 3,
 ( #29620, #50236, #44662, #60722, #24352, #7582, #8274, #13532, #2340, #28931, #46020, #61750, #23658, #33820, #45684, #66990 ),
 .UNSPECIFIED., .F., .F.,
 ( 4, 2, 2, 2, 2, 2, 2, 4 ),
 ( 0.000000000000000000, 0.1249999999999996669, 0.2499999999999993339, 0.3749999999999990008, 0.4999999999999986677, 0.6249999999999991118, 0.7499999999999995559, 1.000000000000000000 ),
 .UNSPECIFIED. ) ;
#62100=CARTESIAN_POINT ( 'NONE',  ( 10.52435971519499880, -3.467537960339900138, -6.614211617270199461 ) ) ;
#62135=MECHANICAL_DESIGN_GEOMETRIC_PRESENTATION_REPRESENTATION('',(#14143),#58794);
#62136=CARTESIAN_POINT ( 'NONE',  ( 9.662000818238999145, -4.767147064380999666, -7.903971937289999694 ) ) ;
#62151=CARTESIAN_POINT ( 'NONE',  ( 10.55569598648999907, -2.869047858956000230, -8.173387776112500447 ) ) ;
#62156=EDGE_LOOP ( 'NONE', ( #26403, #49761, #7073, #56899, #68008, #15295, #7473, #19898, #57196, #48507, #34959, #33135 ) ) ;
#62181=CARTESIAN_POINT ( 'NONE',  ( 10.61656919669529842, -2.774362666861999838, -7.862118085997298778 ) ) ;
#62200=CARTESIAN_POINT ( 'NONE',  ( 9.197076168957998732, -4.439974903344300117, -8.247081005603298820 ) ) ;
#62219=CARTESIAN_POINT ( 'NONE',  ( 11.77359063708300013, -3.044227915785300276, -7.768721787835699999 ) ) ;
#62263=CARTESIAN_POINT ( 'NONE',  ( 9.961445400145626294, -3.652722274830687343, -6.696924380570436597 ) ) ;
#62269=CARTESIAN_POINT ( 'NONE',  ( 11.29364426047339975, -3.533902447304699823, -8.230103870496201068 ) ) ;
#62290=CARTESIAN_POINT ( 'NONE',  ( 10.73976354018279977, -4.327184855449098144, -6.282534154164605589 ) ) ;
#62297=CARTESIAN_POINT ( 'NONE',  ( 10.34393020684899867, -5.250000000000000000, -7.500000000000000000 ) ) ;
#62319=CARTESIAN_POINT ( 'NONE',  ( 9.581988259785999773, -4.149395984695000372, -8.631996151823999597 ) ) ;
#62344=CARTESIAN_POINT ( 'NONE',  ( 10.56080513895999928, -2.973119161490000106, -6.929150654994399083 ) ) ;
#62376=CARTESIAN_POINT ( 'NONE',  ( 9.643930206848999376, -2.750000000000000000, -7.500000000000000000 ) ) ;
#62392=DIRECTION ( 'NONE',  ( -1.000000000000000000, 0.000000000000000000, 0.000000000000000000 ) ) ;
#62434=CARTESIAN_POINT ( 'NONE',  ( 11.37299956498129916, -5.207010770456999893, -7.174999999999999822 ) ) ;
#62445=CARTESIAN_POINT ( 'NONE',  ( 11.25962254157670905, -3.830327337663943510, -8.360248390549317676 ) ) ;
#62452=EDGE_LOOP ( 'NONE', ( #22935, #37915, #68807, #14807 ) ) ;
#62519=CARTESIAN_POINT ( 'NONE',  ( 10.43210941423799909, -3.358814833524500276, -6.917608226833099394 ) ) ;
#62520=CARTESIAN_POINT ( 'NONE',  ( 11.23195122972050086, -3.492749840905900349, -6.326963915009999440 ) ) ;
#62537=CARTESIAN_POINT ( 'NONE',  ( 8.766480666858997850, -3.710922827228400056, -8.317400147935998689 ) ) ;
#62555=CARTESIAN_POINT ( 'NONE',  ( 11.06795257254739973, -4.963546614172099858, -7.780229861306499295 ) ) ;
#62597=CARTESIAN_POINT ( 'NONE',  ( 10.01210369451062654, -4.198138975488563851, -6.647783351891156656 ) ) ;
#62601=CARTESIAN_POINT ( 'NONE',  ( 10.38287885159599888, -3.139900861731399928, -7.397393329751199786 ) ) ;
#62654=CARTESIAN_POINT ( 'NONE',  ( 9.377342523874999003, -5.264483068122999931, -7.306436165809000016 ) ) ;
#62659=CARTESIAN_POINT ( 'NONE',  ( 8.763353253171903390, -4.132446745988498371, -8.413353309630901222 ) ) ;
#62676=CARTESIAN_POINT ( 'NONE',  ( 9.099999931440999390, -2.750000000000000000, -7.500000000000000000 ) ) ;
#62679=CARTESIAN_POINT ( 'NONE',  ( 10.52435971519499880, -3.467537960339900138, -6.614211617270199461 ) ) ;
#62696=VERTEX_POINT ( 'NONE', #40856 ) ;
#62782=CARTESIAN_POINT ( 'NONE',  ( 11.27531844363630320, -3.660964894626073107, -8.308695084076106241 ) ) ;
#62792=LINE ( 'NONE', #19815, #46051 ) ;
#62856=CARTESIAN_POINT ( 'NONE',  ( 11.26487482311540056, -3.069598554678400149, -7.875904247640098887 ) ) ;
#62893=CARTESIAN_POINT ( 'NONE',  ( 11.50687348028854906, -5.003459210197000573, -8.042549288197099244 ) ) ;
#62919=CARTESIAN_POINT ( 'NONE',  ( 8.801820635884373800, -3.939853377893446584, -8.450403350428134175 ) ) ;
#62922=CARTESIAN_POINT ( 'NONE',  ( 8.724024145839392119, -4.217522721361648408, -8.345440805164775711 ) ) ;
#62930=CARTESIAN_POINT ( 'NONE',  ( 9.201637546194751494, -3.727464796005204750, -6.269669426086102781 ) ) ;
#62935=CARTESIAN_POINT ( 'NONE',  ( 9.556179045228626379, -4.616765641734932757, -6.879409626165266189 ) ) ;
#62939=CARTESIAN_POINT ( 'NONE',  ( 10.23103300763299828, -3.307558760216100069, -8.226274395107198600 ) ) ;
#62944=CARTESIAN_POINT ( 'NONE',  ( 10.35226354018316108, -5.092232985442820770, -6.870476274536370553 ) ) ;
#62953=ORIENTED_EDGE ( 'NONE', *, *, #34544, .T. ) ;
#62971=CARTESIAN_POINT ( 'NONE',  ( 11.32299956498189886, -5.207010770456999893, -7.174999999999999822 ) ) ;
#62985=CARTESIAN_POINT ( 'NONE',  ( 9.959912909067998754, -4.809406943772300380, -8.490578012456198920 ) ) ;
#63011=CARTESIAN_POINT ( 'NONE',  ( 10.52946886766499901, -4.430164648092599577, -6.718432993015899690 ) ) ;
#63052=FACE_OUTER_BOUND ( 'NONE', #15669, .T. ) ;
#63109=DIRECTION ( 'NONE',  ( -1.000000000000000000, 0.000000000000000000, 0.000000000000000000 ) ) ;
#63118=CARTESIAN_POINT ( 'NONE',  ( 10.52946886766499901, -4.430164648092599577, -6.718432993015899690 ) ) ;
#63183=CARTESIAN_POINT ( 'NONE',  ( 9.154341692891295068, -2.749999283195044164, -7.336371291557481022 ) ) ;
#63185=CARTESIAN_POINT ( 'NONE',  ( 11.43028911132391379, -5.144000659054666080, -8.059011948032955175 ) ) ;
#63194=CARTESIAN_POINT ( 'NONE',  ( 11.73256516821459883, -3.293702443348299980, -8.212808089543500500 ) ) ;
#63213=CARTESIAN_POINT ( 'NONE',  ( 9.653000818238998804, -4.767147064380999666, -7.903971937289999694 ) ) ;
#63221=EDGE_CURVE ( 'NONE', #15621, #17417, #41544, .T. ) ;
#63235=CARTESIAN_POINT ( 'NONE',  ( 10.47303166480599934, -5.137916160623999140, -7.580230465881790280 ) ) ;
#63236=ORIENTED_EDGE ( 'NONE', *, *, #35028, .F. ) ;
#63238=CARTESIAN_POINT ( 'NONE',  ( 10.12435795695566476, -2.750000000000000000, -7.807440182398264206 ) ) ;
#63262=CARTESIAN_POINT ( 'NONE',  ( 8.789886373836322875, -3.999992178805580334, -8.439846342473931173 ) ) ;
#63264=EDGE_LOOP ( 'NONE', ( #31698, #10035, #30280, #20375, #46970 ) ) ;
#63273=EDGE_LOOP ( 'NONE', ( #33582, #6179, #32754, #13511 ) ) ;
#63285=CARTESIAN_POINT ( 'NONE',  ( 10.52641638348499953, -4.974961480482700260, -7.262511127784999410 ) ) ;
#63302=CARTESIAN_POINT ( 'NONE',  ( 9.456405316140999773, -4.271593136661399726, -8.750048621292000561 ) ) ;
#63332=CARTESIAN_POINT ( 'NONE',  ( 9.757279731608999640, -3.885210315895800015, -6.225948307210999566 ) ) ;
#63355=CARTESIAN_POINT ( 'NONE',  ( 11.28118179236249929, -4.267047616085000605, -6.250199235344999771 ) ) ;
#63379=AXIS2_PLACEMENT_3D ( 'NONE', #27044, #5017, #25659 ) ;
#63415=CARTESIAN_POINT ( 'NONE',  ( 9.940621437244999470, -3.424116261072899903, -6.851875117168399143 ) ) ;
#63432=CARTESIAN_POINT ( 'NONE',  ( 11.18412378248529926, -4.549028353065900809, -6.461285588983000316 ) ) ;
#63445=ORIENTED_EDGE ( 'NONE', *, *, #60720, .F. ) ;
#63508=EDGE_CURVE ( 'NONE', #54024, #60220, #4390, .T. ) ;
#63551=CARTESIAN_POINT ( 'NONE',  ( 11.53564291764652872, -4.995889373412399692, -7.376893506359599506 ) ) ;
#63570=CARTESIAN_POINT ( 'NONE',  ( 8.741151519676998660, -3.981249765141819719, -8.366807394121199337 ) ) ;
#63586=CARTESIAN_POINT ( 'NONE',  ( 11.58071932425156980, -4.167269912168199753, -8.628410767520000135 ) ) ;
#63601=B_SPLINE_CURVE_WITH_KNOTS ( 'NONE', 3,
 ( #50568, #34842, #56153, #8261, #24342, #31650, #37234, #48069, #47041, #32004, #42483, #31309, #41791, #68694, #69047, #20808, #26755, #173 ),
 .UNSPECIFIED., .F., .F.,
 ( 4, 2, 2, 2, 2, 2, 2, 2, 4 ),
 ( 0.000000000000000000, 0.1250000000000000000, 0.2500000000000000000, 0.3750000000000000000, 0.5000000000000000000, 0.6250000000000000000, 0.7500000000000000000, 0.8750000000000000000, 1.000000000000000000 ),
 .UNSPECIFIED. ) ;
#63636=CARTESIAN_POINT ( 'NONE',  ( 10.25564828895399927, -3.119330945648699949, -7.981013126389099099 ) ) ;
#63641=CARTESIAN_POINT ( 'NONE',  ( 10.27934687351620724, -4.163624617374463988, -6.249999999999999112 ) ) ;
#63650=CARTESIAN_POINT ( 'NONE',  ( 9.279101285863998072, -4.823683599683300294, -6.521261160937499746 ) ) ;
#63655=B_SPLINE_SURFACE_WITH_KNOTS ( 'NONE', 3, 3, ( 
 ( #37679, #27198, #54449, #39067, #55142, #7245, #277, #43972, #16351, #60388, #65276, #28230, #49545, #22626, #59693, #17747, #33480, #1658, #22974, #21935, #60040, #17390, #38720, #64234, #43273, #42929, #32787, #59009, #44324, #65622, #11794, #1311, #22286, #43627, #11111 ),
 ( #12492, #64921, #49204, #33827, #32446, #12152, #5857, #53760, #48517, #54795, #626, #64581, #16691, #38019, #59346, #11446, #54102, #6197, #17036, #33134, #6550, #27892, #34171, #56174, #66999, #61079, #24360, #2347, #29628, #3368, #56517, #45005, #8962, #61757, #24706 ),
 ( #7590, #67335, #45692, #19455, #13199, #50931, #23329, #39760, #2691, #55491, #55836, #40431, #29971, #19109, #56865, #44669, #50590, #13876, #35207, #8623, #65963, #51274, #18779, #7940, #46028, #3030, #61422, #34526, #40776, #62100, #8284, #14219, #35547, #66311, #23667 ),
 ( #49897, #18435, #66660, #29276, #24016, #2006, #18088, #45350, #40110, #13540, #34859, #39409, #60730, #12844, #28940, #50243, #14900, #36224, #4047, #42503, #31329, #47407, #52641, #57538, #30990, #68026, #58233, #63118, #5089, #25730, #15588, #4734, #52993, #36567, #26425 ) ),
 .UNSPECIFIED., .F., .F., .F.,
 ( 4, 4 ),
 ( 4, 1, 1, 1, 1, 1, 1, 1, 1, 1, 1, 1, 1, 1, 1, 1, 1, 1, 1, 1, 1, 1, 1, 1, 1, 1, 1, 1, 1, 1, 1, 1, 4 ),
 ( -0.02000000000000000042, 1.020000000000000018 ),
 ( 0.1633025096610999927, 0.1899619885200000136, 0.2166214673788000034, 0.2432809462376999965, 0.2699404250964999585, 0.2965999039553000038, 0.3232593828141999692, 0.3499188616730000145, 0.3765783405318000043, 0.4032378193906999697, 0.4298972982494999595, 0.4565567771083000048, 0.4832162559671999702, 0.5098757348260000155, 0.5365352136848999809, 0.5631946925437000262, 0.5898541714025000715, 0.6165136502614000369, 0.6431731291201999712, 0.6698326079790000165, 0.6964920868378999819, 0.7231515656967000272, 0.7498110445554999615, 0.7764705234143999268, 0.8031300022731999722, 0.8297894811320000175, 0.8564489599908999828, 0.8831084388497000282, 0.9097679177085999935, 0.9364273965674000388, 0.9630868754261999731, 0.9897463542851000495, 1.016405833144000015 ),
 .UNSPECIFIED. ) ;
#63678=CARTESIAN_POINT ( 'NONE',  ( 8.807788144226000426, -3.909067355573210278, -8.453461841935100196 ) ) ;
#63683=CARTESIAN_POINT ( 'NONE',  ( 9.630633995698000049, -2.728594541839999721, -7.641111829547599932 ) ) ;
#63705=CARTESIAN_POINT ( 'NONE',  ( 10.15303300763299887, -3.212834858289399964, -8.325626572044798834 ) ) ;
#63761=CARTESIAN_POINT ( 'NONE',  ( 9.256734463322999318, -3.909687748588949852, -8.362294405496898619 ) ) ;
#63775=CARTESIAN_POINT ( 'NONE',  ( 10.73213259636989925, -4.907524392912299582, -7.994504989494399361 ) ) ;
#63801=ORIENTED_EDGE ( 'NONE', *, *, #32793, .T. ) ;
#63805=AXIS2_PLACEMENT_3D ( 'NONE', #961, #22272, #43614 ) ;
#63851=CARTESIAN_POINT ( 'NONE',  ( 11.07299956498199833, -2.792989229543000107, -7.825000000000000178 ) ) ;
#63888=CARTESIAN_POINT ( 'NONE',  ( 10.35826357027499789, -3.149486845331399998, -7.664090691848299386 ) ) ;
#63907=CARTESIAN_POINT ( 'NONE',  ( 11.58810207955109917, -4.796537143354000499, -7.174999999999999822 ) ) ;
#63926=CARTESIAN_POINT ( 'NONE',  ( 11.40841235500449891, -4.841138636481000290, -6.729431436870699557 ) ) ;
#63961=VERTEX_POINT ( 'NONE', #16773 ) ;
#63972=CARTESIAN_POINT ( 'NONE',  ( 10.87103032197929942, -3.416314376401300201, -6.683751296690399357 ) ) ;
#63989=CARTESIAN_POINT ( 'NONE',  ( 10.26291290906799958, -4.635529777446699917, -8.277781595084700683 ) ) ;
#64008=CARTESIAN_POINT ( 'NONE',  ( 11.14955063476181607, -3.023401864784705850, -6.673569913327194847 ) ) ;
#64016=CARTESIAN_POINT ( 'NONE',  ( 8.982564767455606614, -5.103418008754404767, -7.795647801703331936 ) ) ;
#64019=CARTESIAN_POINT ( 'NONE',  ( 8.896088727410999653, -5.274736981944999847, -7.606911245136100064 ) ) ;
#64039=CARTESIAN_POINT ( 'NONE',  ( 11.06379841651039797, -4.401637675674300532, -8.567697191971999970 ) ) ;
#64045=CARTESIAN_POINT ( 'NONE',  ( 10.73724174883999893, -4.024531238983009906, -8.391788556008700439 ) ) ;
#64102=CARTESIAN_POINT ( 'NONE',  ( 10.01660887879199890, -4.196341783741199372, -6.655513263298900029 ) ) ;
#64115=CARTESIAN_POINT ( 'NONE',  ( 11.15278751119019773, -4.790480620979200133, -7.913556523549700294 ) ) ;
#64181=ORIENTED_EDGE ( 'NONE', *, *, #61787, .T. ) ;
#64185=CARTESIAN_POINT ( 'NONE',  ( 8.599999986286999132, -3.249999986289399789, -7.500000000038047787 ) ) ;
#64201=CARTESIAN_POINT ( 'NONE',  ( 10.94452754078378121, -3.491551460122512385, -6.788965764111623002 ) ) ;
#64224=B_SPLINE_SURFACE_WITH_KNOTS ( 'NONE', 3, 3, ( 
 ( #7166, #22547, #39331, #65886, #2609, #13118, #49818, #66578, #60997, #18356, #11711, #1577, #60652, #50169, #54366, #23250, #33050, #34447, #43890, #17311, #44593, #38636, #7862, #29196, #59958, #18698, #33401, #40031, #12069, #22895, #44246, #38990, #56442, #42351, #4926, #36403, #51201, #31855, #13461, #8204, #19032, #10515, #58076, #53170, #24629, #63302, #34784, #3294, #14141, #45616, #67259, #52829, #63650, #56093, #29553, #40359, #5272, #10180, #26612, #45949, #15429, #50854, #19376, #57720, #66922, #40697, #26262 ),
 ( #2949, #62026, #31507, #47592, #68899, #24282, #36756, #31176, #9828, #21014, #15768, #4576, #52480, #37097, #58410, #68547, #47931, #30, #61681, #21352, #61343, #13798, #35128, #29894, #8546, #25913, #47244, #20669, #41997, #10859, #65017, #49297, #43379, #33576, #65373, #43722, #38818, #26953, #22032, #48961, #16447, #37431, #27641, #12250, #28328, #49649, #1754, #17134, #58753, #54896, #38469, #1409, #22726, #59789, #54550, #5954, #372, #37776, #44072, #64325, #33232, #11892, #48619, #6647, #1070, #27988, #27295 ),
 ( #22381, #60144, #6996, #17494, #42680, #54194, #720, #63989, #64679, #16106, #32205, #53519, #5606, #48265, #21689, #43023, #59101, #11204, #32540, #53855, #16786, #38116, #59441, #11540, #32883, #6296, #55244, #7341, #23428, #28683, #29379, #40203, #50000, #44424, #44766, #13978, #45787, #29727, #18186, #51370, #34961, #67098, #18877, #51031, #50690, #61521, #35303, #66067, #8724, #56278, #60486, #30067, #60832, #2111, #39508, #12945, #33923, #61857, #12595, #45447, #3130, #23769, #56619, #19208, #24113, #40532, #34273 ),
 ( #2787, #24462, #55936, #23075, #18532, #8385, #66760, #65722, #13636, #17846, #55592, #39163, #7694, #29036, #50345, #8038, #2445, #45104, #66413, #39859, #61180, #13299, #34623, #19900, #41565, #31089, #52397, #9060, #63213, #4489, #68810, #20930, #9741, #37016, #14994, #35974, #10091, #4148, #25829, #15682, #31771, #41908, #30399, #40880, #24802, #68458, #62200, #52742, #67434, #4836, #14321, #56958, #46472, #42266, #35646, #51707, #3803, #25141, #67778, #47159, #20581, #41226, #46127, #62537, #63570, #26178, #31426 ) ),
 .UNSPECIFIED., .F., .F., .F.,
 ( 4, 4 ),
 ( 4, 1, 1, 1, 1, 1, 1, 1, 1, 1, 1, 1, 1, 1, 1, 1, 1, 1, 1, 1, 1, 1, 1, 1, 1, 1, 1, 1, 1, 1, 1, 1, 1, 1, 1, 1, 1, 1, 1, 1, 1, 1, 1, 1, 1, 1, 1, 1, 1, 1, 1, 1, 1, 1, 1, 1, 1, 1, 1, 1, 1, 1, 1, 1, 4 ),
 ( -0.02000000000000000042, 1.020000000000000018 ),
 ( -0.02000000000000000042, -0.003749999999999999861, 0.01250000000000000069, 0.02875000000000000125, 0.04499999999999999833, 0.06124999999999999889, 0.07749999999999999944, 0.09375000000000000000, 0.1100000000000000006, 0.1262500000000000011, 0.1424999999999999878, 0.1587500000000000022, 0.1749999999999999889, 0.1912500000000000033, 0.2074999999999999900, 0.2237500000000000044, 0.2399999999999999911, 0.2562499999999999778, 0.2725000000000000200, 0.2887500000000000067, 0.3049999999999999933, 0.3212499999999999800, 0.3375000000000000222, 0.3537500000000000089, 0.3699999999999999956, 0.3862499999999999822, 0.4025000000000000244, 0.4187500000000000111, 0.4349999999999999978, 0.4512499999999999845, 0.4675000000000000266, 0.4837500000000000133, 0.5000000000000000000, 0.5162499999999999867, 0.5324999999999999734, 0.5487499999999999600, 0.5649999999999999467, 0.5812500000000000444, 0.5975000000000000311, 0.6137500000000000178, 0.6300000000000000044, 0.6462499999999999911, 0.6624999999999999778, 0.6787499999999999645, 0.6949999999999999512, 0.7112500000000000488, 0.7275000000000000355, 0.7437500000000000222, 0.7600000000000000089, 0.7762499999999999956, 0.7924999999999999822, 0.8087499999999999689, 0.8249999999999999556, 0.8412500000000000533, 0.8575000000000000400, 0.8737500000000000266, 0.8900000000000000133, 0.9062500000000000000, 0.9224999999999999867, 0.9387499999999999734, 0.9549999999999999600, 0.9712499999999999467, 0.9875000000000000444, 1.003749999999999920, 1.020000000000000018 ),
 .UNSPECIFIED. ) ;
#64230=CARTESIAN_POINT ( 'NONE',  ( 10.94487616594229884, -4.303437140848100029, -6.543508100188799581 ) ) ;
#64234=CARTESIAN_POINT ( 'NONE',  ( 10.92968717260509948, -4.687649763627899979, -8.622362941748999532 ) ) ;
#64243=VECTOR ( 'NONE', #29760, 1000.000000000000000 ) ;
#64266=CARTESIAN_POINT ( 'NONE',  ( 10.66995391537419913, -3.056324258617099776, -8.140910455049299443 ) ) ;
#64272=CARTESIAN_POINT ( 'NONE',  ( 10.97028665956023019, -4.742415037725370652, -8.549395343567622874 ) ) ;
#64312=CARTESIAN_POINT ( 'NONE',  ( 10.30487885159599770, -3.003595720052600448, -7.381132626649399064 ) ) ;
#64325=CARTESIAN_POINT ( 'NONE',  ( 9.023797255587998833, -2.859210004667000149, -7.451702546394010085 ) ) ;
#64373=CARTESIAN_POINT ( 'NONE',  ( 8.786046699800500903, -3.154588942369298099, -7.961595344540238095 ) ) ;
#64380=CARTESIAN_POINT ( 'NONE',  ( 11.45348876160960039, -4.885820101980599794, -8.421216112044099589 ) ) ;
#64384=CARTESIAN_POINT ( 'NONE',  ( 8.748305582559998683, -3.908727042518870043, -8.362426869835999810 ) ) ;
#64386=CARTESIAN_POINT ( 'NONE',  ( 11.02812378248509795, -4.416893162838900544, -6.711274001288999536 ) ) ;
#64438=CARTESIAN_POINT ( 'NONE',  ( 10.01459632033899894, -4.929952350555500296, -7.120485934352199564 ) ) ;
#64454=CARTESIAN_POINT ( 'NONE',  ( 11.06967835872019812, -4.754733798270200928, -7.024326263066900111 ) ) ;
#64470=CARTESIAN_POINT ( 'NONE',  ( 10.32309687351566652, -5.217465845835395299, -7.172815144550894750 ) ) ;
#64491=ORIENTED_EDGE ( 'NONE', *, *, #56184, .T. ) ;
#64534=CARTESIAN_POINT ( 'NONE',  ( 10.93937577273821482, -4.461177266722074819, -8.699885912910445995 ) ) ;
#64554=VERTEX_POINT ( 'NONE', #52912 ) ;
#64564=CARTESIAN_POINT ( 'NONE',  ( 9.279336721442293268, -4.163631234563185401, -6.250006800841094723 ) ) ;
#64566=FACE_OUTER_BOUND ( 'NONE', #30041, .T. ) ;
#64577=CARTESIAN_POINT ( 'NONE',  ( 10.89564560330029863, -3.692495237344800341, -6.544808043482999160 ) ) ;
#64581=CARTESIAN_POINT ( 'NONE',  ( 11.35034208742529849, -4.630634088820300143, -8.491292290686200062 ) ) ;
#64613=CARTESIAN_POINT ( 'NONE',  ( 11.28118179236249929, -4.267047616085000605, -6.250199235344999771 ) ) ;
#64664=CARTESIAN_POINT ( 'NONE',  ( 10.89149144726329865, -4.659577337894599935, -6.569275630703699242 ) ) ;
#64668=CARTESIAN_POINT ( 'NONE',  ( 11.60000000000000142, -4.745632530848085118, -8.163463725006291583 ) ) ;
#64679=CARTESIAN_POINT ( 'NONE',  ( 10.23758376188599861, -4.847012523549299345, -8.039825975318500184 ) ) ;
#64726=CARTESIAN_POINT ( 'NONE',  ( 10.64533863405319991, -3.296214805808900028, -8.397761948794601139 ) ) ;
#64735=CARTESIAN_POINT ( 'NONE',  ( 11.59999999999999964, -4.149724965537171073, -6.485689145701417857 ) ) ;
#64786=EDGE_CURVE ( 'NONE', #17417, #54684, #47239, .T. ) ;
#64788=CARTESIAN_POINT ( 'NONE',  ( 10.08857120343299840, -4.055348968344419269, -8.640469672413999547 ) ) ;
#64801=CARTESIAN_POINT ( 'NONE',  ( 10.86190547754509872, -3.108323067758099967, -7.528299448264639260 ) ) ;
#64816=CARTESIAN_POINT ( 'NONE',  ( 11.30367835872029936, -5.113555564477999305, -6.798177532456199934 ) ) ;
#64824=ORIENTED_EDGE ( 'NONE', *, *, #55842, .T. ) ;
#64859=CARTESIAN_POINT ( 'NONE',  ( 11.59999999999999964, -4.000000000000000000, -7.500000000000000000 ) ) ;
#64879=DIRECTION ( 'NONE',  ( -1.000000000000000000, 0.000000000000000000, 0.000000000000000000 ) ) ;
#64888=CARTESIAN_POINT ( 'NONE',  ( 8.807788144226000426, -3.909067355573210278, -8.453461841935100196 ) ) ;
#64905=PLANE ( 'NONE',  #57715 ) ;
#64917=CARTESIAN_POINT ( 'NONE',  ( 10.52641638348499953, -4.974961480482700260, -7.262511127784999410 ) ) ;
#64921=CARTESIAN_POINT ( 'NONE',  ( 11.75203632436369894, -5.109717061557999429, -7.240848640331599917 ) ) ;
#64951=CARTESIAN_POINT ( 'NONE',  ( 11.05964426047339799, -3.312306505177499805, -8.577215873335999774 ) ) ;
#64952=VERTEX_POINT ( 'NONE', #11954 ) ;
#64958=CARTESIAN_POINT ( 'NONE',  ( 11.12299956498149811, -2.792989229543000107, -7.825000000000000178 ) ) ;
#64992=VECTOR ( 'NONE', #48097, 1000.000000000000000 ) ;
#65001=CARTESIAN_POINT ( 'NONE',  ( 10.15303300763299887, -3.212834858289399964, -8.325626572044798834 ) ) ;
#65013=EDGE_CURVE ( 'NONE', #54684, #62696, #38944, .T. ) ;
#65017=CARTESIAN_POINT ( 'NONE',  ( 9.758342523874999230, -5.128664655368000425, -7.327226901081999699 ) ) ;
#65035=CARTESIAN_POINT ( 'NONE',  ( 10.85056919669530018, -3.169300617545700138, -7.745432529082900253 ) ) ;
#65063=VERTEX_POINT ( 'NONE', #26604 ) ;
#65068=CARTESIAN_POINT ( 'NONE',  ( 11.05964426047339799, -3.312306505177499805, -8.577215873335999774 ) ) ;
#65080=CARTESIAN_POINT ( 'NONE',  ( 11.53979707368350027, -4.430269712815499972, -6.748224392138099326 ) ) ;
#65089=B_SPLINE_CURVE_WITH_KNOTS ( 'NONE', 3,
 ( #62297, #24554, #14415, #40973, #8129, #29475, #24893, #23513, #30487, #56371 ),
 .UNSPECIFIED., .F., .F.,
 ( 4, 2, 2, 2, 4 ),
 ( 0.000000000000000000, 0.2500000000000000000, 0.5000000000000000000, 0.7500000000000000000, 1.000000000000000000 ),
 .UNSPECIFIED. ) ;
#65122=CIRCLE ( 'NONE', #60651, 0.7499999936418002555 ) ;
#65133=CARTESIAN_POINT ( 'NONE',  ( 10.18988779216199880, -2.943881405003000218, -7.880862084500499520 ) ) ;
#65148=CARTESIAN_POINT ( 'NONE',  ( 10.98146005378009882, -3.088328798999600000, -7.013182449205100255 ) ) ;
#65150=CARTESIAN_POINT ( 'NONE',  ( 10.53976354018315753, -3.672815144550900524, -8.717465845835397076 ) ) ;
#65155=CARTESIAN_POINT ( 'NONE',  ( 8.776575450301999481, -4.067929031554969654, -8.439408300974900357 ) ) ;
#65187=DIRECTION ( 'NONE',  ( -1.000000000000000000, 0.000000000000000000, 0.000000000000000000 ) ) ;
#65189=AXIS2_PLACEMENT_3D ( 'NONE', #51999, #47115, #20192 ) ;
#65272=CARTESIAN_POINT ( 'NONE',  ( 10.72333863405319931, -3.380905141010200232, -8.289729326049599223 ) ) ;
#65276=CARTESIAN_POINT ( 'NONE',  ( 11.46989666366029859, -4.058428102321880004, -8.814970315645998866 ) ) ;
#65307=CARTESIAN_POINT ( 'NONE',  ( 10.66579975933730040, -2.791514215189000225, -7.084213409908699965 ) ) ;
#65358=CARTESIAN_POINT ( 'NONE',  ( 10.34995525820099971, -4.107710726525199973, -6.364355462479999836 ) ) ;
#65362=CARTESIAN_POINT ( 'NONE',  ( 11.59999999999999787, -4.198022108741683134, -8.571335789050445797 ) ) ;
#65373=CARTESIAN_POINT ( 'NONE',  ( 9.657025935145998830, -4.165792341207500193, -6.370288821165999593 ) ) ;
#65389=CARTESIAN_POINT ( 'NONE',  ( 10.45672469555900008, -3.566534988568399900, -6.750062220519700062 ) ) ;
#65399=CARTESIAN_POINT ( 'NONE',  ( 11.07273594314529142, -2.871094011463778184, -7.175020482857276782 ) ) ;
#65407=CARTESIAN_POINT ( 'NONE',  ( 11.30361999289329944, -4.544092497359196514, -6.342116603374310380 ) ) ;
#65426=CARTESIAN_POINT ( 'NONE',  ( 10.78887616594230003, -4.386455737425299262, -6.281817606595999415 ) ) ;
#65485=CARTESIAN_POINT ( 'NONE',  ( 8.950772138681999834, -4.373757805842100055, -6.567719246739500250 ) ) ;
#65502=CARTESIAN_POINT ( 'NONE',  ( 10.43559687351661758, -5.092232985442824322, -8.129523725463622341 ) ) ;
#65507=SURFACE_SIDE_STYLE ('',( #39644 ) ) ;
#65514=CARTESIAN_POINT ( 'NONE',  ( 10.51414141025500015, -3.384226587288500010, -8.596754040696000132 ) ) ;
#65533=B_SPLINE_CURVE_WITH_KNOTS ( 'NONE', 3,
 ( #11584, #37140, #64373, #42728, #48661, #22772 ),
 .UNSPECIFIED., .F., .F.,
 ( 4, 2, 4 ),
 ( 0.000000000000000000, 0.5000000000000000000, 1.000000000000000000 ),
 .UNSPECIFIED. ) ;
#65622=CARTESIAN_POINT ( 'NONE',  ( 10.68035971519489813, -3.321859513918399731, -6.371865185335000348 ) ) ;
#65655=CARTESIAN_POINT ( 'NONE',  ( 10.81349144726329925, -4.738947899111299655, -6.457276458983999490 ) ) ;
#65662=ORIENTED_EDGE ( 'NONE', *, *, #27109, .T. ) ;
#65707=CARTESIAN_POINT ( 'NONE',  ( 11.18687482311539938, -2.942322404451000128, -7.927326830586499007 ) ) ;
#65710=CARTESIAN_POINT ( 'NONE',  ( 11.59999999999999964, -3.075975407729480526, -8.335607184109880663 ) ) ;
#65722=CARTESIAN_POINT ( 'NONE',  ( 10.18491290906799840, -4.548591194283900130, -8.171383386399000415 ) ) ;
#65740=CARTESIAN_POINT ( 'NONE',  ( 10.67826222744820086, -4.668580868411999596, -8.050725169876500331 ) ) ;
#65776=CARTESIAN_POINT ( 'NONE',  ( 8.719914745407999490, -4.065337473341759988, -8.403568966271999230 ) ) ;
#65833=CARTESIAN_POINT ( 'NONE',  ( 9.356038493598999750, -3.273092657276900130, -6.806856425099999441 ) ) ;
#65834=CARTESIAN_POINT ( 'NONE',  ( 9.771013540183334456, -4.768183399968641822, -6.500416447002272058 ) ) ;
#65862=CARTESIAN_POINT ( 'NONE',  ( 11.09590547754519996, -2.684394667508000154, -7.541753805330609239 ) ) ;
#65886=CARTESIAN_POINT ( 'NONE',  ( 10.52022949779799887, -3.290320231472799950, -8.564302809495998758 ) ) ;
#65963=CARTESIAN_POINT ( 'NONE',  ( 10.89835090130999973, -3.121033016283800254, -8.043647632228999811 ) ) ;
#65995=CARTESIAN_POINT ( 'NONE',  ( 10.51810807141099779, -3.940954591493389891, -8.776647962565998995 ) ) ;
#66049=CARTESIAN_POINT ( 'NONE',  ( 11.49056651104150006, -3.914543207408039738, -6.638028001068500217 ) ) ;
#66050=CARTESIAN_POINT ( 'NONE',  ( 11.26072066707849828, -3.023932655881500065, -6.909591111168198907 ) ) ;
#66067=CARTESIAN_POINT ( 'NONE',  ( 9.249747021775998945, -4.754947163618299832, -8.162493079567200382 ) ) ;
#66082=B_SPLINE_CURVE_WITH_KNOTS ( 'NONE', 3,
 ( #54234, #43764, #44807, #7734 ),
 .UNSPECIFIED., .F., .F.,
 ( 4, 4 ),
 ( 0.000000000000000000, 1.000000000000000000 ),
 .UNSPECIFIED. ) ;
#66083=CARTESIAN_POINT ( 'NONE',  ( 11.07210672858429845, -4.692204557952299737, -6.979277962544199632 ) ) ;
#66120=CARTESIAN_POINT ( 'NONE',  ( 10.61656919669529842, -2.774362666861999838, -7.862118085997298778 ) ) ;
#66125=CARTESIAN_POINT ( 'NONE',  ( 11.57299956498156845, -2.792989229543000107, -7.825000000000000178 ) ) ;
#66180=CARTESIAN_POINT ( 'NONE',  ( 9.176721904869998170, -3.004358235431599855, -8.058956102599799109 ) ) ;
#66182=CARTESIAN_POINT ( 'NONE',  ( 9.646013540183332680, -3.000416447002271170, -6.731816600031360842 ) ) ;
#66195=CARTESIAN_POINT ( 'NONE',  ( 10.47726354018323214, -4.629523725463626782, -8.592232985442821658 ) ) ;
#66208=DIRECTION ( 'NONE',  ( 0.000000000000000000, -1.000000000000000000, 0.000000000000000000 ) ) ;
#66266=DIRECTION ( 'NONE',  ( 1.000000000000000000, 0.000000000000000000, 0.000000000000000000 ) ) ;
#66279=CARTESIAN_POINT ( 'NONE',  ( 10.40299135172147693, -3.204747416617449218, -7.137146156348714854 ) ) ;
#66306=CARTESIAN_POINT ( 'NONE',  ( 10.02145237372899800, -3.956267952212241479, -8.774080944853649200 ) ) ;
#66311=CARTESIAN_POINT ( 'NONE',  ( 10.37199293566600034, -3.366612813978900220, -8.276990458557699881 ) ) ;
#66345=CARTESIAN_POINT ( 'NONE',  ( 10.21924205624999971, -4.310927436352299580, -8.309340504471899536 ) ) ;
#66362=CARTESIAN_POINT ( 'NONE',  ( 11.01279632507519857, -3.375091146194399983, -8.658468685623999406 ) ) ;
#66396=CARTESIAN_POINT ( 'NONE',  ( 11.42887348028849992, -5.124210964533999935, -8.107837221875000111 ) ) ;
#66413=CARTESIAN_POINT ( 'NONE',  ( 9.906292290062998163, -3.250213325543700016, -7.064651992867799990 ) ) ;
#66429=CARTESIAN_POINT ( 'NONE',  ( 10.70287750876920008, -4.469200303112399908, -8.228113772635300194 ) ) ;
#66464=CARTESIAN_POINT ( 'NONE',  ( 10.41964694612699915, -5.186980343482999523, -7.973702485506099613 ) ) ;
#66476=CARTESIAN_POINT ( 'NONE',  ( 11.68333460557258796, -3.837988184179999873, -8.490304555719900392 ) ) ;
#66516=CARTESIAN_POINT ( 'NONE',  ( 10.69601354018300832, -3.000416447002272058, -6.731816600031361730 ) ) ;
#66524=CARTESIAN_POINT ( 'NONE',  ( 9.354025935145999782, -4.165792341207500193, -6.370288821165999593 ) ) ;
#66540=CARTESIAN_POINT ( 'NONE',  ( 10.60226354018307937, -2.907767014557176566, -8.129523725463620565 ) ) ;
#66545=FACE_OUTER_BOUND ( 'NONE', #12889, .T. ) ;
#66553=CARTESIAN_POINT ( 'NONE',  ( 11.64633327354034797, -4.864904118400500188, -6.934277916748599502 ) ) ;
#66578=CARTESIAN_POINT ( 'NONE',  ( 10.41891290906799838, -4.809406943772300380, -8.490578012456198920 ) ) ;
#66627=CARTESIAN_POINT ( 'NONE',  ( 10.47683719568447636, -3.813711395361371714, -6.645958924689391090 ) ) ;
#66660=CARTESIAN_POINT ( 'NONE',  ( 11.56833327354034857, -4.746587807672299597, -7.011667014989399149 ) ) ;
#66709=CARTESIAN_POINT ( 'NONE',  ( 11.60477869730532774, -4.467447516829900600, -6.578238193496799724 ) ) ;
#66741=CARTESIAN_POINT ( 'NONE',  ( 11.85979573085659844, -3.159987984332300215, -7.645349278262099979 ) ) ;
#66742=CARTESIAN_POINT ( 'NONE',  ( 10.86272200990529946, -5.206705454565000224, -7.079074440652799893 ) ) ;
#66760=CARTESIAN_POINT ( 'NONE',  ( 10.21024205624999937, -4.310927436352299580, -8.309340504471899536 ) ) ;
#66779=CARTESIAN_POINT ( 'NONE',  ( 10.82179975933729921, -3.051121678931899783, -7.173532873542499466 ) ) ;
#66827=CARTESIAN_POINT ( 'NONE',  ( 10.75210807141120029, -3.959980833595939664, -8.365272822098500427 ) ) ;
#66861=EDGE_CURVE ( 'NONE', #60220, #6314, #32200, .T. ) ;
#66870=CARTESIAN_POINT ( 'NONE',  ( 9.759292290062999697, -3.012566816337000297, -6.926667499798199401 ) ) ;
#66897=CARTESIAN_POINT ( 'NONE',  ( 10.43614141025499897, -3.450366949021700158, -8.478951440767898973 ) ) ;
#66902=DIRECTION ( 'NONE',  ( -1.000000000000000000, 0.000000000000000000, 0.000000000000000000 ) ) ;
#66922=CARTESIAN_POINT ( 'NONE',  ( 8.975151519677000422, -3.972335373863620234, -8.778912113473998247 ) ) ;
#66971=ORIENTED_EDGE ( 'NONE', *, *, #52580, .T. ) ;
#66975=ORIENTED_EDGE ( 'NONE', *, *, #10142, .F. ) ;
#66990=CARTESIAN_POINT ( 'NONE',  ( 8.810863317747999801, -3.039136629551499880, -7.500000000073117512 ) ) ;
#66999=CARTESIAN_POINT ( 'NONE',  ( 10.81013259637009938, -5.031671030421000168, -8.062151801142800167 ) ) ;
#67026=ORIENTED_EDGE ( 'NONE', *, *, #13683, .F. ) ;
#67034=CARTESIAN_POINT ( 'NONE',  ( 9.408709346416998187, -3.216804796119200116, -7.128095150442700145 ) ) ;
#67050=CARTESIAN_POINT ( 'NONE',  ( 10.81013259637009938, -5.031671030421000168, -8.062151801142800167 ) ) ;
#67066=CARTESIAN_POINT ( 'NONE',  ( 9.099999931440999390, -4.000000000000000000, -7.500000000000000000 ) ) ;
#67078=CARTESIAN_POINT ( 'NONE',  ( 10.59195391537400077, -2.942766577210000012, -8.218034727798299244 ) ) ;
#67080=FACE_OUTER_BOUND ( 'NONE', #50081, .T. ) ;
#67098=CARTESIAN_POINT ( 'NONE',  ( 9.401721904869997815, -3.124169273628900179, -7.991693846894699860 ) ) ;
#67115=CARTESIAN_POINT ( 'NONE',  ( 11.75718044953559804, -3.110233631466100324, -7.963966784336999005 ) ) ;
#67161=CARTESIAN_POINT ( 'NONE',  ( 11.39210538575740017, -3.157545584346100220, -7.298582155985900322 ) ) ;
#67208=CARTESIAN_POINT ( 'NONE',  ( 8.847442991499999465, -4.071878040089889517, -6.360452723514999462 ) ) ;
#67235=CARTESIAN_POINT ( 'NONE',  ( 11.35545123989519922, -3.524778630617700248, -8.417769225118700405 ) ) ;
#67259=CARTESIAN_POINT ( 'NONE',  ( 9.329759580229000093, -5.244164909883999748, -7.202614619576299226 ) ) ;
#67335=CARTESIAN_POINT ( 'NONE',  ( 11.67403632436368888, -4.976178716761900489, -7.272033745815799755 ) ) ;
#67366=CARTESIAN_POINT ( 'NONE',  ( 10.22272469555899832, -3.360453478306600239, -6.393520617113999549 ) ) ;
#67370=CARTESIAN_POINT ( 'NONE',  ( 10.06726717315599906, -4.659895246859299789, -6.937642277832399174 ) ) ;
#67386=CARTESIAN_POINT ( 'NONE',  ( 11.26212378248529866, -4.615095948180499619, -6.336291382830999908 ) ) ;
#67415=CARTESIAN_POINT ( 'NONE',  ( 11.31825954179440075, -3.333768806796900019, -8.053565341712399572 ) ) ;
#67417=CARTESIAN_POINT ( 'NONE',  ( 10.14887885159599890, -2.730985436695000157, -7.348611220446799486 ) ) ;
#67434=CARTESIAN_POINT ( 'NONE',  ( 9.146417874593998576, -4.797903641662700558, -7.839201596587598964 ) ) ;
#67445=ORIENTED_EDGE ( 'NONE', *, *, #40750, .T. ) ;
#67453=CARTESIAN_POINT ( 'NONE',  ( 10.35410941423799791, -3.257202320419700037, -6.825313060354999628 ) ) ;
#67503=CARTESIAN_POINT ( 'NONE',  ( 10.06276198887462847, -4.665935521472182934, -6.932494801640175730 ) ) ;
#67507=CARTESIAN_POINT ( 'NONE',  ( 10.97364560330029981, -3.734560974198899874, -6.675475461903199736 ) ) ;
#67551=CARTESIAN_POINT ( 'NONE',  ( 9.050076168957998490, -4.579425901182000658, -8.483869947211399420 ) ) ;
#67578=CARTESIAN_POINT ( 'NONE',  ( 10.93479632507519916, -3.442212747724900268, -8.534037301706000278 ) ) ;
#67670=CARTESIAN_POINT ( 'NONE',  ( 10.06927318630900103, -3.243547362524661359, -8.526145288591964189 ) ) ;
#67707=B_SPLINE_CURVE_WITH_KNOTS ( 'NONE', 3,
 ( #35713, #31499, #21006, #62944, #42341, #31845, #46890, #57031, #63641, #4226, #5262, #30469, #25213, #41301, #68194, #14732, #57364, #9469 ),
 .UNSPECIFIED., .F., .F.,
 ( 4, 2, 2, 2, 2, 2, 2, 2, 4 ),
 ( 0.000000000000000000, 0.1250000000000000000, 0.2500000000000000000, 0.3750000000000000000, 0.5000000000000000000, 0.6250000000000000000, 0.7500000000000000000, 0.8750000000000000000, 1.000000000000000000 ),
 .UNSPECIFIED. ) ;
#67755=CARTESIAN_POINT ( 'NONE',  ( 10.97364560330029981, -3.734560974198899874, -6.675475461903199736 ) ) ;
#67756=CARTESIAN_POINT ( 'NONE',  ( 10.81349144726329925, -4.738947899111299655, -6.457276458983999490 ) ) ;
#67778=CARTESIAN_POINT ( 'NONE',  ( 8.893126402770997530, -3.188752782784400441, -7.194081880505399873 ) ) ;
#67798=CARTESIAN_POINT ( 'NONE',  ( 11.04333729122639873, -5.003122373830000136, -7.473611442402849470 ) ) ;
#67838=CARTESIAN_POINT ( 'NONE',  ( 9.140654977342494547, -2.950420301507454379, -6.802596805975135830 ) ) ;
#67844=CARTESIAN_POINT ( 'NONE',  ( 10.03743284169262573, -4.454886069780877200, -6.752597208702827203 ) ) ;
#67849=CARTESIAN_POINT ( 'NONE',  ( 10.85056919669530018, -3.169300617545700138, -7.745432529082900253 ) ) ;
#67868=CARTESIAN_POINT ( 'NONE',  ( 10.79184687351629890, -4.999583552997724389, -6.731816600031356401 ) ) ;
#67875=AXIS2_PLACEMENT_3D ( 'NONE', #68294, #68639, #9923 ) ;
#67899=CARTESIAN_POINT ( 'NONE',  ( 9.225367640781000134, -3.396982508013000501, -6.371835875489000323 ) ) ;
#67925=CARTESIAN_POINT ( 'NONE',  ( 10.85679632507500081, -3.509334349252600127, -8.409605917786398877 ) ) ;
#67926=CARTESIAN_POINT ( 'NONE',  ( 11.60000000000000142, -3.752125624359933909, -6.451199048602688002 ) ) ;
#67987=VERTEX_POINT ( 'NONE', #16326 ) ;
#68008=ORIENTED_EDGE ( 'NONE', *, *, #23599, .F. ) ;
#68026=CARTESIAN_POINT ( 'NONE',  ( 10.61257802013489737, -4.891884252872400474, -7.479237407015119743 ) ) ;
#68030=CARTESIAN_POINT ( 'NONE',  ( 11.21253483539785201, -4.338990010211682069, -8.308639362931229400 ) ) ;
#68101=CARTESIAN_POINT ( 'NONE',  ( 10.92441504065829960, -3.305585767322499979, -6.982228367137699898 ) ) ;
#68140=CARTESIAN_POINT ( 'NONE',  ( 11.38795122972049967, -3.601717549869600354, -6.578956058177199751 ) ) ;
#68178=CARTESIAN_POINT ( 'NONE',  ( 9.171146261768624797, -3.287258916643901241, -6.460774852777244170 ) ) ;
#68185=CARTESIAN_POINT ( 'NONE',  ( 9.328216720588626387, -3.237060173287368503, -7.928316576537355331 ) ) ;
#68189=CARTESIAN_POINT ( 'NONE',  ( 11.67918044953561996, -2.988516238873000219, -8.027436060358800418 ) ) ;
#68194=CARTESIAN_POINT ( 'NONE',  ( 10.18559687351583243, -2.907767014557174790, -6.870476274536379435 ) ) ;
#68235=CARTESIAN_POINT ( 'NONE',  ( 9.934583761885999564, -5.078750111091999919, -8.187519150726398465 ) ) ;
#68262=CARTESIAN_POINT ( 'NONE',  ( 11.40211496860029783, -3.206052520092899982, -7.093139000852099585 ) ) ;
#68277=B_SPLINE_CURVE_WITH_KNOTS ( 'NONE', 3,
 ( #58013, #63238, #31111, #10450 ),
 .UNSPECIFIED., .F., .F.,
 ( 4, 4 ),
 ( 0.000000000000000000, 1.000000000000000000 ),
 .UNSPECIFIED. ) ;
#68294=CARTESIAN_POINT ( 'NONE',  ( 11.59999999999999964, -4.000000000000000000, -7.500000000000000000 ) ) ;
#68363=CARTESIAN_POINT ( 'NONE',  ( 9.560596873515667227, -3.370476274536376771, -8.592232985442823434 ) ) ;
#68385=CARTESIAN_POINT ( 'NONE',  ( 11.25740844561608611, -2.954218652640771214, -7.175000373111195984 ) ) ;
#68430=CARTESIAN_POINT ( 'NONE',  ( 9.143927823787141307, -2.750011555256801188, -7.499999844943244121 ) ) ;
#68432=CARTESIAN_POINT ( 'NONE',  ( 11.59999999999999964, -2.935681553670999921, -8.155535082817699788 ) ) ;
#68442=CARTESIAN_POINT ( 'NONE',  ( 11.48641235500450009, -4.739919807690899489, -6.822158181405299615 ) ) ;
#68458=CARTESIAN_POINT ( 'NONE',  ( 9.222405316139999698, -4.184077495686000958, -8.347244604637999998 ) ) ;
#68478=CARTESIAN_POINT ( 'NONE',  ( 10.79303032197930001, -3.336467919271199900, -6.572090902022299730 ) ) ;
#68520=CARTESIAN_POINT ( 'NONE',  ( 9.242292592096250203, -4.365494583328262124, -6.294013902202234334 ) ) ;
#68527=CARTESIAN_POINT ( 'NONE',  ( 10.18940772478662637, -4.553612660159668479, -8.177528816364860731 ) ) ;
#68531=CARTESIAN_POINT ( 'NONE',  ( 11.28949010443639978, -2.999324937259999935, -7.574834962826040297 ) ) ;
#68547=CARTESIAN_POINT ( 'NONE',  ( 10.13827973160999818, -3.897539901865500145, -6.362794488108000301 ) ) ;
#68563=CARTESIAN_POINT ( 'NONE',  ( 9.057169810767971896, -3.796486612318636933, -8.707169876682314680 ) ) ;
#68578=AXIS2_PLACEMENT_3D ( 'NONE', #50822, #57774, #31563 ) ;
#68579=CARTESIAN_POINT ( 'NONE',  ( 8.769442991499998286, -4.080527519162810535, -6.223324745230999433 ) ) ;
#68583=CARTESIAN_POINT ( 'NONE',  ( 9.099999931440999390, -2.935682118448999844, -8.155535999783198875 ) ) ;
#68602=CARTESIAN_POINT ( 'NONE',  ( 11.33041235500449950, -4.942357465271699724, -6.636704692336500067 ) ) ;
#68608=CARTESIAN_POINT ( 'NONE',  ( 10.57102344389999971, -4.762665848028800220, -7.037150754511299233 ) ) ;
#68639=DIRECTION ( 'NONE',  ( -1.000000000000000000, 0.000000000000000000, 0.000000000000000000 ) ) ;
#68661=CARTESIAN_POINT ( 'NONE',  ( 9.712659112603999390, -4.376739491155700712, -8.280881105104999307 ) ) ;
#68676=CARTESIAN_POINT ( 'NONE',  ( 11.14256920625030034, -3.957769094421040190, -6.325872106312999676 ) ) ;
#68694=CARTESIAN_POINT ( 'NONE',  ( 9.541846873516668381, -3.000416447002275611, -8.268183399968640046 ) ) ;
#68760=CARTESIAN_POINT ( 'NONE',  ( 10.89529697814178100, -3.173432105636238454, -7.215614489968412926 ) ) ;
#68791=CARTESIAN_POINT ( 'NONE',  ( 10.60441638348510018, -4.841589649988700117, -7.294998899090099798 ) ) ;
#68807=ORIENTED_EDGE ( 'NONE', *, *, #11583, .F. ) ;
#68810=CARTESIAN_POINT ( 'NONE',  ( 9.602342523874998648, -4.857027829858100887, -7.368808371628100318 ) ) ;
#68829=CARTESIAN_POINT ( 'NONE',  ( 10.42380110216399913, -4.973546009874400653, -6.905442784147899360 ) ) ;
#68882=CARTESIAN_POINT ( 'NONE',  ( 10.74795391537419853, -3.169881940022800215, -8.063786182297898009 ) ) ;
#68890=B_SPLINE_CURVE_WITH_KNOTS ( 'NONE', 3,
 ( #19125, #40449, #34191, #61775 ),
 .UNSPECIFIED., .F., .F.,
 ( 4, 4 ),
 ( 0.000000000000000000, 1.000000000000000000 ),
 .UNSPECIFIED. ) ;
#68899=CARTESIAN_POINT ( 'NONE',  ( 10.41690035061499842, -3.695660922043800145, -8.600505223349999895 ) ) ;
#68915=CARTESIAN_POINT ( 'NONE',  ( 11.28830977893788123, -4.976598135215292373, -6.673569913327194847 ) ) ;
#68932=CARTESIAN_POINT ( 'NONE',  ( 9.883925467520999320, -5.276153033933000280, -7.411581555133209598 ) ) ;
#68947=CARTESIAN_POINT ( 'NONE',  ( 11.08810207955139937, -4.796537143354000499, -7.174999999999999822 ) ) ;
#68954=CARTESIAN_POINT ( 'NONE',  ( 10.27610941423800028, -3.155589807313900153, -6.733017893878099791 ) ) ;
#68962=CARTESIAN_POINT ( 'NONE',  ( 9.789763540182331525, -4.327184855449096368, -6.282534154164603812 ) ) ;
#69012=CARTESIAN_POINT ( 'NONE',  ( 9.586013376692998023, -4.772923352651200268, -7.107192877568799361 ) ) ;
#69028=CARTESIAN_POINT ( 'NONE',  ( 11.35545123989519922, -3.524778630617700248, -8.417769225118700405 ) ) ;
#69047=CARTESIAN_POINT ( 'NONE',  ( 9.552263540183332680, -2.907767014557177898, -8.129523725463625894 ) ) ;
#69143=CARTESIAN_POINT ( 'NONE',  ( 10.67826222744820086, -4.668580868411999596, -8.050725169876500331 ) ) ;
#69176=CARTESIAN_POINT ( 'NONE',  ( 11.55610404293055993, -4.502836909561000134, -8.523936114709998790 ) ) ;
ENDSEC;
END-ISO-10303-21;
